ISO-10303-21;
HEADER;
/* Generated by software containing ST-Developer
 * from STEP Tools, Inc. (www.steptools.com) 
 */

FILE_DESCRIPTION(
/* description */ ('Independent equipment support assembly with bolted 600 x 500 mm welde
d perimeter frame, four adjustable legs and swivel feet. Nominal overa
ll height 518 mm. No load rating assigned.'),
/* implementation_level */ '2;1');

FILE_NAME(
/* name */ 'Socket head cap screw M10x20.step',
/* time_stamp */ '2026-11-07T17:30:39-08:00',
/* author */ (''),
/* organization */ (''),
/* preprocessor_version */ 'ST-DEVELOPER v20.2',
/* originating_system */ 'Autodesk Translation Framework v15.17.0.0',
/* authorisation */ '');

FILE_SCHEMA (('AUTOMOTIVE_DESIGN { 1 0 10303 214 3 1 1 }'));
ENDSEC;

DATA;
#10=MECHANICAL_DESIGN_GEOMETRIC_PRESENTATION_REPRESENTATION('',(#2215),#63755);
#255=CONICAL_SURFACE('',#15120,4.5,0.785398163397448);
#271=B_SPLINE_SURFACE_WITH_KNOTS('',3,3,((#45785,#45786,#45787,#45788,#45789,
#45790,#45791,#45792,#45793,#45794,#45795,#45796,#45797,#45798,#45799,#45800,
#45801,#45802,#45803,#45804,#45805,#45806,#45807,#45808,#45809,#45810,#45811,
#45812,#45813,#45814,#45815,#45816,#45817,#45818,#45819,#45820,#45821,#45822,
#45823,#45824,#45825,#45826,#45827,#45828,#45829,#45830,#45831,#45832,#45833,
#45834,#45835,#45836,#45837,#45838,#45839,#45840,#45841,#45842,#45843,#45844,
#45845,#45846,#45847,#45848,#45849,#45850,#45851,#45852,#45853,#45854,#45855,
#45856,#45857,#45858,#45859,#45860,#45861,#45862,#45863,#45864,#45865,#45866,
#45867,#45868,#45869,#45870,#45871,#45872,#45873,#45874,#45875,#45876,#45877,
#45878,#45879,#45880,#45881,#45882,#45883,#45884,#45885,#45886,#45887,#45888,
#45889,#45890,#45891,#45892,#45893,#45894,#45895,#45896,#45897,#45898,#45899,
#45900,#45901,#45902,#45903,#45904,#45905,#45906,#45907,#45908,#45909,#45910,
#45911,#45912,#45913),(#45914,#45915,#45916,#45917,#45918,#45919,#45920,
#45921,#45922,#45923,#45924,#45925,#45926,#45927,#45928,#45929,#45930,#45931,
#45932,#45933,#45934,#45935,#45936,#45937,#45938,#45939,#45940,#45941,#45942,
#45943,#45944,#45945,#45946,#45947,#45948,#45949,#45950,#45951,#45952,#45953,
#45954,#45955,#45956,#45957,#45958,#45959,#45960,#45961,#45962,#45963,#45964,
#45965,#45966,#45967,#45968,#45969,#45970,#45971,#45972,#45973,#45974,#45975,
#45976,#45977,#45978,#45979,#45980,#45981,#45982,#45983,#45984,#45985,#45986,
#45987,#45988,#45989,#45990,#45991,#45992,#45993,#45994,#45995,#45996,#45997,
#45998,#45999,#46000,#46001,#46002,#46003,#46004,#46005,#46006,#46007,#46008,
#46009,#46010,#46011,#46012,#46013,#46014,#46015,#46016,#46017,#46018,#46019,
#46020,#46021,#46022,#46023,#46024,#46025,#46026,#46027,#46028,#46029,#46030,
#46031,#46032,#46033,#46034,#46035,#46036,#46037,#46038,#46039,#46040,#46041,
#46042),(#46043,#46044,#46045,#46046,#46047,#46048,#46049,#46050,#46051,
#46052,#46053,#46054,#46055,#46056,#46057,#46058,#46059,#46060,#46061,#46062,
#46063,#46064,#46065,#46066,#46067,#46068,#46069,#46070,#46071,#46072,#46073,
#46074,#46075,#46076,#46077,#46078,#46079,#46080,#46081,#46082,#46083,#46084,
#46085,#46086,#46087,#46088,#46089,#46090,#46091,#46092,#46093,#46094,#46095,
#46096,#46097,#46098,#46099,#46100,#46101,#46102,#46103,#46104,#46105,#46106,
#46107,#46108,#46109,#46110,#46111,#46112,#46113,#46114,#46115,#46116,#46117,
#46118,#46119,#46120,#46121,#46122,#46123,#46124,#46125,#46126,#46127,#46128,
#46129,#46130,#46131,#46132,#46133,#46134,#46135,#46136,#46137,#46138,#46139,
#46140,#46141,#46142,#46143,#46144,#46145,#46146,#46147,#46148,#46149,#46150,
#46151,#46152,#46153,#46154,#46155,#46156,#46157,#46158,#46159,#46160,#46161,
#46162,#46163,#46164,#46165,#46166,#46167,#46168,#46169,#46170,#46171),
(#46172,#46173,#46174,#46175,#46176,#46177,#46178,#46179,#46180,#46181,
#46182,#46183,#46184,#46185,#46186,#46187,#46188,#46189,#46190,#46191,#46192,
#46193,#46194,#46195,#46196,#46197,#46198,#46199,#46200,#46201,#46202,#46203,
#46204,#46205,#46206,#46207,#46208,#46209,#46210,#46211,#46212,#46213,#46214,
#46215,#46216,#46217,#46218,#46219,#46220,#46221,#46222,#46223,#46224,#46225,
#46226,#46227,#46228,#46229,#46230,#46231,#46232,#46233,#46234,#46235,#46236,
#46237,#46238,#46239,#46240,#46241,#46242,#46243,#46244,#46245,#46246,#46247,
#46248,#46249,#46250,#46251,#46252,#46253,#46254,#46255,#46256,#46257,#46258,
#46259,#46260,#46261,#46262,#46263,#46264,#46265,#46266,#46267,#46268,#46269,
#46270,#46271,#46272,#46273,#46274,#46275,#46276,#46277,#46278,#46279,#46280,
#46281,#46282,#46283,#46284,#46285,#46286,#46287,#46288,#46289,#46290,#46291,
#46292,#46293,#46294,#46295,#46296,#46297,#46298,#46299,#46300)),
 .UNSPECIFIED.,.F.,.F.,.F.,(4,4),(4,1,1,1,1,1,1,1,1,1,1,1,1,1,1,1,1,1,1,
1,1,1,1,1,1,1,1,1,1,1,1,1,1,1,1,1,1,1,1,1,1,1,1,1,1,1,1,1,1,1,1,1,1,1,1,
1,1,1,1,1,1,1,1,1,1,1,1,1,1,1,1,1,1,1,1,1,1,1,1,1,1,1,1,1,1,1,1,1,1,1,1,
1,1,1,1,1,1,1,1,1,1,1,1,1,1,1,1,1,1,1,1,1,1,1,1,1,1,1,1,1,1,1,1,1,1,1,4),
(0.,0.0658179306876173),(11.6150328478182,12.1123165623719,12.6096002769257,
13.6041677060331,14.5987351351405,15.5933025642479,16.5878699933554,17.5824374224628,
18.5770048515702,19.5715722806776,20.5661397097851,21.5607071388925,22.5552745679999,
23.5498419971074,24.5444094262148,25.5389768553222,26.5335442844296,27.5281117135371,
28.5226791426445,29.5172465717519,30.5118140008593,31.5063814299668,32.5009488590742,
33.4955162881816,34.490083717289,35.4846511463965,36.4792185755039,37.4737860046113,
38.4683534337187,39.4629208628262,40.4574882919336,41.452055721041,42.4466231501485,
43.4411905792559,44.4357580083633,45.4303254374707,46.4248928665782,47.4194602956856,
48.414027724793,49.4085951539004,50.4031625830079,51.3977300121153,52.3922974412227,
53.3868648703302,54.3814322994376,55.375999728545,56.3705671576524,57.3651345867599,
58.3597020158673,59.3542694449747,60.3488368740821,61.3434043031896,62.337971732297,
63.3325391614044,64.3271065905118,65.3216740196193,66.3162414487267,67.3108088778341,
68.3053763069416,69.299943736049,70.2945111651564,71.2890785942638,72.2836460233713,
73.2782134524787,74.2727808815861,75.2673483106935,76.261915739801,77.2564831689084,
78.2510505980158,79.2456180271232,80.2401854562307,81.2347528853381,82.2293203144455,
83.223887743553,84.2184551726604,85.2130226017678,86.2075900308752,87.2021574599827,
88.1967248890901,89.1912923181975,90.1858597473049,91.1804271764124,92.1749946055198,
93.1695620346272,94.1641294637347,95.1586968928421,96.1532643219495,97.1478317510569,
98.1423991801644,99.1369666092718,100.131534038379,101.126101467487,102.120668896594,
103.115236325701,104.109803754809,105.104371183916,106.098938613024,107.093506042131,
108.088073471239,109.082640900346,110.077208329453,111.071775758561,112.066343187668,
113.060910616776,114.055478045883,115.050045474991,116.044612904098,117.039180333205,
118.033747762313,119.02831519142,120.022882620528,121.017450049635,122.012017478743,
123.00658490785,124.001152336957,124.995719766065,125.990287195172,126.98485462428,
127.979422053387,128.973989482495,129.968556911602,130.963124340709,131.957691769817,
132.952259198924,133.946826628032,134.444110342585,134.941394057139),
 .UNSPECIFIED.);
#272=B_SPLINE_SURFACE_WITH_KNOTS('',3,3,((#46445,#46446,#46447,#46448,#46449,
#46450,#46451,#46452,#46453,#46454,#46455,#46456,#46457,#46458,#46459,#46460,
#46461,#46462,#46463,#46464,#46465,#46466,#46467,#46468,#46469,#46470,#46471,
#46472,#46473,#46474,#46475,#46476,#46477,#46478,#46479,#46480,#46481,#46482,
#46483,#46484,#46485,#46486,#46487,#46488,#46489,#46490,#46491,#46492,#46493,
#46494,#46495,#46496,#46497,#46498,#46499,#46500,#46501,#46502,#46503,#46504,
#46505,#46506,#46507,#46508,#46509,#46510,#46511,#46512,#46513,#46514,#46515,
#46516,#46517,#46518,#46519,#46520,#46521,#46522,#46523,#46524,#46525,#46526,
#46527,#46528,#46529,#46530,#46531,#46532,#46533,#46534,#46535,#46536,#46537,
#46538,#46539,#46540,#46541,#46542,#46543,#46544,#46545,#46546,#46547,#46548,
#46549,#46550,#46551,#46552,#46553,#46554,#46555,#46556,#46557,#46558,#46559,
#46560,#46561,#46562,#46563,#46564,#46565,#46566,#46567,#46568,#46569,#46570,
#46571,#46572,#46573,#46574,#46575),(#46576,#46577,#46578,#46579,#46580,
#46581,#46582,#46583,#46584,#46585,#46586,#46587,#46588,#46589,#46590,#46591,
#46592,#46593,#46594,#46595,#46596,#46597,#46598,#46599,#46600,#46601,#46602,
#46603,#46604,#46605,#46606,#46607,#46608,#46609,#46610,#46611,#46612,#46613,
#46614,#46615,#46616,#46617,#46618,#46619,#46620,#46621,#46622,#46623,#46624,
#46625,#46626,#46627,#46628,#46629,#46630,#46631,#46632,#46633,#46634,#46635,
#46636,#46637,#46638,#46639,#46640,#46641,#46642,#46643,#46644,#46645,#46646,
#46647,#46648,#46649,#46650,#46651,#46652,#46653,#46654,#46655,#46656,#46657,
#46658,#46659,#46660,#46661,#46662,#46663,#46664,#46665,#46666,#46667,#46668,
#46669,#46670,#46671,#46672,#46673,#46674,#46675,#46676,#46677,#46678,#46679,
#46680,#46681,#46682,#46683,#46684,#46685,#46686,#46687,#46688,#46689,#46690,
#46691,#46692,#46693,#46694,#46695,#46696,#46697,#46698,#46699,#46700,#46701,
#46702,#46703,#46704,#46705,#46706),(#46707,#46708,#46709,#46710,#46711,
#46712,#46713,#46714,#46715,#46716,#46717,#46718,#46719,#46720,#46721,#46722,
#46723,#46724,#46725,#46726,#46727,#46728,#46729,#46730,#46731,#46732,#46733,
#46734,#46735,#46736,#46737,#46738,#46739,#46740,#46741,#46742,#46743,#46744,
#46745,#46746,#46747,#46748,#46749,#46750,#46751,#46752,#46753,#46754,#46755,
#46756,#46757,#46758,#46759,#46760,#46761,#46762,#46763,#46764,#46765,#46766,
#46767,#46768,#46769,#46770,#46771,#46772,#46773,#46774,#46775,#46776,#46777,
#46778,#46779,#46780,#46781,#46782,#46783,#46784,#46785,#46786,#46787,#46788,
#46789,#46790,#46791,#46792,#46793,#46794,#46795,#46796,#46797,#46798,#46799,
#46800,#46801,#46802,#46803,#46804,#46805,#46806,#46807,#46808,#46809,#46810,
#46811,#46812,#46813,#46814,#46815,#46816,#46817,#46818,#46819,#46820,#46821,
#46822,#46823,#46824,#46825,#46826,#46827,#46828,#46829,#46830,#46831,#46832,
#46833,#46834,#46835,#46836,#46837),(#46838,#46839,#46840,#46841,#46842,
#46843,#46844,#46845,#46846,#46847,#46848,#46849,#46850,#46851,#46852,#46853,
#46854,#46855,#46856,#46857,#46858,#46859,#46860,#46861,#46862,#46863,#46864,
#46865,#46866,#46867,#46868,#46869,#46870,#46871,#46872,#46873,#46874,#46875,
#46876,#46877,#46878,#46879,#46880,#46881,#46882,#46883,#46884,#46885,#46886,
#46887,#46888,#46889,#46890,#46891,#46892,#46893,#46894,#46895,#46896,#46897,
#46898,#46899,#46900,#46901,#46902,#46903,#46904,#46905,#46906,#46907,#46908,
#46909,#46910,#46911,#46912,#46913,#46914,#46915,#46916,#46917,#46918,#46919,
#46920,#46921,#46922,#46923,#46924,#46925,#46926,#46927,#46928,#46929,#46930,
#46931,#46932,#46933,#46934,#46935,#46936,#46937,#46938,#46939,#46940,#46941,
#46942,#46943,#46944,#46945,#46946,#46947,#46948,#46949,#46950,#46951,#46952,
#46953,#46954,#46955,#46956,#46957,#46958,#46959,#46960,#46961,#46962,#46963,
#46964,#46965,#46966,#46967,#46968)),.UNSPECIFIED.,.F.,.F.,.F.,(4,4),(4,
1,1,1,1,1,1,1,1,1,1,1,1,1,1,1,1,1,1,1,1,1,1,1,1,1,1,1,1,1,1,1,1,1,1,1,1,
1,1,1,1,1,1,1,1,1,1,1,1,1,1,1,1,1,1,1,1,1,1,1,1,1,1,1,1,1,1,1,1,1,1,1,1,
1,1,1,1,1,1,1,1,1,1,1,1,1,1,1,1,1,1,1,1,1,1,1,1,1,1,1,1,1,1,1,1,1,1,1,1,
1,1,1,1,1,1,1,1,1,1,1,1,1,1,1,1,1,1,1,4),(0.,0.0658179306876173),(8.30838445208313,
8.80598005718054,9.30357566227795,10.2987668724728,11.2939580826676,12.2891492928624,
13.2843405030573,14.2795317132521,15.2747229234469,16.2699141336417,17.2651053438366,
18.2602965540314,19.2554877642262,20.250678974421,21.2458701846159,22.2410613948107,
23.2362526050055,24.2314438152003,25.2266350253952,26.22182623559,27.2170174457848,
28.2122086559796,29.2073998661744,30.2025910763693,31.1977822865641,32.1929734967589,
33.1881647069537,34.1833559171486,35.1785471273434,36.1737383375382,37.168929547733,
38.1641207579279,39.1593119681227,40.1545031783175,41.1496943885123,42.1448855987072,
43.140076808902,44.1352680190968,45.1304592292916,46.1256504394865,47.1208416496813,
48.1160328598761,49.1112240700709,50.1064152802658,51.1016064904606,52.0967977006554,
53.0919889108502,54.0871801210451,55.0823713312399,56.0775625414347,57.0727537516295,
58.0679449618244,59.0631361720192,60.058327382214,61.0535185924088,62.0487098026037,
63.0439010127985,64.0390922229933,65.0342834331881,66.029474643383,67.0246658535778,
68.0198570637726,69.0150482739674,70.0102394841623,71.0054306943571,72.0006219045519,
72.9958131147467,73.9910043249416,74.9861955351364,75.9813867453312,76.976577955526,
77.9717691657209,78.9669603759157,79.9621515861105,80.9573427963053,81.9525340065002,
82.947725216695,83.9429164268898,84.9381076370846,85.9332988472795,86.9284900574743,
87.9236812676691,88.9188724778639,89.9140636880588,90.9092548982536,91.9044461084484,
92.8996373186432,93.8948285288381,94.8900197390329,95.8852109492277,96.8804021594225,
97.8755933696174,98.8707845798122,99.865975790007,100.861167000202,101.856358210397,
102.851549420591,103.846740630786,104.841931840981,105.837123051176,106.832314261371,
107.827505471566,108.82269668176,109.817887891955,110.81307910215,111.808270312345,
112.80346152254,113.798652732735,114.793843942929,115.789035153124,116.784226363319,
117.779417573514,118.774608783709,119.769799993904,120.764991204098,121.760182414293,
122.755373624488,123.750564834683,124.745756044878,125.740947255072,126.736138465267,
127.731329675462,128.726520885657,129.721712095852,130.716903306047,131.712094516241,
132.707285726436,133.204881331534,133.702476936631),.UNSPECIFIED.);
#418=CIRCLE('',#15081,4.942);
#419=CIRCLE('',#15101,4.372);
#420=CIRCLE('',#15121,4.942);
#421=CIRCLE('',#15122,4.);
#422=CIRCLE('',#15124,4.372);
#423=CIRCLE('',#15134,8.);
#424=CIRCLE('',#15136,8.);
#1028=B_SPLINE_CURVE_WITH_KNOTS('',3,(#44037,#44038,#44039,#44040,#44041,
#44042,#44043,#44044,#44045,#44046),.UNSPECIFIED.,.F.,.F.,(4,3,3,4),(-4.09293042013065,
-3.97826971642971,-2.98370228732228,-2.06773127522702),.UNSPECIFIED.);
#1029=B_SPLINE_CURVE_WITH_KNOTS('',3,(#44049,#44050,#44051,#44052,#44053,
#44054,#44055,#44056,#44057,#44058),.UNSPECIFIED.,.F.,.F.,(4,3,3,4),(0.,
0.49759560509741,0.995191210194833,1.11639350868605),.UNSPECIFIED.);
#1030=B_SPLINE_CURVE_WITH_KNOTS('',3,(#44063,#44064,#44065,#44066,#44067,
#44068,#44069,#44070,#44071,#44072,#44073,#44074,#44075,#44076,#44077,#44078,
#44079,#44080,#44081,#44082,#44083,#44084),.UNSPECIFIED.,.F.,.F.,(4,3,3,
3,3,3,3,4),(-10.3761157273102,-9.94567429107427,-8.95110686196684,-7.95653943285942,
-6.96197200375199,-5.96740457464456,-4.97283714553713,-4.09293042013065),
 .UNSPECIFIED.);
#1031=B_SPLINE_CURVE_WITH_KNOTS('',3,(#44085,#44086,#44087,#44088,#44089,
#44090,#44091,#44092,#44093,#44094,#44095,#44096,#44097,#44098,#44099,#44100,
#44101,#44102,#44103,#44104,#44105,#44106),.UNSPECIFIED.,.F.,.F.,(4,3,3,
3,3,3,3,4),(1.11639350868605,1.99038242038966,2.98557363058448,3.9807648407793,
4.97595605097413,5.97114726116895,6.96633847136377,7.39957881586564),
 .UNSPECIFIED.);
#1032=B_SPLINE_CURVE_WITH_KNOTS('',3,(#44111,#44112,#44113,#44114,#44115,
#44116,#44117,#44118,#44119,#44120,#44121,#44122,#44123,#44124,#44125,#44126,
#44127,#44128,#44129,#44130,#44131,#44132),.UNSPECIFIED.,.F.,.F.,(4,3,3,
3,3,3,3,4),(-16.6593010344898,-15.9130788657188,-14.9185114366114,-13.923944007504,
-12.9293765783965,-11.9348091492891,-10.9402417201817,-10.3761157273102),
 .UNSPECIFIED.);
#1033=B_SPLINE_CURVE_WITH_KNOTS('',3,(#44133,#44134,#44135,#44136,#44137,
#44138,#44139,#44140,#44141,#44142,#44143,#44144,#44145,#44146,#44147,#44148,
#44149,#44150,#44151,#44152,#44153,#44154),.UNSPECIFIED.,.F.,.F.,(4,3,3,
3,3,3,3,4),(7.39957881586564,7.9615296815586,8.95672089175343,9.95191210194825,
10.9471033121431,11.9422945223379,12.9374857325327,13.6827641230452),
 .UNSPECIFIED.);
#1034=B_SPLINE_CURVE_WITH_KNOTS('',3,(#44159,#44160,#44161,#44162,#44163,
#44164,#44165,#44166,#44167,#44168,#44169,#44170,#44171,#44172,#44173,#44174,
#44175,#44176,#44177,#44178,#44179,#44180,#44181,#44182,#44183),
 .UNSPECIFIED.,.F.,.F.,(4,3,3,3,3,3,3,3,4),(-22.9424863416694,-22.8750508694708,
-21.8804834403634,-20.885916011256,-19.8913485821485,-18.8967811530411,
-17.9022137239337,-16.9076462948263,-16.6593010344898),.UNSPECIFIED.);
#1035=B_SPLINE_CURVE_WITH_KNOTS('',3,(#44184,#44185,#44186,#44187,#44188,
#44189,#44190,#44191,#44192,#44193,#44194,#44195,#44196,#44197,#44198,#44199,
#44200,#44201,#44202,#44203,#44204,#44205,#44206,#44207,#44208),
 .UNSPECIFIED.,.F.,.F.,(4,3,3,3,3,3,3,3,4),(13.6827641230452,13.9326769427276,
14.9278681529224,15.9230593631172,16.918250573312,17.9134417835069,18.9086329937017,
19.9038242038965,19.9659494302248),.UNSPECIFIED.);
#1036=B_SPLINE_CURVE_WITH_KNOTS('',3,(#44213,#44214,#44215,#44216,#44217,
#44218,#44219,#44220,#44221,#44222,#44223,#44224,#44225,#44226,#44227,#44228,
#44229,#44230,#44231,#44232,#44233,#44234),.UNSPECIFIED.,.F.,.F.,(4,3,3,
3,3,3,3,4),(-29.225671648849,-28.8424554441154,-27.847888015008,-26.8533205859005,
-25.8587531567931,-24.8641857276857,-23.8696182985782,-22.9424863416694),
 .UNSPECIFIED.);
#1037=B_SPLINE_CURVE_WITH_KNOTS('',3,(#44235,#44236,#44237,#44238,#44239,
#44240,#44241,#44242,#44243,#44244,#44245,#44246,#44247,#44248,#44249,#44250,
#44251,#44252,#44253,#44254,#44255,#44256),.UNSPECIFIED.,.F.,.F.,(4,3,3,
3,3,3,3,4),(19.9659494302248,20.8990154140913,21.8942066242861,22.889397834481,
23.8845890446758,24.8797802548706,25.8749714650654,26.2491347374044),
 .UNSPECIFIED.);
#1038=B_SPLINE_CURVE_WITH_KNOTS('',3,(#44261,#44262,#44263,#44264,#44265,
#44266,#44267,#44268,#44269,#44270,#44271,#44272,#44273,#44274,#44275,#44276,
#44277,#44278,#44279,#44280,#44281,#44282),.UNSPECIFIED.,.F.,.F.,(4,3,3,
3,3,3,3,4),(-35.5088569560286,-34.8098600187599,-33.8152925896525,-32.8207251605451,
-31.8261577314377,-30.8315903023302,-29.8370228732228,-29.225671648849),
 .UNSPECIFIED.);
#1039=B_SPLINE_CURVE_WITH_KNOTS('',3,(#44283,#44284,#44285,#44286,#44287,
#44288,#44289,#44290,#44291,#44292,#44293,#44294,#44295,#44296,#44297,#44298,
#44299,#44300,#44301,#44302,#44303,#44304),.UNSPECIFIED.,.F.,.F.,(4,3,3,
3,3,3,3,4),(26.2491347374044,26.8701626752603,27.8653538854551,28.8605450956499,
29.8557363058448,30.8509275160396,31.8461187262344,32.532320044584),
 .UNSPECIFIED.);
#1040=B_SPLINE_CURVE_WITH_KNOTS('',3,(#44309,#44310,#44311,#44312,#44313,
#44314,#44315,#44316,#44317,#44318,#44319,#44320,#44321,#44322,#44323,#44324,
#44325,#44326,#44327,#44328,#44329,#44330,#44331,#44332,#44333),
 .UNSPECIFIED.,.F.,.F.,(4,3,3,3,3,3,3,3,4),(-41.7920422632082,-41.7718320225119,
-40.7772645934045,-39.7826971642971,-38.7881297351896,-37.7935623060822,
-36.7989948769748,-35.8044274478674,-35.5088569560286),.UNSPECIFIED.);
#1041=B_SPLINE_CURVE_WITH_KNOTS('',3,(#44334,#44335,#44336,#44337,#44338,
#44339,#44340,#44341,#44342,#44343,#44344,#44345,#44346,#44347,#44348,#44349,
#44350,#44351,#44352,#44353,#44354,#44355,#44356,#44357,#44358),
 .UNSPECIFIED.,.F.,.F.,(4,3,3,3,3,3,3,3,4),(32.532320044584,32.8413099364292,
33.8365011466241,34.8316923568189,35.8268835670137,36.8220747772085,37.8172659874034,
38.8124571975982,38.8155053517636),.UNSPECIFIED.);
#1042=B_SPLINE_CURVE_WITH_KNOTS('',3,(#44363,#44364,#44365,#44366,#44367,
#44368,#44369,#44370,#44371,#44372,#44373,#44374,#44375,#44376,#44377,#44378,
#44379,#44380,#44381,#44382,#44383,#44384),.UNSPECIFIED.,.F.,.F.,(4,3,3,
3,3,3,3,4),(-48.0752275703878,-47.7392365971565,-46.7446691680491,-45.7501017389416,
-44.7555343098342,-43.7609668807268,-42.7663994516193,-41.7920422632082),
 .UNSPECIFIED.);
#1043=B_SPLINE_CURVE_WITH_KNOTS('',3,(#44385,#44386,#44387,#44388,#44389,
#44390,#44391,#44392,#44393,#44394,#44395,#44396,#44397,#44398,#44399,#44400,
#44401,#44402,#44403,#44404,#44405,#44406),.UNSPECIFIED.,.F.,.F.,(4,3,3,
3,3,3,3,4),(38.8155053517636,39.807648407793,40.8028396179878,41.7980308281826,
42.7932220383775,43.7884132485723,44.7836044587671,45.0986906589432),
 .UNSPECIFIED.);
#1044=B_SPLINE_CURVE_WITH_KNOTS('',3,(#44411,#44412,#44413,#44414,#44415,
#44416,#44417,#44418,#44419,#44420,#44421,#44422,#44423,#44424,#44425,#44426,
#44427,#44428,#44429,#44430,#44431,#44432),.UNSPECIFIED.,.F.,.F.,(4,3,3,
3,3,3,3,4),(-54.3584128775674,-53.7066411718011,-52.7120737426936,-51.7175063135862,
-50.7229388844788,-49.7283714553713,-48.7338040262639,-48.0752275703878),
 .UNSPECIFIED.);
#1045=B_SPLINE_CURVE_WITH_KNOTS('',3,(#44433,#44434,#44435,#44436,#44437,
#44438,#44439,#44440,#44441,#44442,#44443,#44444,#44445,#44446,#44447,#44448,
#44449,#44450,#44451,#44452,#44453,#44454),.UNSPECIFIED.,.F.,.F.,(4,3,3,
3,3,3,3,4),(45.0986906589432,45.7787956689619,46.7739868791568,47.7691780893516,
48.7643692995464,49.7595605097412,50.7547517199361,51.3818759661228),
 .UNSPECIFIED.);
#1046=B_SPLINE_CURVE_WITH_KNOTS('',3,(#44459,#44460,#44461,#44462,#44463,
#44464,#44465,#44466,#44467,#44468,#44469,#44470,#44471,#44472,#44473,#44474,
#44475,#44476,#44477,#44478,#44479,#44480),.UNSPECIFIED.,.F.,.F.,(4,3,3,
3,3,3,3,4),(-60.641598184747,-59.6740457464456,-58.6794783173382,-57.6849108882308,
-56.6903434591233,-55.6957760300159,-54.7012086009085,-54.3584128775674),
 .UNSPECIFIED.);
#1047=B_SPLINE_CURVE_WITH_KNOTS('',3,(#44481,#44482,#44483,#44484,#44485,
#44486,#44487,#44488,#44489,#44490,#44491,#44492,#44493,#44494,#44495,#44496,
#44497,#44498,#44499,#44500,#44501,#44502),.UNSPECIFIED.,.F.,.F.,(4,3,3,
3,3,3,3,4),(51.3818759661228,51.7499429301309,52.7451341403257,53.7403253505205,
54.7355165607154,55.7307077709102,56.725898981105,57.6650612733024),
 .UNSPECIFIED.);
#1048=B_SPLINE_CURVE_WITH_KNOTS('',3,(#44507,#44508,#44509,#44510,#44511,
#44512,#44513,#44514,#44515,#44516,#44517,#44518,#44519,#44520,#44521,#44522,
#44523,#44524,#44525,#44526,#44527,#44528,#44529,#44530,#44531),
 .UNSPECIFIED.,.F.,.F.,(4,3,3,3,3,3,3,3,4),(-66.9247834919265,-66.6360177501976,
-65.6414503210902,-64.6468828919827,-63.6523154628753,-62.6577480337679,
-61.6631806046605,-60.668613175553,-60.641598184747),.UNSPECIFIED.);
#1049=B_SPLINE_CURVE_WITH_KNOTS('',3,(#44532,#44533,#44534,#44535,#44536,
#44537,#44538,#44539,#44540,#44541,#44542,#44543,#44544,#44545,#44546,#44547,
#44548,#44549,#44550,#44551,#44552,#44553,#44554,#44555,#44556),
 .UNSPECIFIED.,.F.,.F.,(4,3,3,3,3,3,3,3,4),(57.6650612733024,57.7210901912998,
58.7162814014946,59.7114726116895,60.7066638218843,61.7018550320791,62.697046242274,
63.6922374524688,63.9482465804819),.UNSPECIFIED.);
#1050=B_SPLINE_CURVE_WITH_KNOTS('',3,(#44561,#44562,#44563,#44564,#44565,
#44566,#44567,#44568,#44569,#44570,#44571,#44572,#44573,#44574,#44575,#44576,
#44577,#44578,#44579,#44580,#44581,#44582),.UNSPECIFIED.,.F.,.F.,(4,3,3,
3,3,3,3,4),(-73.2079687991061,-72.6034223248422,-71.6088548957347,-70.6142874666273,
-69.6197200375199,-68.6251526084124,-67.630585179305,-66.9247834919265),
 .UNSPECIFIED.);
#1051=B_SPLINE_CURVE_WITH_KNOTS('',3,(#44583,#44584,#44585,#44586,#44587,
#44588,#44589,#44590,#44591,#44592,#44593,#44594,#44595,#44596,#44597,#44598,
#44599,#44600,#44601,#44602,#44603,#44604),.UNSPECIFIED.,.F.,.F.,(4,3,3,
3,3,3,3,4),(63.9482465804819,64.6874286626636,65.6826198728584,66.6778110830533,
67.6730022932481,68.6681935034429,69.6633847136378,70.2314318876615),
 .UNSPECIFIED.);
#1052=B_SPLINE_CURVE_WITH_KNOTS('',3,(#44609,#44610,#44611,#44612,#44613,
#44614,#44615,#44616,#44617,#44618,#44619,#44620,#44621,#44622,#44623,#44624,
#44625,#44626,#44627,#44628,#44629,#44630),.UNSPECIFIED.,.F.,.F.,(4,3,3,
3,3,3,3,4),(-79.4911541062857,-78.5708268994867,-77.5762594703793,-76.5816920412719,
-75.5871246121644,-74.592557183057,-73.5979897539496,-73.2079687991061),
 .UNSPECIFIED.);
#1053=B_SPLINE_CURVE_WITH_KNOTS('',3,(#44631,#44632,#44633,#44634,#44635,
#44636,#44637,#44638,#44639,#44640,#44641,#44642,#44643,#44644,#44645,#44646,
#44647,#44648,#44649,#44650,#44651,#44652),.UNSPECIFIED.,.F.,.F.,(4,3,3,
3,3,3,3,4),(70.2314318876615,70.6585759238326,71.6537671340274,72.6489583442222,
73.644149554417,74.6393407646119,75.6345319748067,76.5146171948411),
 .UNSPECIFIED.);
#1054=B_SPLINE_CURVE_WITH_KNOTS('',3,(#44657,#44658,#44659,#44660,#44661,
#44662,#44663,#44664,#44665,#44666,#44667,#44668,#44669,#44670,#44671,#44672,
#44673,#44674,#44675,#44676,#44677,#44678,#44679,#44680,#44681),
 .UNSPECIFIED.,.F.,.F.,(4,3,3,3,3,3,3,3,4),(-85.7743394134653,-85.5327989032387,
-84.5382314741313,-83.5436640450238,-82.5490966159164,-81.554529186809,
-80.5599617577016,-79.5653943285942,-79.4911541062857),.UNSPECIFIED.);
#1055=B_SPLINE_CURVE_WITH_KNOTS('',3,(#44682,#44683,#44684,#44685,#44686,
#44687,#44688,#44689,#44690,#44691,#44692,#44693,#44694,#44695,#44696,#44697,
#44698,#44699,#44700,#44701,#44702,#44703,#44704,#44705,#44706),
 .UNSPECIFIED.,.F.,.F.,(4,3,3,3,3,3,3,3,4),(76.5146171948411,76.6297231850015,
77.6249143951963,78.6201056053912,79.615296815586,80.6104880257808,81.6056792359756,
82.6008704461705,82.7978025020207),.UNSPECIFIED.);
#1056=B_SPLINE_CURVE_WITH_KNOTS('',3,(#44711,#44712,#44713,#44714,#44715,
#44716,#44717,#44718,#44719,#44720,#44721,#44722,#44723,#44724,#44725,#44726,
#44727,#44728,#44729,#44730,#44731,#44732),.UNSPECIFIED.,.F.,.F.,(4,3,3,
3,3,3,3,4),(-92.0575247206449,-91.5002034778833,-90.5056360487758,-89.5110686196684,
-88.516501190561,-87.5219337614536,-86.5273663323461,-85.7743394134653),
 .UNSPECIFIED.);
#1057=B_SPLINE_CURVE_WITH_KNOTS('',3,(#44733,#44734,#44735,#44736,#44737,
#44738,#44739,#44740,#44741,#44742,#44743,#44744,#44745,#44746,#44747,#44748,
#44749,#44750,#44751,#44752,#44753,#44754),.UNSPECIFIED.,.F.,.F.,(4,3,3,
3,3,3,3,4),(82.7978025020207,83.5960616563653,84.5912528665601,85.5864440767549,
86.5816352869498,87.5768264971446,88.5720177073394,89.0809878092003),
 .UNSPECIFIED.);
#1058=B_SPLINE_CURVE_WITH_KNOTS('',3,(#44759,#44760,#44761,#44762,#44763,
#44764,#44765,#44766,#44767,#44768,#44769,#44770,#44771,#44772,#44773,#44774,
#44775,#44776,#44777,#44778,#44779,#44780),.UNSPECIFIED.,.F.,.F.,(4,3,3,
3,3,3,3,4),(-98.3407100278245,-97.4676080525278,-96.4730406234204,-95.478473194313,
-94.4839057652055,-93.4893383360981,-92.4947709069907,-92.0575247206449),
 .UNSPECIFIED.);
#1059=B_SPLINE_CURVE_WITH_KNOTS('',3,(#44781,#44782,#44783,#44784,#44785,
#44786,#44787,#44788,#44789,#44790,#44791,#44792,#44793,#44794,#44795,#44796,
#44797,#44798,#44799,#44800,#44801,#44802),.UNSPECIFIED.,.F.,.F.,(4,3,3,
3,3,3,3,4),(89.0809878092003,89.5672089175342,90.5624001277291,91.5575913379239,
92.5527825481187,93.5479737583135,94.5431649685084,95.3641731163799),
 .UNSPECIFIED.);
#1060=B_SPLINE_CURVE_WITH_KNOTS('',3,(#44807,#44808,#44809,#44810,#44811,
#44812,#44813,#44814,#44815,#44816,#44817,#44818,#44819,#44820,#44821,#44822,
#44823,#44824,#44825,#44826,#44827,#44828,#44829,#44830,#44831),
 .UNSPECIFIED.,.F.,.F.,(4,3,3,3,3,3,3,3,4),(-104.623895335004,-104.42958005628,
-103.435012627172,-102.440445198065,-101.445877768958,-100.45131033985,
-99.4567429107427,-98.4621754816353,-98.3407100278245),.UNSPECIFIED.);
#1061=B_SPLINE_CURVE_WITH_KNOTS('',3,(#44832,#44833,#44834,#44835,#44836,
#44837,#44838,#44839,#44840,#44841,#44842,#44843,#44844,#44845,#44846,#44847,
#44848,#44849,#44850,#44851,#44852,#44853,#44854,#44855,#44856),
 .UNSPECIFIED.,.F.,.F.,(4,3,3,3,3,3,3,3,4),(95.3641731163799,95.5383561787032,
96.533547388898,97.5287385990929,98.5239298092877,99.5191210194825,100.514312229677,
101.509503439872,101.64735842356),.UNSPECIFIED.);
#1062=B_SPLINE_CURVE_WITH_KNOTS('',3,(#44861,#44862,#44863,#44864,#44865,
#44866,#44867,#44868,#44869,#44870,#44871,#44872,#44873,#44874,#44875,#44876,
#44877,#44878,#44879,#44880,#44881,#44882),.UNSPECIFIED.,.F.,.F.,(4,3,3,
3,3,3,3,4),(-110.907080642184,-110.396984630924,-109.402417201817,-108.40784977271,
-107.413282343602,-106.418714914495,-105.424147485387,-104.623895335004),
 .UNSPECIFIED.);
#1063=B_SPLINE_CURVE_WITH_KNOTS('',3,(#44883,#44884,#44885,#44886,#44887,
#44888,#44889,#44890,#44891,#44892,#44893,#44894,#44895,#44896,#44897,#44898,
#44899,#44900,#44901,#44902,#44903,#44904),.UNSPECIFIED.,.F.,.F.,(4,3,3,
3,3,3,3,4),(101.64735842356,102.504694650067,103.499885860262,104.495077070457,
105.490268280651,106.485459490846,107.480650701041,107.930543730739),
 .UNSPECIFIED.);
#1064=B_SPLINE_CURVE_WITH_KNOTS('',3,(#44909,#44910,#44911,#44912,#44913,
#44914,#44915,#44916,#44917,#44918,#44919,#44920,#44921,#44922,#44923,#44924,
#44925,#44926,#44927,#44928,#44929,#44930),.UNSPECIFIED.,.F.,.F.,(4,3,3,
3,3,3,3,4),(-117.190265949363,-116.364389205569,-115.369821776462,-114.375254347354,
-113.380686918247,-112.386119489139,-111.391552060032,-110.907080642184),
 .UNSPECIFIED.);
#1065=B_SPLINE_CURVE_WITH_KNOTS('',3,(#44931,#44932,#44933,#44934,#44935,
#44936,#44937,#44938,#44939,#44940,#44941,#44942,#44943,#44944,#44945,#44946,
#44947,#44948,#44949,#44950,#44951,#44952),.UNSPECIFIED.,.F.,.F.,(4,3,3,
3,3,3,3,4),(107.930543730739,108.475841911236,109.471033121431,110.466224331626,
111.46141554182,112.456606752015,113.45179796221,114.213729037919),
 .UNSPECIFIED.);
#1066=B_SPLINE_CURVE_WITH_KNOTS('',3,(#44958,#44959,#44960,#44961,#44962,
#44963,#44964,#44965,#44966,#44967,#44968),.UNSPECIFIED.,.F.,.F.,(4,1,1,
1,1,1,1,1,4),(128.805298797182,128.973989482495,129.968556911602,130.963124340709,
131.957691769817,132.952259198924,133.946826628032,134.444110342585,134.941394057139),
 .UNSPECIFIED.);
#1067=B_SPLINE_CURVE_WITH_KNOTS('',3,(#44971,#44972,#44973,#44974,#44975,
#44976,#44977,#44978,#44979),.UNSPECIFIED.,.F.,.F.,(4,1,1,1,1,1,4),(128.805298797182,
129.721712095852,130.716903306047,131.712094516241,132.707285726436,133.204881331534,
133.702476936631),.UNSPECIFIED.);
#1068=B_SPLINE_CURVE_WITH_KNOTS('',3,(#44984,#44985,#44986,#44987,#44988,
#44989,#44990,#44991,#44992,#44993),.UNSPECIFIED.,.F.,.F.,(4,1,1,1,1,1,
1,4),(122.522113490002,123.00658490785,124.001152336957,124.995719766065,
125.990287195172,126.98485462428,127.979422053387,128.805298797182),
 .UNSPECIFIED.);
#1069=B_SPLINE_CURVE_WITH_KNOTS('',3,(#44994,#44995,#44996,#44997,#44998,
#44999,#45000,#45001,#45002,#45003,#45004),.UNSPECIFIED.,.F.,.F.,(4,1,1,
1,1,1,1,1,4),(122.522113490002,122.755373624488,123.750564834683,124.745756044878,
125.740947255072,126.736138465267,127.731329675462,128.726520885657,128.805298797182),
 .UNSPECIFIED.);
#1070=B_SPLINE_CURVE_WITH_KNOTS('',3,(#45009,#45010,#45011,#45012,#45013,
#45014,#45015,#45016,#45017,#45018),.UNSPECIFIED.,.F.,.F.,(4,1,1,1,1,1,
1,4),(116.238928182822,117.039180333205,118.033747762313,119.02831519142,
120.022882620528,121.017450049635,122.012017478743,122.522113490002),
 .UNSPECIFIED.);
#1071=B_SPLINE_CURVE_WITH_KNOTS('',3,(#45019,#45020,#45021,#45022,#45023,
#45024,#45025,#45026,#45027,#45028),.UNSPECIFIED.,.F.,.F.,(4,1,1,1,1,1,
1,4),(116.238928182822,116.784226363319,117.779417573514,118.774608783709,
119.769799993904,120.764991204098,121.760182414293,122.522113490002),
 .UNSPECIFIED.);
#1072=B_SPLINE_CURVE_WITH_KNOTS('',3,(#45033,#45034,#45035,#45036,#45037,
#45038,#45039,#45040,#45041,#45042,#45043),.UNSPECIFIED.,.F.,.F.,(4,1,1,
1,1,1,1,1,4),(109.955742875643,110.077208329453,111.071775758561,112.066343187668,
113.060910616776,114.055478045883,115.050045474991,116.044612904098,116.238928182822),
 .UNSPECIFIED.);
#1073=B_SPLINE_CURVE_WITH_KNOTS('',3,(#45044,#45045,#45046,#45047,#45048,
#45049,#45050,#45051,#45052,#45053),.UNSPECIFIED.,.F.,.F.,(4,1,1,1,1,1,
1,4),(109.955742875643,110.81307910215,111.808270312345,112.80346152254,
113.798652732735,114.793843942929,115.789035153124,116.238928182822),
 .UNSPECIFIED.);
#1074=B_SPLINE_CURVE_WITH_KNOTS('',3,(#45058,#45059,#45060,#45061,#45062,
#45063,#45064,#45065,#45066,#45067),.UNSPECIFIED.,.F.,.F.,(4,1,1,1,1,1,
1,4),(103.672557568463,104.109803754809,105.104371183916,106.098938613024,
107.093506042131,108.088073471239,109.082640900346,109.955742875643),
 .UNSPECIFIED.);
#1075=B_SPLINE_CURVE_WITH_KNOTS('',3,(#45068,#45069,#45070,#45071,#45072,
#45073,#45074,#45075,#45076,#45077,#45078),.UNSPECIFIED.,.F.,.F.,(4,1,1,
1,1,1,1,1,4),(103.672557568463,103.846740630786,104.841931840981,105.837123051176,
106.832314261371,107.827505471566,108.82269668176,109.817887891955,109.955742875643),
 .UNSPECIFIED.);
#1076=B_SPLINE_CURVE_WITH_KNOTS('',3,(#45083,#45084,#45085,#45086,#45087,
#45088,#45089,#45090,#45091,#45092),.UNSPECIFIED.,.F.,.F.,(4,1,1,1,1,1,
1,4),(97.3893722612836,98.1423991801644,99.1369666092718,100.131534038379,
101.126101467487,102.120668896594,103.115236325701,103.672557568463),
 .UNSPECIFIED.);
#1077=B_SPLINE_CURVE_WITH_KNOTS('',3,(#45093,#45094,#45095,#45096,#45097,
#45098,#45099,#45100,#45101,#45102),.UNSPECIFIED.,.F.,.F.,(4,1,1,1,1,1,
1,4),(97.3893722612835,97.8755933696174,98.8707845798122,99.865975790007,
100.861167000202,101.856358210397,102.851549420591,103.672557568463),
 .UNSPECIFIED.);
#1078=B_SPLINE_CURVE_WITH_KNOTS('',3,(#45107,#45108,#45109,#45110,#45111,
#45112,#45113,#45114,#45115,#45116,#45117),.UNSPECIFIED.,.F.,.F.,(4,1,1,
1,1,1,1,1,4),(91.106186954104,91.1804271764124,92.1749946055198,93.1695620346272,
94.1641294637347,95.1586968928421,96.1532643219495,97.1478317510569,97.3893722612836),
 .UNSPECIFIED.);
#1079=B_SPLINE_CURVE_WITH_KNOTS('',3,(#45118,#45119,#45120,#45121,#45122,
#45123,#45124,#45125,#45126,#45127),.UNSPECIFIED.,.F.,.F.,(4,1,1,1,1,1,
1,4),(91.106186954104,91.9044461084484,92.8996373186432,93.8948285288381,
94.8900197390329,95.8852109492277,96.8804021594225,97.3893722612835),
 .UNSPECIFIED.);
#1080=B_SPLINE_CURVE_WITH_KNOTS('',3,(#45132,#45133,#45134,#45135,#45136,
#45137,#45138,#45139,#45140,#45141),.UNSPECIFIED.,.F.,.F.,(4,1,1,1,1,1,
1,4),(84.8230016469244,85.2130226017678,86.2075900308752,87.2021574599827,
88.1967248890901,89.1912923181975,90.1858597473049,91.106186954104),
 .UNSPECIFIED.);
#1081=B_SPLINE_CURVE_WITH_KNOTS('',3,(#45142,#45143,#45144,#45145,#45146,
#45147,#45148,#45149,#45150,#45151,#45152),.UNSPECIFIED.,.F.,.F.,(4,1,1,
1,1,1,1,1,4),(84.8230016469244,84.9381076370846,85.9332988472795,86.9284900574743,
87.9236812676691,88.9188724778639,89.9140636880588,90.9092548982536,91.106186954104),
 .UNSPECIFIED.);
#1082=B_SPLINE_CURVE_WITH_KNOTS('',3,(#45157,#45158,#45159,#45160,#45161,
#45162,#45163,#45164,#45165,#45166),.UNSPECIFIED.,.F.,.F.,(4,1,1,1,1,1,
1,4),(78.5398163397448,79.2456180271232,80.2401854562307,81.2347528853381,
82.2293203144455,83.223887743553,84.2184551726604,84.8230016469244),
 .UNSPECIFIED.);
#1083=B_SPLINE_CURVE_WITH_KNOTS('',3,(#45167,#45168,#45169,#45170,#45171,
#45172,#45173,#45174,#45175,#45176),.UNSPECIFIED.,.F.,.F.,(4,1,1,1,1,1,
1,4),(78.5398163397448,78.9669603759157,79.9621515861105,80.9573427963053,
81.9525340065002,82.947725216695,83.9429164268898,84.8230016469244),
 .UNSPECIFIED.);
#1084=B_SPLINE_CURVE_WITH_KNOTS('',3,(#45181,#45182,#45183,#45184,#45185,
#45186,#45187,#45188,#45189,#45190,#45191),.UNSPECIFIED.,.F.,.F.,(4,1,1,
1,1,1,1,1,4),(72.2566310325652,72.2836460233713,73.2782134524787,74.2727808815861,
75.2673483106935,76.261915739801,77.2564831689084,78.2510505980158,78.5398163397448),
 .UNSPECIFIED.);
#1085=B_SPLINE_CURVE_WITH_KNOTS('',3,(#45192,#45193,#45194,#45195,#45196,
#45197,#45198,#45199,#45200,#45201),.UNSPECIFIED.,.F.,.F.,(4,1,1,1,1,1,
1,4),(72.2566310325652,72.9958131147467,73.9910043249416,74.9861955351364,
75.9813867453312,76.976577955526,77.9717691657209,78.5398163397448),
 .UNSPECIFIED.);
#1086=B_SPLINE_CURVE_WITH_KNOTS('',3,(#45206,#45207,#45208,#45209,#45210,
#45211,#45212,#45213,#45214,#45215),.UNSPECIFIED.,.F.,.F.,(4,1,1,1,1,1,
1,4),(65.9734457253856,66.3162414487267,67.3108088778341,68.3053763069416,
69.299943736049,70.2945111651564,71.2890785942638,72.2566310325652),
 .UNSPECIFIED.);
#1087=B_SPLINE_CURVE_WITH_KNOTS('',3,(#45216,#45217,#45218,#45219,#45220,
#45221,#45222,#45223,#45224,#45225,#45226),.UNSPECIFIED.,.F.,.F.,(4,1,1,
1,1,1,1,1,4),(65.9734457253856,66.029474643383,67.0246658535778,68.0198570637726,
69.0150482739674,70.0102394841623,71.0054306943571,72.0006219045519,72.2566310325652),
 .UNSPECIFIED.);
#1088=B_SPLINE_CURVE_WITH_KNOTS('',3,(#45231,#45232,#45233,#45234,#45235,
#45236,#45237,#45238,#45239,#45240),.UNSPECIFIED.,.F.,.F.,(4,1,1,1,1,1,
1,4),(59.690260418206,60.3488368740821,61.3434043031896,62.337971732297,
63.3325391614044,64.3271065905118,65.3216740196193,65.9734457253856),
 .UNSPECIFIED.);
#1089=B_SPLINE_CURVE_WITH_KNOTS('',3,(#45241,#45242,#45243,#45244,#45245,
#45246,#45247,#45248,#45249,#45250),.UNSPECIFIED.,.F.,.F.,(4,1,1,1,1,1,
1,4),(59.690260418206,60.058327382214,61.0535185924088,62.0487098026037,
63.0439010127985,64.0390922229933,65.0342834331881,65.9734457253856),
 .UNSPECIFIED.);
#1090=B_SPLINE_CURVE_WITH_KNOTS('',3,(#45255,#45256,#45257,#45258,#45259,
#45260,#45261,#45262,#45263,#45264),.UNSPECIFIED.,.F.,.F.,(4,1,1,1,1,1,
1,4),(53.4070751110264,54.3814322994376,55.375999728545,56.3705671576524,
57.3651345867599,58.3597020158673,59.3542694449747,59.690260418206),
 .UNSPECIFIED.);
#1091=B_SPLINE_CURVE_WITH_KNOTS('',3,(#45265,#45266,#45267,#45268,#45269,
#45270,#45271,#45272,#45273,#45274),.UNSPECIFIED.,.F.,.F.,(4,1,1,1,1,1,
1,4),(53.4070751110264,54.0871801210451,55.0823713312399,56.0775625414347,
57.0727537516295,58.0679449618244,59.0631361720192,59.690260418206),
 .UNSPECIFIED.);
#1092=B_SPLINE_CURVE_WITH_KNOTS('',3,(#45279,#45280,#45281,#45282,#45283,
#45284,#45285,#45286,#45287,#45288,#45289),.UNSPECIFIED.,.F.,.F.,(4,1,1,
1,1,1,1,1,4),(47.1238898038468,47.4194602956856,48.414027724793,49.4085951539004,
50.4031625830079,51.3977300121153,52.3922974412227,53.3868648703302,53.4070751110264),
 .UNSPECIFIED.);
#1093=B_SPLINE_CURVE_WITH_KNOTS('',3,(#45290,#45291,#45292,#45293,#45294,
#45295,#45296,#45297,#45298,#45299),.UNSPECIFIED.,.F.,.F.,(4,1,1,1,1,1,
1,4),(47.1238898038468,48.1160328598761,49.1112240700709,50.1064152802658,
51.1016064904606,52.0967977006554,53.0919889108502,53.4070751110264),
 .UNSPECIFIED.);
#1094=B_SPLINE_CURVE_WITH_KNOTS('',3,(#45304,#45305,#45306,#45307,#45308,
#45309,#45310,#45311,#45312,#45313),.UNSPECIFIED.,.F.,.F.,(4,1,1,1,1,1,
1,4),(40.8407044966672,41.452055721041,42.4466231501485,43.4411905792559,
44.4357580083633,45.4303254374707,46.4248928665782,47.1238898038468),
 .UNSPECIFIED.);
#1095=B_SPLINE_CURVE_WITH_KNOTS('',3,(#45314,#45315,#45316,#45317,#45318,
#45319,#45320,#45321,#45322,#45323,#45324),.UNSPECIFIED.,.F.,.F.,(4,1,1,
1,1,1,1,1,4),(40.8407044966672,41.1496943885123,42.1448855987072,43.140076808902,
44.1352680190968,45.1304592292916,46.1256504394865,47.1208416496813,47.1238898038468),
 .UNSPECIFIED.);
#1096=B_SPLINE_CURVE_WITH_KNOTS('',3,(#45329,#45330,#45331,#45332,#45333,
#45334,#45335,#45336,#45337,#45338),.UNSPECIFIED.,.F.,.F.,(4,1,1,1,1,1,
1,4),(34.5575191894876,35.4846511463965,36.4792185755039,37.4737860046113,
38.4683534337187,39.4629208628262,40.4574882919336,40.8407044966672),
 .UNSPECIFIED.);
#1097=B_SPLINE_CURVE_WITH_KNOTS('',3,(#45339,#45340,#45341,#45342,#45343,
#45344,#45345,#45346,#45347,#45348),.UNSPECIFIED.,.F.,.F.,(4,1,1,1,1,1,
1,4),(34.5575191894876,35.1785471273434,36.1737383375382,37.168929547733,
38.1641207579279,39.1593119681227,40.1545031783175,40.8407044966672),
 .UNSPECIFIED.);
#1098=B_SPLINE_CURVE_WITH_KNOTS('',3,(#45353,#45354,#45355,#45356,#45357,
#45358,#45359,#45360,#45361,#45362,#45363),.UNSPECIFIED.,.F.,.F.,(4,1,1,
1,1,1,1,1,4),(28.274333882308,28.5226791426445,29.5172465717519,30.5118140008593,
31.5063814299668,32.5009488590742,33.4955162881816,34.490083717289,34.5575191894876),
 .UNSPECIFIED.);
#1099=B_SPLINE_CURVE_WITH_KNOTS('',3,(#45364,#45365,#45366,#45367,#45368,
#45369,#45370,#45371,#45372,#45373),.UNSPECIFIED.,.F.,.F.,(4,1,1,1,1,1,
1,4),(28.274333882308,29.2073998661744,30.2025910763693,31.1977822865641,
32.1929734967589,33.1881647069537,34.1833559171486,34.5575191894876),
 .UNSPECIFIED.);
#1100=B_SPLINE_CURVE_WITH_KNOTS('',3,(#45378,#45379,#45380,#45381,#45382,
#45383,#45384,#45385,#45386,#45387),.UNSPECIFIED.,.F.,.F.,(4,1,1,1,1,1,
1,4),(21.9911485751285,22.5552745679999,23.5498419971074,24.5444094262148,
25.5389768553222,26.5335442844296,27.5281117135371,28.274333882308),
 .UNSPECIFIED.);
#1101=B_SPLINE_CURVE_WITH_KNOTS('',3,(#45388,#45389,#45390,#45391,#45392,
#45393,#45394,#45395,#45396,#45397,#45398),.UNSPECIFIED.,.F.,.F.,(4,1,1,
1,1,1,1,1,4),(21.9911485751285,22.2410613948107,23.2362526050055,24.2314438152003,
25.2266350253952,26.22182623559,27.2170174457848,28.2122086559796,28.274333882308),
 .UNSPECIFIED.);
#1102=B_SPLINE_CURVE_WITH_KNOTS('',3,(#45403,#45404,#45405,#45406,#45407,
#45408,#45409,#45410,#45411,#45412),.UNSPECIFIED.,.F.,.F.,(4,1,1,1,1,1,
1,4),(15.7079632679489,16.5878699933554,17.5824374224628,18.5770048515702,
19.5715722806776,20.5661397097851,21.5607071388925,21.9911485751285),
 .UNSPECIFIED.);
#1103=B_SPLINE_CURVE_WITH_KNOTS('',3,(#45413,#45414,#45415,#45416,#45417,
#45418,#45419,#45420,#45421,#45422),.UNSPECIFIED.,.F.,.F.,(4,1,1,1,1,1,
1,4),(15.7079632679489,16.2699141336417,17.2651053438366,18.2602965540314,
19.2554877642262,20.250678974421,21.2458701846159,21.9911485751285),
 .UNSPECIFIED.);
#1104=B_SPLINE_CURVE_WITH_KNOTS('',3,(#45425,#45426,#45427,#45428,#45429,
#45430,#45431,#45432,#45433,#45434,#45435,#45436,#45437,#45438,#45439,#45440,
#45441,#45442,#45443,#45444,#45445,#45446,#45447,#45448,#45449,#45450,#45451,
#45452,#45453,#45454,#45455,#45456,#45457,#45458,#45459,#45460,#45461,#45462,
#45463,#45464,#45465,#45466,#45467,#45468,#45469,#45470,#45471,#45472,#45473,
#45474,#45475,#45476,#45477,#45478,#45479,#45480,#45481,#45482,#45483,#45484,
#45485,#45486,#45487,#45488,#45489,#45490,#45491,#45492,#45493,#45494,#45495,
#45496,#45497,#45498,#45499,#45500,#45501,#45502,#45503,#45504,#45505,#45506,
#45507,#45508,#45509,#45510,#45511,#45512,#45513,#45514,#45515,#45516,#45517,
#45518,#45519,#45520,#45521,#45522,#45523,#45524,#45525,#45526,#45527,#45528,
#45529,#45530,#45531,#45532,#45533,#45534,#45535,#45536,#45537,#45538,#45539,
#45540,#45541,#45542,#45543,#45544,#45545,#45546,#45547,#45548,#45549,#45550,
#45551,#45552,#45553,#45554,#45555,#45556,#45557,#45558,#45559,#45560,#45561,
#45562,#45563,#45564,#45565,#45566,#45567,#45568,#45569,#45570,#45571,#45572,
#45573,#45574,#45575,#45576,#45577,#45578,#45579,#45580,#45581,#45582,#45583,
#45584,#45585,#45586,#45587,#45588,#45589,#45590,#45591,#45592,#45593,#45594,
#45595,#45596,#45597,#45598,#45599,#45600,#45601,#45602,#45603,#45604,#45605,
#45606,#45607,#45608,#45609,#45610,#45611,#45612,#45613,#45614,#45615,#45616,
#45617,#45618,#45619,#45620,#45621,#45622,#45623,#45624,#45625,#45626,#45627,
#45628,#45629,#45630,#45631,#45632,#45633,#45634,#45635,#45636,#45637,#45638,
#45639,#45640,#45641,#45642,#45643,#45644,#45645,#45646,#45647,#45648,#45649,
#45650,#45651,#45652,#45653,#45654,#45655,#45656,#45657,#45658,#45659,#45660,
#45661,#45662,#45663,#45664,#45665,#45666,#45667,#45668),.UNSPECIFIED.,
 .F.,.F.,(4,3,3,3,3,3,3,3,3,3,3,3,3,3,3,3,3,3,3,3,3,3,3,3,3,3,3,3,3,3,3,
3,3,3,3,3,3,3,3,3,3,3,3,3,3,3,3,3,3,3,3,3,3,3,3,3,3,3,3,3,3,3,3,3,3,3,3,
3,3,3,3,3,3,3,3,3,3,3,3,3,3,4),(-2.64334436896556,-2.60354403016607,-2.56319357704322,
-2.52826625024512,-2.51459318907079,-2.50781535649548,-2.46564981317316,
-2.42348426985084,-2.39566963603287,-2.38341570939638,-2.37761610684016,
-2.336849738158,-2.29583153162079,-2.25519438983726,-2.22808079457215,-2.2136427889914,
-2.20824896814423,-2.20096719930704,-2.16123852890373,-2.12054358173304,
-2.07915011465577,-2.03779648847865,-2.03243166702702,-1.99089005776529,
-1.94895701700167,-1.90713874879756,-1.86743433790788,-1.85926764668736,
-1.85203534200324,-1.80992713326301,-1.76842432689819,-1.74832110523882,
-1.70676763322338,-1.68046855645703,-1.67322668686903,-1.63229330306282,
-1.58900444080018,-1.54654889761395,-1.51397808603242,-1.5045713939363,
-1.49689579776549,-1.49148547399684,-1.44889513044297,-1.40637477884859,
-1.36441427917375,-1.32519834206773,-1.31745702219618,-1.31155026142285,
-1.28598240496172,-1.24479777214057,-1.20266268120784,-1.15989915790716,
-1.13825803467134,-1.13225377395059,-1.12622665290763,-1.08347961800304,
-1.04027268262164,-0.997123369249094,-0.954546729607404,-0.947141190072399,
-0.941377976925763,-0.897944447185484,-0.855190214624572,-0.813641186133967,
-0.785925562678236,-0.769826109785476,-0.761910560472749,-0.75632393840638,
-0.714342458530382,-0.67097419230323,-0.627232222714931,-0.595102096230848,
-0.581045165894062,-0.572765453161588,-0.566918945151293,-0.523130330920948,
-0.47917700856887,-0.435659870904986,-0.402925540873628,-0.383690774196495,
-0.377633521738216,-0.37019121084227),.UNSPECIFIED.);
#1105=B_SPLINE_CURVE_WITH_KNOTS('',3,(#45670,#45671,#45672,#45673,#45674,
#45675,#45676,#45677,#45678,#45679,#45680,#45681,#45682,#45683,#45684,#45685,
#45686,#45687,#45688,#45689,#45690,#45691,#45692,#45693,#45694,#45695,#45696,
#45697,#45698,#45699,#45700,#45701,#45702,#45703,#45704,#45705,#45706,#45707,
#45708,#45709,#45710,#45711,#45712,#45713,#45714,#45715,#45716,#45717,#45718,
#45719,#45720,#45721,#45722,#45723,#45724,#45725,#45726,#45727,#45728,#45729,
#45730,#45731,#45732,#45733,#45734,#45735,#45736,#45737,#45738,#45739,#45740,
#45741,#45742),.UNSPECIFIED.,.F.,.F.,(4,3,3,3,3,3,3,3,3,3,3,3,3,3,3,3,3,
3,3,3,3,3,3,3,4),(-0.710745924398683,-0.666804013499017,-0.623090002091155,
-0.580490043399667,-0.549769720878275,-0.540030794848239,-0.533787755766615,
-0.491609440904295,-0.4576087533141,-0.414988201685294,-0.372400295436586,
-0.356121723662545,-0.350309819512417,-0.308708315030754,-0.266458526938774,
-0.224208738846794,-0.196182646490945,-0.183254318429312,-0.17525918271343,
-0.169900496948286,-0.127425372711214,-0.0868708094010787,-0.0467252344004481,
-0.00739903503843566,0.),.UNSPECIFIED.);
#1106=B_SPLINE_CURVE_WITH_KNOTS('',3,(#45745,#45746,#45747,#45748,#45749,
#45750,#45751,#45752,#45753,#45754,#45755,#45756,#45757,#45758,#45759,#45760,
#45761,#45762,#45763,#45764,#45765,#45766,#45767,#45768,#45769,#45770,#45771,
#45772,#45773,#45774,#45775,#45776,#45777,#45778,#45779,#45780,#45781),
 .UNSPECIFIED.,.F.,.F.,(4,3,3,3,3,3,3,3,3,3,3,3,4),(-0.37019121084227,-0.331697325929431,
-0.288622232780515,-0.244797719637212,-0.21419800468256,-0.2008106293899,
-0.194172952745162,-0.188472403894731,-0.144967619206762,-0.100508059630889,
-0.0559598465844598,-0.0119678329618413,0.),.UNSPECIFIED.);
#1107=B_SPLINE_CURVE_WITH_KNOTS('',3,(#46302,#46303,#46304,#46305,#46306,
#46307,#46308,#46309,#46310),.UNSPECIFIED.,.F.,.F.,(4,1,1,1,1,1,4),(11.6150328478182,
12.1123165623719,12.6096002769257,13.6041677060331,14.5987351351405,15.5933025642479,
15.7079632679489),.UNSPECIFIED.);
#1108=B_SPLINE_CURVE_WITH_KNOTS('',3,(#46311,#46312,#46313,#46314,#46315,
#46316,#46317,#46318,#46319,#46320,#46321,#46322,#46323,#46324,#46325,#46326,
#46327,#46328,#46329,#46330,#46331,#46332,#46333,#46334,#46335,#46336,#46337,
#46338,#46339,#46340,#46341,#46342,#46343,#46344,#46345,#46346,#46347,#46348,
#46349,#46350,#46351,#46352,#46353,#46354,#46355,#46356,#46357,#46358,#46359,
#46360,#46361,#46362,#46363,#46364,#46365,#46366,#46367,#46368,#46369,#46370,
#46371,#46372,#46373,#46374,#46375,#46376,#46377,#46378,#46379,#46380,#46381,
#46382,#46383,#46384,#46385,#46386,#46387,#46388,#46389,#46390,#46391,#46392,
#46393,#46394,#46395,#46396,#46397,#46398,#46399,#46400,#46401,#46402,#46403,
#46404,#46405,#46406,#46407,#46408,#46409,#46410,#46411,#46412,#46413),
 .UNSPECIFIED.,.F.,.F.,(4,3,3,3,3,3,3,3,3,3,3,3,3,3,3,3,3,3,3,3,3,3,3,3,
3,3,3,3,3,3,3,3,3,3,4),(-0.965990216419481,-0.9272199902169,-0.883653696268922,
-0.856578499606751,-0.840281614965736,-0.83272424860471,-0.78942649842623,
-0.747054504832225,-0.728516757634848,-0.714850133126621,-0.708733859333935,
-0.665685633827477,-0.622719517527392,-0.579652275564091,-0.547351844091615,
-0.533932274491217,-0.525881927440116,-0.484249432147785,-0.450450549674188,
-0.408562082241703,-0.366597621077022,-0.351118396676314,-0.345479700399037,
-0.304353213451827,-0.263090931261655,-0.221828649071483,-0.194100067937547,
-0.181335497105944,-0.172973757166477,-0.167228677968348,-0.125421508476261,
-0.0849791978641806,-0.0449278087924871,-0.005690172937603,0.),
 .UNSPECIFIED.);
#1109=B_SPLINE_CURVE_WITH_KNOTS('',3,(#46414,#46415,#46416,#46417,#46418,
#46419,#46420,#46421,#46422,#46423,#46424,#46425,#46426,#46427,#46428,#46429,
#46430,#46431,#46432),.UNSPECIFIED.,.F.,.F.,(4,3,3,3,3,3,4),(-121.812676859456,
-121.337226351106,-120.342658921999,-119.348091492891,-118.353524063784,
-117.358956634676,-117.190265949363),.UNSPECIFIED.);
#1110=B_SPLINE_CURVE_WITH_KNOTS('',3,(#46435,#46436,#46437,#46438,#46439,
#46440,#46441,#46442,#46443),.UNSPECIFIED.,.F.,.F.,(4,1,1,1,1,1,4),(10.3761157273101,
11.2939580826676,12.2891492928624,13.2843405030573,14.2795317132521,15.2747229234469,
15.7079632679489),.UNSPECIFIED.);
#1111=B_SPLINE_CURVE_WITH_KNOTS('',3,(#46969,#46970,#46971,#46972,#46973,
#46974,#46975,#46976,#46977,#46978,#46979,#46980,#46981,#46982,#46983,#46984,
#46985,#46986,#46987,#46988,#46989,#46990),.UNSPECIFIED.,.F.,.F.,(4,3,3,
3,3,3,3,4),(114.213729037919,114.446989172405,115.4421803826,116.437371592795,
117.432562802989,118.427754013184,119.422945223379,119.744945584229),
 .UNSPECIFIED.);
#1112=B_SPLINE_CURVE_WITH_KNOTS('',3,(#46991,#46992,#46993,#46994,#46995,
#46996,#46997,#46998,#46999,#47000,#47001,#47002,#47003,#47004,#47005,#47006,
#47007,#47008,#47009,#47010,#47011,#47012,#47013,#47014,#47015,#47016,#47017,
#47018,#47019,#47020,#47021,#47022,#47023,#47024,#47025,#47026,#47027,#47028,
#47029,#47030,#47031,#47032,#47033,#47034,#47035,#47036,#47037,#47038,#47039,
#47040,#47041,#47042,#47043,#47044,#47045,#47046,#47047,#47048,#47049,#47050,
#47051,#47052,#47053,#47054,#47055,#47056,#47057,#47058,#47059,#47060,#47061,
#47062,#47063,#47064,#47065,#47066,#47067,#47068,#47069,#47070,#47071,#47072,
#47073,#47074,#47075,#47076,#47077,#47078,#47079,#47080,#47081,#47082,#47083,
#47084,#47085,#47086,#47087,#47088,#47089,#47090,#47091,#47092,#47093,#47094,
#47095,#47096),.UNSPECIFIED.,.F.,.F.,(4,3,3,3,3,3,3,3,3,3,3,3,3,3,3,3,3,
3,3,3,3,3,3,3,3,3,3,3,3,3,3,3,3,3,3,4),(-0.968477696161952,-0.934401878411372,
-0.894940908856935,-0.869057110968003,-0.857761995024893,-0.84957581141373,
-0.809420536841839,-0.768342987565862,-0.750371559757621,-0.741288256886726,
-0.734041921366352,-0.692568544969978,-0.650621991967233,-0.60816652963393,
-0.576324932883953,-0.562465720811907,-0.556565387998925,-0.513962262185476,
-0.480800142634022,-0.43927778705218,-0.397173024145668,-0.382659788254531,
-0.376822993230344,-0.334735665268914,-0.292008067784669,-0.248907378913767,
-0.243684959408641,-0.213224339482561,-0.199897818264901,-0.191569349313896,
-0.186008989480452,-0.142614739306227,-0.0987671132040068,-0.0550446346348842,
-0.0119839009752852,0.),.UNSPECIFIED.);
#1896=CYLINDRICAL_SURFACE('',#15080,4.942);
#1897=CYLINDRICAL_SURFACE('',#15082,4.942);
#1898=CYLINDRICAL_SURFACE('',#15083,4.942);
#1899=CYLINDRICAL_SURFACE('',#15084,4.942);
#1900=CYLINDRICAL_SURFACE('',#15085,4.942);
#1901=CYLINDRICAL_SURFACE('',#15086,4.942);
#1902=CYLINDRICAL_SURFACE('',#15087,4.942);
#1903=CYLINDRICAL_SURFACE('',#15088,4.942);
#1904=CYLINDRICAL_SURFACE('',#15089,4.942);
#1905=CYLINDRICAL_SURFACE('',#15090,4.942);
#1906=CYLINDRICAL_SURFACE('',#15091,4.942);
#1907=CYLINDRICAL_SURFACE('',#15092,4.942);
#1908=CYLINDRICAL_SURFACE('',#15093,4.942);
#1909=CYLINDRICAL_SURFACE('',#15094,4.942);
#1910=CYLINDRICAL_SURFACE('',#15095,4.942);
#1911=CYLINDRICAL_SURFACE('',#15096,4.942);
#1912=CYLINDRICAL_SURFACE('',#15097,4.942);
#1913=CYLINDRICAL_SURFACE('',#15098,4.942);
#1914=CYLINDRICAL_SURFACE('',#15099,4.942);
#1915=CYLINDRICAL_SURFACE('',#15100,4.372);
#1916=CYLINDRICAL_SURFACE('',#15102,4.372);
#1917=CYLINDRICAL_SURFACE('',#15103,4.372);
#1918=CYLINDRICAL_SURFACE('',#15104,4.372);
#1919=CYLINDRICAL_SURFACE('',#15105,4.372);
#1920=CYLINDRICAL_SURFACE('',#15106,4.372);
#1921=CYLINDRICAL_SURFACE('',#15107,4.372);
#1922=CYLINDRICAL_SURFACE('',#15108,4.372);
#1923=CYLINDRICAL_SURFACE('',#15109,4.372);
#1924=CYLINDRICAL_SURFACE('',#15110,4.372);
#1925=CYLINDRICAL_SURFACE('',#15111,4.372);
#1926=CYLINDRICAL_SURFACE('',#15112,4.372);
#1927=CYLINDRICAL_SURFACE('',#15113,4.372);
#1928=CYLINDRICAL_SURFACE('',#15114,4.372);
#1929=CYLINDRICAL_SURFACE('',#15115,4.372);
#1930=CYLINDRICAL_SURFACE('',#15116,4.372);
#1931=CYLINDRICAL_SURFACE('',#15117,4.372);
#1932=CYLINDRICAL_SURFACE('',#15118,4.372);
#1933=CYLINDRICAL_SURFACE('',#15119,4.372);
#1934=CYLINDRICAL_SURFACE('',#15123,4.372);
#1935=CYLINDRICAL_SURFACE('',#15125,4.942);
#1936=CYLINDRICAL_SURFACE('',#15135,8.);
#2183=SHAPE_REPRESENTATION_RELATIONSHIP('SRR','None',#63868,#2199);
#2199=ADVANCED_BREP_SHAPE_REPRESENTATION('',(#2231),#63746);
#2215=STYLED_ITEM('',(#63960),#2231);
#2231=MANIFOLD_SOLID_BREP('Body1',#14316);
#2279=FACE_BOUND('',#3561,.T.);
#2280=FACE_BOUND('',#3564,.T.);
#2711=FACE_OUTER_BOUND('',#3510,.T.);
#2712=FACE_OUTER_BOUND('',#3511,.T.);
#2713=FACE_OUTER_BOUND('',#3512,.T.);
#2714=FACE_OUTER_BOUND('',#3513,.T.);
#2715=FACE_OUTER_BOUND('',#3514,.T.);
#2716=FACE_OUTER_BOUND('',#3515,.T.);
#2717=FACE_OUTER_BOUND('',#3516,.T.);
#2718=FACE_OUTER_BOUND('',#3517,.T.);
#2719=FACE_OUTER_BOUND('',#3518,.T.);
#2720=FACE_OUTER_BOUND('',#3519,.T.);
#2721=FACE_OUTER_BOUND('',#3520,.T.);
#2722=FACE_OUTER_BOUND('',#3521,.T.);
#2723=FACE_OUTER_BOUND('',#3522,.T.);
#2724=FACE_OUTER_BOUND('',#3523,.T.);
#2725=FACE_OUTER_BOUND('',#3524,.T.);
#2726=FACE_OUTER_BOUND('',#3525,.T.);
#2727=FACE_OUTER_BOUND('',#3526,.T.);
#2728=FACE_OUTER_BOUND('',#3527,.T.);
#2729=FACE_OUTER_BOUND('',#3528,.T.);
#2730=FACE_OUTER_BOUND('',#3529,.T.);
#2731=FACE_OUTER_BOUND('',#3530,.T.);
#2732=FACE_OUTER_BOUND('',#3531,.T.);
#2733=FACE_OUTER_BOUND('',#3532,.T.);
#2734=FACE_OUTER_BOUND('',#3533,.T.);
#2735=FACE_OUTER_BOUND('',#3534,.T.);
#2736=FACE_OUTER_BOUND('',#3535,.T.);
#2737=FACE_OUTER_BOUND('',#3536,.T.);
#2738=FACE_OUTER_BOUND('',#3537,.T.);
#2739=FACE_OUTER_BOUND('',#3538,.T.);
#2740=FACE_OUTER_BOUND('',#3539,.T.);
#2741=FACE_OUTER_BOUND('',#3540,.T.);
#2742=FACE_OUTER_BOUND('',#3541,.T.);
#2743=FACE_OUTER_BOUND('',#3542,.T.);
#2744=FACE_OUTER_BOUND('',#3543,.T.);
#2745=FACE_OUTER_BOUND('',#3544,.T.);
#2746=FACE_OUTER_BOUND('',#3545,.T.);
#2747=FACE_OUTER_BOUND('',#3546,.T.);
#2748=FACE_OUTER_BOUND('',#3547,.T.);
#2749=FACE_OUTER_BOUND('',#3548,.T.);
#2750=FACE_OUTER_BOUND('',#3549,.T.);
#2751=FACE_OUTER_BOUND('',#3550,.T.);
#2752=FACE_OUTER_BOUND('',#3551,.T.);
#2753=FACE_OUTER_BOUND('',#3552,.T.);
#2754=FACE_OUTER_BOUND('',#3553,.T.);
#2755=FACE_OUTER_BOUND('',#3554,.T.);
#2756=FACE_OUTER_BOUND('',#3555,.T.);
#2757=FACE_OUTER_BOUND('',#3556,.T.);
#2758=FACE_OUTER_BOUND('',#3557,.T.);
#2759=FACE_OUTER_BOUND('',#3558,.T.);
#2760=FACE_OUTER_BOUND('',#3559,.T.);
#2761=FACE_OUTER_BOUND('',#3560,.T.);
#2762=FACE_OUTER_BOUND('',#3562,.T.);
#2763=FACE_OUTER_BOUND('',#3563,.T.);
#2764=FACE_OUTER_BOUND('',#3565,.T.);
#3510=EDGE_LOOP('',(#11461,#11462,#11463,#11464));
#3511=EDGE_LOOP('',(#11465,#11466,#11467,#11468));
#3512=EDGE_LOOP('',(#11469,#11470,#11471,#11472));
#3513=EDGE_LOOP('',(#11473,#11474,#11475,#11476));
#3514=EDGE_LOOP('',(#11477,#11478,#11479,#11480));
#3515=EDGE_LOOP('',(#11481,#11482,#11483,#11484));
#3516=EDGE_LOOP('',(#11485,#11486,#11487,#11488));
#3517=EDGE_LOOP('',(#11489,#11490,#11491,#11492));
#3518=EDGE_LOOP('',(#11493,#11494,#11495,#11496));
#3519=EDGE_LOOP('',(#11497,#11498,#11499,#11500));
#3520=EDGE_LOOP('',(#11501,#11502,#11503,#11504));
#3521=EDGE_LOOP('',(#11505,#11506,#11507,#11508));
#3522=EDGE_LOOP('',(#11509,#11510,#11511,#11512));
#3523=EDGE_LOOP('',(#11513,#11514,#11515,#11516));
#3524=EDGE_LOOP('',(#11517,#11518,#11519,#11520));
#3525=EDGE_LOOP('',(#11521,#11522,#11523,#11524));
#3526=EDGE_LOOP('',(#11525,#11526,#11527,#11528));
#3527=EDGE_LOOP('',(#11529,#11530,#11531,#11532));
#3528=EDGE_LOOP('',(#11533,#11534,#11535,#11536));
#3529=EDGE_LOOP('',(#11537,#11538,#11539,#11540));
#3530=EDGE_LOOP('',(#11541,#11542,#11543,#11544));
#3531=EDGE_LOOP('',(#11545,#11546,#11547,#11548));
#3532=EDGE_LOOP('',(#11549,#11550,#11551,#11552));
#3533=EDGE_LOOP('',(#11553,#11554,#11555,#11556));
#3534=EDGE_LOOP('',(#11557,#11558,#11559,#11560));
#3535=EDGE_LOOP('',(#11561,#11562,#11563,#11564));
#3536=EDGE_LOOP('',(#11565,#11566,#11567,#11568));
#3537=EDGE_LOOP('',(#11569,#11570,#11571,#11572));
#3538=EDGE_LOOP('',(#11573,#11574,#11575,#11576));
#3539=EDGE_LOOP('',(#11577,#11578,#11579,#11580));
#3540=EDGE_LOOP('',(#11581,#11582,#11583,#11584));
#3541=EDGE_LOOP('',(#11585,#11586,#11587,#11588));
#3542=EDGE_LOOP('',(#11589,#11590,#11591,#11592));
#3543=EDGE_LOOP('',(#11593,#11594,#11595,#11596));
#3544=EDGE_LOOP('',(#11597,#11598,#11599,#11600));
#3545=EDGE_LOOP('',(#11601,#11602,#11603,#11604));
#3546=EDGE_LOOP('',(#11605,#11606,#11607,#11608));
#3547=EDGE_LOOP('',(#11609,#11610,#11611,#11612));
#3548=EDGE_LOOP('',(#11613,#11614,#11615,#11616,#11617,#11618,#11619,#11620));
#3549=EDGE_LOOP('',(#11621,#11622,#11623,#11624,#11625,#11626,#11627,#11628,
#11629,#11630,#11631,#11632,#11633,#11634,#11635,#11636,#11637,#11638,#11639,
#11640,#11641,#11642,#11643,#11644,#11645,#11646,#11647,#11648,#11649,#11650,
#11651,#11652,#11653,#11654,#11655,#11656,#11657,#11658,#11659,#11660,#11661,
#11662));
#3550=EDGE_LOOP('',(#11663,#11664,#11665,#11666));
#3551=EDGE_LOOP('',(#11667,#11668,#11669,#11670,#11671,#11672,#11673,#11674,
#11675,#11676,#11677,#11678,#11679,#11680,#11681,#11682,#11683,#11684,#11685,
#11686,#11687,#11688,#11689,#11690,#11691,#11692,#11693,#11694,#11695,#11696,
#11697,#11698,#11699,#11700,#11701,#11702,#11703,#11704,#11705,#11706,#11707,
#11708,#11709));
#3552=EDGE_LOOP('',(#11710,#11711,#11712,#11713));
#3553=EDGE_LOOP('',(#11714,#11715,#11716,#11717));
#3554=EDGE_LOOP('',(#11718,#11719,#11720,#11721));
#3555=EDGE_LOOP('',(#11722,#11723,#11724,#11725));
#3556=EDGE_LOOP('',(#11726,#11727,#11728,#11729));
#3557=EDGE_LOOP('',(#11730,#11731,#11732,#11733));
#3558=EDGE_LOOP('',(#11734,#11735,#11736,#11737));
#3559=EDGE_LOOP('',(#11738,#11739,#11740,#11741,#11742,#11743));
#3560=EDGE_LOOP('',(#11744));
#3561=EDGE_LOOP('',(#11745,#11746,#11747,#11748));
#3562=EDGE_LOOP('',(#11749,#11750,#11751,#11752));
#3563=EDGE_LOOP('',(#11753));
#3564=EDGE_LOOP('',(#11754,#11755,#11756,#11757,#11758,#11759));
#3565=EDGE_LOOP('',(#11760));
#4379=LINE('',#44035,#5215);
#4380=LINE('',#44062,#5216);
#4381=LINE('',#44110,#5217);
#4382=LINE('',#44158,#5218);
#4383=LINE('',#44212,#5219);
#4384=LINE('',#44260,#5220);
#4385=LINE('',#44308,#5221);
#4386=LINE('',#44362,#5222);
#4387=LINE('',#44410,#5223);
#4388=LINE('',#44458,#5224);
#4389=LINE('',#44506,#5225);
#4390=LINE('',#44560,#5226);
#4391=LINE('',#44608,#5227);
#4392=LINE('',#44656,#5228);
#4393=LINE('',#44710,#5229);
#4394=LINE('',#44758,#5230);
#4395=LINE('',#44806,#5231);
#4396=LINE('',#44860,#5232);
#4397=LINE('',#44908,#5233);
#4398=LINE('',#44956,#5234);
#4399=LINE('',#44983,#5235);
#4400=LINE('',#45008,#5236);
#4401=LINE('',#45032,#5237);
#4402=LINE('',#45057,#5238);
#4403=LINE('',#45082,#5239);
#4404=LINE('',#45106,#5240);
#4405=LINE('',#45131,#5241);
#4406=LINE('',#45156,#5242);
#4407=LINE('',#45180,#5243);
#4408=LINE('',#45205,#5244);
#4409=LINE('',#45230,#5245);
#4410=LINE('',#45254,#5246);
#4411=LINE('',#45278,#5247);
#4412=LINE('',#45303,#5248);
#4413=LINE('',#45328,#5249);
#4414=LINE('',#45352,#5250);
#4415=LINE('',#45377,#5251);
#4416=LINE('',#45402,#5252);
#4417=LINE('',#45783,#5253);
#4418=LINE('',#47101,#5254);
#4419=LINE('',#47103,#5255);
#4420=LINE('',#47105,#5256);
#4421=LINE('',#47106,#5257);
#4422=LINE('',#47109,#5258);
#4423=LINE('',#47111,#5259);
#4424=LINE('',#47112,#5260);
#4425=LINE('',#47115,#5261);
#4426=LINE('',#47117,#5262);
#4427=LINE('',#47118,#5263);
#4428=LINE('',#47121,#5264);
#4429=LINE('',#47123,#5265);
#4430=LINE('',#47124,#5266);
#4431=LINE('',#47127,#5267);
#4432=LINE('',#47129,#5268);
#4433=LINE('',#47130,#5269);
#4434=LINE('',#47132,#5270);
#4435=LINE('',#47133,#5271);
#4436=LINE('',#47140,#5272);
#5215=VECTOR('',#17166,5.);
#5216=VECTOR('',#17171,5.);
#5217=VECTOR('',#17174,5.);
#5218=VECTOR('',#17177,5.);
#5219=VECTOR('',#17180,5.);
#5220=VECTOR('',#17183,5.);
#5221=VECTOR('',#17186,5.);
#5222=VECTOR('',#17189,5.);
#5223=VECTOR('',#17192,5.);
#5224=VECTOR('',#17195,5.);
#5225=VECTOR('',#17198,5.);
#5226=VECTOR('',#17201,5.);
#5227=VECTOR('',#17204,5.);
#5228=VECTOR('',#17207,5.);
#5229=VECTOR('',#17210,5.);
#5230=VECTOR('',#17213,5.);
#5231=VECTOR('',#17216,5.);
#5232=VECTOR('',#17219,5.);
#5233=VECTOR('',#17222,5.);
#5234=VECTOR('',#17225,4.372);
#5235=VECTOR('',#17230,4.372);
#5236=VECTOR('',#17233,4.372);
#5237=VECTOR('',#17236,4.372);
#5238=VECTOR('',#17239,4.372);
#5239=VECTOR('',#17242,4.372);
#5240=VECTOR('',#17245,4.372);
#5241=VECTOR('',#17248,4.372);
#5242=VECTOR('',#17251,4.372);
#5243=VECTOR('',#17254,4.372);
#5244=VECTOR('',#17257,4.372);
#5245=VECTOR('',#17260,4.372);
#5246=VECTOR('',#17263,4.372);
#5247=VECTOR('',#17266,4.372);
#5248=VECTOR('',#17269,4.372);
#5249=VECTOR('',#17272,4.372);
#5250=VECTOR('',#17275,4.372);
#5251=VECTOR('',#17278,4.372);
#5252=VECTOR('',#17281,4.372);
#5253=VECTOR('',#17286,4.5);
#5254=VECTOR('',#17297,10.);
#5255=VECTOR('',#17298,10.);
#5256=VECTOR('',#17299,10.);
#5257=VECTOR('',#17300,10.);
#5258=VECTOR('',#17303,10.);
#5259=VECTOR('',#17304,10.);
#5260=VECTOR('',#17305,10.);
#5261=VECTOR('',#17308,10.);
#5262=VECTOR('',#17309,10.);
#5263=VECTOR('',#17310,10.);
#5264=VECTOR('',#17313,10.);
#5265=VECTOR('',#17314,10.);
#5266=VECTOR('',#17315,10.);
#5267=VECTOR('',#17318,10.);
#5268=VECTOR('',#17319,10.);
#5269=VECTOR('',#17320,10.);
#5270=VECTOR('',#17323,10.);
#5271=VECTOR('',#17324,10.);
#5272=VECTOR('',#17333,8.);
#6336=VERTEX_POINT('',#44033);
#6337=VERTEX_POINT('',#44034);
#6338=VERTEX_POINT('',#44036);
#6339=VERTEX_POINT('',#44047);
#6340=VERTEX_POINT('',#44060);
#6341=VERTEX_POINT('',#44061);
#6342=VERTEX_POINT('',#44108);
#6343=VERTEX_POINT('',#44109);
#6344=VERTEX_POINT('',#44156);
#6345=VERTEX_POINT('',#44157);
#6346=VERTEX_POINT('',#44210);
#6347=VERTEX_POINT('',#44211);
#6348=VERTEX_POINT('',#44258);
#6349=VERTEX_POINT('',#44259);
#6350=VERTEX_POINT('',#44306);
#6351=VERTEX_POINT('',#44307);
#6352=VERTEX_POINT('',#44360);
#6353=VERTEX_POINT('',#44361);
#6354=VERTEX_POINT('',#44408);
#6355=VERTEX_POINT('',#44409);
#6356=VERTEX_POINT('',#44456);
#6357=VERTEX_POINT('',#44457);
#6358=VERTEX_POINT('',#44504);
#6359=VERTEX_POINT('',#44505);
#6360=VERTEX_POINT('',#44558);
#6361=VERTEX_POINT('',#44559);
#6362=VERTEX_POINT('',#44606);
#6363=VERTEX_POINT('',#44607);
#6364=VERTEX_POINT('',#44654);
#6365=VERTEX_POINT('',#44655);
#6366=VERTEX_POINT('',#44708);
#6367=VERTEX_POINT('',#44709);
#6368=VERTEX_POINT('',#44756);
#6369=VERTEX_POINT('',#44757);
#6370=VERTEX_POINT('',#44804);
#6371=VERTEX_POINT('',#44805);
#6372=VERTEX_POINT('',#44858);
#6373=VERTEX_POINT('',#44859);
#6374=VERTEX_POINT('',#44906);
#6375=VERTEX_POINT('',#44907);
#6376=VERTEX_POINT('',#44954);
#6377=VERTEX_POINT('',#44955);
#6378=VERTEX_POINT('',#44957);
#6379=VERTEX_POINT('',#44969);
#6380=VERTEX_POINT('',#44981);
#6381=VERTEX_POINT('',#44982);
#6382=VERTEX_POINT('',#45006);
#6383=VERTEX_POINT('',#45007);
#6384=VERTEX_POINT('',#45030);
#6385=VERTEX_POINT('',#45031);
#6386=VERTEX_POINT('',#45055);
#6387=VERTEX_POINT('',#45056);
#6388=VERTEX_POINT('',#45080);
#6389=VERTEX_POINT('',#45081);
#6390=VERTEX_POINT('',#45104);
#6391=VERTEX_POINT('',#45105);
#6392=VERTEX_POINT('',#45129);
#6393=VERTEX_POINT('',#45130);
#6394=VERTEX_POINT('',#45154);
#6395=VERTEX_POINT('',#45155);
#6396=VERTEX_POINT('',#45178);
#6397=VERTEX_POINT('',#45179);
#6398=VERTEX_POINT('',#45203);
#6399=VERTEX_POINT('',#45204);
#6400=VERTEX_POINT('',#45228);
#6401=VERTEX_POINT('',#45229);
#6402=VERTEX_POINT('',#45252);
#6403=VERTEX_POINT('',#45253);
#6404=VERTEX_POINT('',#45276);
#6405=VERTEX_POINT('',#45277);
#6406=VERTEX_POINT('',#45301);
#6407=VERTEX_POINT('',#45302);
#6408=VERTEX_POINT('',#45326);
#6409=VERTEX_POINT('',#45327);
#6410=VERTEX_POINT('',#45350);
#6411=VERTEX_POINT('',#45351);
#6412=VERTEX_POINT('',#45375);
#6413=VERTEX_POINT('',#45376);
#6414=VERTEX_POINT('',#45400);
#6415=VERTEX_POINT('',#45401);
#6416=VERTEX_POINT('',#45424);
#6417=VERTEX_POINT('',#45669);
#6418=VERTEX_POINT('',#45743);
#6419=VERTEX_POINT('',#45782);
#6420=VERTEX_POINT('',#46301);
#6421=VERTEX_POINT('',#46434);
#6422=VERTEX_POINT('',#47099);
#6423=VERTEX_POINT('',#47100);
#6424=VERTEX_POINT('',#47102);
#6425=VERTEX_POINT('',#47104);
#6426=VERTEX_POINT('',#47108);
#6427=VERTEX_POINT('',#47110);
#6428=VERTEX_POINT('',#47114);
#6429=VERTEX_POINT('',#47116);
#6430=VERTEX_POINT('',#47120);
#6431=VERTEX_POINT('',#47122);
#6432=VERTEX_POINT('',#47126);
#6433=VERTEX_POINT('',#47128);
#6434=VERTEX_POINT('',#47136);
#6435=VERTEX_POINT('',#47139);
#8153=EDGE_CURVE('',#6336,#6337,#4379,.T.);
#8154=EDGE_CURVE('',#6336,#6338,#1028,.T.);
#8155=EDGE_CURVE('',#6338,#6339,#418,.F.);
#8156=EDGE_CURVE('',#6339,#6337,#1029,.T.);
#8157=EDGE_CURVE('',#6340,#6341,#4380,.T.);
#8158=EDGE_CURVE('',#6340,#6336,#1030,.T.);
#8159=EDGE_CURVE('',#6337,#6341,#1031,.T.);
#8160=EDGE_CURVE('',#6342,#6343,#4381,.T.);
#8161=EDGE_CURVE('',#6342,#6340,#1032,.T.);
#8162=EDGE_CURVE('',#6341,#6343,#1033,.T.);
#8163=EDGE_CURVE('',#6344,#6345,#4382,.T.);
#8164=EDGE_CURVE('',#6344,#6342,#1034,.T.);
#8165=EDGE_CURVE('',#6343,#6345,#1035,.T.);
#8166=EDGE_CURVE('',#6346,#6347,#4383,.T.);
#8167=EDGE_CURVE('',#6346,#6344,#1036,.T.);
#8168=EDGE_CURVE('',#6345,#6347,#1037,.T.);
#8169=EDGE_CURVE('',#6348,#6349,#4384,.T.);
#8170=EDGE_CURVE('',#6348,#6346,#1038,.T.);
#8171=EDGE_CURVE('',#6347,#6349,#1039,.T.);
#8172=EDGE_CURVE('',#6350,#6351,#4385,.T.);
#8173=EDGE_CURVE('',#6350,#6348,#1040,.T.);
#8174=EDGE_CURVE('',#6349,#6351,#1041,.T.);
#8175=EDGE_CURVE('',#6352,#6353,#4386,.T.);
#8176=EDGE_CURVE('',#6352,#6350,#1042,.T.);
#8177=EDGE_CURVE('',#6351,#6353,#1043,.T.);
#8178=EDGE_CURVE('',#6354,#6355,#4387,.T.);
#8179=EDGE_CURVE('',#6354,#6352,#1044,.T.);
#8180=EDGE_CURVE('',#6353,#6355,#1045,.T.);
#8181=EDGE_CURVE('',#6356,#6357,#4388,.T.);
#8182=EDGE_CURVE('',#6356,#6354,#1046,.T.);
#8183=EDGE_CURVE('',#6355,#6357,#1047,.T.);
#8184=EDGE_CURVE('',#6358,#6359,#4389,.T.);
#8185=EDGE_CURVE('',#6358,#6356,#1048,.T.);
#8186=EDGE_CURVE('',#6357,#6359,#1049,.T.);
#8187=EDGE_CURVE('',#6360,#6361,#4390,.T.);
#8188=EDGE_CURVE('',#6360,#6358,#1050,.T.);
#8189=EDGE_CURVE('',#6359,#6361,#1051,.T.);
#8190=EDGE_CURVE('',#6362,#6363,#4391,.T.);
#8191=EDGE_CURVE('',#6362,#6360,#1052,.T.);
#8192=EDGE_CURVE('',#6361,#6363,#1053,.T.);
#8193=EDGE_CURVE('',#6364,#6365,#4392,.T.);
#8194=EDGE_CURVE('',#6364,#6362,#1054,.T.);
#8195=EDGE_CURVE('',#6363,#6365,#1055,.T.);
#8196=EDGE_CURVE('',#6366,#6367,#4393,.T.);
#8197=EDGE_CURVE('',#6366,#6364,#1056,.T.);
#8198=EDGE_CURVE('',#6365,#6367,#1057,.T.);
#8199=EDGE_CURVE('',#6368,#6369,#4394,.T.);
#8200=EDGE_CURVE('',#6368,#6366,#1058,.T.);
#8201=EDGE_CURVE('',#6367,#6369,#1059,.T.);
#8202=EDGE_CURVE('',#6370,#6371,#4395,.T.);
#8203=EDGE_CURVE('',#6370,#6368,#1060,.T.);
#8204=EDGE_CURVE('',#6369,#6371,#1061,.T.);
#8205=EDGE_CURVE('',#6372,#6373,#4396,.T.);
#8206=EDGE_CURVE('',#6372,#6370,#1062,.T.);
#8207=EDGE_CURVE('',#6371,#6373,#1063,.T.);
#8208=EDGE_CURVE('',#6374,#6375,#4397,.T.);
#8209=EDGE_CURVE('',#6374,#6372,#1064,.T.);
#8210=EDGE_CURVE('',#6373,#6375,#1065,.T.);
#8211=EDGE_CURVE('',#6376,#6377,#4398,.T.);
#8212=EDGE_CURVE('',#6376,#6378,#1066,.T.);
#8213=EDGE_CURVE('',#6378,#6379,#419,.T.);
#8214=EDGE_CURVE('',#6377,#6379,#1067,.T.);
#8215=EDGE_CURVE('',#6380,#6381,#4399,.T.);
#8216=EDGE_CURVE('',#6380,#6376,#1068,.T.);
#8217=EDGE_CURVE('',#6381,#6377,#1069,.T.);
#8218=EDGE_CURVE('',#6382,#6383,#4400,.T.);
#8219=EDGE_CURVE('',#6382,#6380,#1070,.T.);
#8220=EDGE_CURVE('',#6383,#6381,#1071,.T.);
#8221=EDGE_CURVE('',#6384,#6385,#4401,.T.);
#8222=EDGE_CURVE('',#6384,#6382,#1072,.T.);
#8223=EDGE_CURVE('',#6385,#6383,#1073,.T.);
#8224=EDGE_CURVE('',#6386,#6387,#4402,.T.);
#8225=EDGE_CURVE('',#6386,#6384,#1074,.T.);
#8226=EDGE_CURVE('',#6387,#6385,#1075,.T.);
#8227=EDGE_CURVE('',#6388,#6389,#4403,.T.);
#8228=EDGE_CURVE('',#6388,#6386,#1076,.T.);
#8229=EDGE_CURVE('',#6389,#6387,#1077,.T.);
#8230=EDGE_CURVE('',#6390,#6391,#4404,.T.);
#8231=EDGE_CURVE('',#6390,#6388,#1078,.T.);
#8232=EDGE_CURVE('',#6391,#6389,#1079,.T.);
#8233=EDGE_CURVE('',#6392,#6393,#4405,.T.);
#8234=EDGE_CURVE('',#6392,#6390,#1080,.T.);
#8235=EDGE_CURVE('',#6393,#6391,#1081,.T.);
#8236=EDGE_CURVE('',#6394,#6395,#4406,.T.);
#8237=EDGE_CURVE('',#6394,#6392,#1082,.T.);
#8238=EDGE_CURVE('',#6395,#6393,#1083,.T.);
#8239=EDGE_CURVE('',#6396,#6397,#4407,.T.);
#8240=EDGE_CURVE('',#6396,#6394,#1084,.T.);
#8241=EDGE_CURVE('',#6397,#6395,#1085,.T.);
#8242=EDGE_CURVE('',#6398,#6399,#4408,.T.);
#8243=EDGE_CURVE('',#6398,#6396,#1086,.T.);
#8244=EDGE_CURVE('',#6399,#6397,#1087,.T.);
#8245=EDGE_CURVE('',#6400,#6401,#4409,.T.);
#8246=EDGE_CURVE('',#6400,#6398,#1088,.T.);
#8247=EDGE_CURVE('',#6401,#6399,#1089,.T.);
#8248=EDGE_CURVE('',#6402,#6403,#4410,.T.);
#8249=EDGE_CURVE('',#6402,#6400,#1090,.T.);
#8250=EDGE_CURVE('',#6403,#6401,#1091,.T.);
#8251=EDGE_CURVE('',#6404,#6405,#4411,.T.);
#8252=EDGE_CURVE('',#6404,#6402,#1092,.T.);
#8253=EDGE_CURVE('',#6405,#6403,#1093,.T.);
#8254=EDGE_CURVE('',#6406,#6407,#4412,.T.);
#8255=EDGE_CURVE('',#6406,#6404,#1094,.T.);
#8256=EDGE_CURVE('',#6407,#6405,#1095,.T.);
#8257=EDGE_CURVE('',#6408,#6409,#4413,.T.);
#8258=EDGE_CURVE('',#6408,#6406,#1096,.T.);
#8259=EDGE_CURVE('',#6409,#6407,#1097,.T.);
#8260=EDGE_CURVE('',#6410,#6411,#4414,.T.);
#8261=EDGE_CURVE('',#6410,#6408,#1098,.T.);
#8262=EDGE_CURVE('',#6411,#6409,#1099,.T.);
#8263=EDGE_CURVE('',#6412,#6413,#4415,.T.);
#8264=EDGE_CURVE('',#6412,#6410,#1100,.T.);
#8265=EDGE_CURVE('',#6413,#6411,#1101,.T.);
#8266=EDGE_CURVE('',#6414,#6415,#4416,.T.);
#8267=EDGE_CURVE('',#6414,#6412,#1102,.T.);
#8268=EDGE_CURVE('',#6415,#6413,#1103,.T.);
#8269=EDGE_CURVE('',#6379,#6416,#1104,.T.);
#8270=EDGE_CURVE('',#6417,#6378,#1105,.T.);
#8271=EDGE_CURVE('',#6418,#6417,#420,.T.);
#8272=EDGE_CURVE('',#6416,#6418,#1106,.T.);
#8273=EDGE_CURVE('',#6416,#6419,#4417,.T.);
#8274=EDGE_CURVE('',#6419,#6419,#421,.T.);
#8275=EDGE_CURVE('',#6420,#6414,#1107,.T.);
#8276=EDGE_CURVE('',#6338,#6420,#1108,.T.);
#8277=EDGE_CURVE('',#6417,#6374,#1109,.T.);
#8278=EDGE_CURVE('',#6421,#6415,#1110,.T.);
#8279=EDGE_CURVE('',#6420,#6421,#422,.T.);
#8280=EDGE_CURVE('',#6375,#6418,#1111,.T.);
#8281=EDGE_CURVE('',#6421,#6339,#1112,.T.);
#8282=EDGE_CURVE('',#6422,#6423,#4418,.T.);
#8283=EDGE_CURVE('',#6422,#6424,#4419,.T.);
#8284=EDGE_CURVE('',#6424,#6425,#4420,.T.);
#8285=EDGE_CURVE('',#6423,#6425,#4421,.T.);
#8286=EDGE_CURVE('',#6426,#6422,#4422,.T.);
#8287=EDGE_CURVE('',#6426,#6427,#4423,.T.);
#8288=EDGE_CURVE('',#6427,#6424,#4424,.T.);
#8289=EDGE_CURVE('',#6428,#6426,#4425,.T.);
#8290=EDGE_CURVE('',#6428,#6429,#4426,.T.);
#8291=EDGE_CURVE('',#6429,#6427,#4427,.T.);
#8292=EDGE_CURVE('',#6430,#6428,#4428,.T.);
#8293=EDGE_CURVE('',#6430,#6431,#4429,.T.);
#8294=EDGE_CURVE('',#6431,#6429,#4430,.T.);
#8295=EDGE_CURVE('',#6432,#6430,#4431,.T.);
#8296=EDGE_CURVE('',#6432,#6433,#4432,.T.);
#8297=EDGE_CURVE('',#6433,#6431,#4433,.T.);
#8298=EDGE_CURVE('',#6423,#6432,#4434,.T.);
#8299=EDGE_CURVE('',#6425,#6433,#4435,.T.);
#8300=EDGE_CURVE('',#6434,#6434,#423,.T.);
#8301=EDGE_CURVE('',#6434,#6435,#4436,.T.);
#8302=EDGE_CURVE('',#6435,#6435,#424,.T.);
#11461=ORIENTED_EDGE('',*,*,#8153,.F.);
#11462=ORIENTED_EDGE('',*,*,#8154,.T.);
#11463=ORIENTED_EDGE('',*,*,#8155,.T.);
#11464=ORIENTED_EDGE('',*,*,#8156,.T.);
#11465=ORIENTED_EDGE('',*,*,#8157,.F.);
#11466=ORIENTED_EDGE('',*,*,#8158,.T.);
#11467=ORIENTED_EDGE('',*,*,#8153,.T.);
#11468=ORIENTED_EDGE('',*,*,#8159,.T.);
#11469=ORIENTED_EDGE('',*,*,#8160,.F.);
#11470=ORIENTED_EDGE('',*,*,#8161,.T.);
#11471=ORIENTED_EDGE('',*,*,#8157,.T.);
#11472=ORIENTED_EDGE('',*,*,#8162,.T.);
#11473=ORIENTED_EDGE('',*,*,#8163,.F.);
#11474=ORIENTED_EDGE('',*,*,#8164,.T.);
#11475=ORIENTED_EDGE('',*,*,#8160,.T.);
#11476=ORIENTED_EDGE('',*,*,#8165,.T.);
#11477=ORIENTED_EDGE('',*,*,#8166,.F.);
#11478=ORIENTED_EDGE('',*,*,#8167,.T.);
#11479=ORIENTED_EDGE('',*,*,#8163,.T.);
#11480=ORIENTED_EDGE('',*,*,#8168,.T.);
#11481=ORIENTED_EDGE('',*,*,#8169,.F.);
#11482=ORIENTED_EDGE('',*,*,#8170,.T.);
#11483=ORIENTED_EDGE('',*,*,#8166,.T.);
#11484=ORIENTED_EDGE('',*,*,#8171,.T.);
#11485=ORIENTED_EDGE('',*,*,#8172,.F.);
#11486=ORIENTED_EDGE('',*,*,#8173,.T.);
#11487=ORIENTED_EDGE('',*,*,#8169,.T.);
#11488=ORIENTED_EDGE('',*,*,#8174,.T.);
#11489=ORIENTED_EDGE('',*,*,#8175,.F.);
#11490=ORIENTED_EDGE('',*,*,#8176,.T.);
#11491=ORIENTED_EDGE('',*,*,#8172,.T.);
#11492=ORIENTED_EDGE('',*,*,#8177,.T.);
#11493=ORIENTED_EDGE('',*,*,#8178,.F.);
#11494=ORIENTED_EDGE('',*,*,#8179,.T.);
#11495=ORIENTED_EDGE('',*,*,#8175,.T.);
#11496=ORIENTED_EDGE('',*,*,#8180,.T.);
#11497=ORIENTED_EDGE('',*,*,#8181,.F.);
#11498=ORIENTED_EDGE('',*,*,#8182,.T.);
#11499=ORIENTED_EDGE('',*,*,#8178,.T.);
#11500=ORIENTED_EDGE('',*,*,#8183,.T.);
#11501=ORIENTED_EDGE('',*,*,#8184,.F.);
#11502=ORIENTED_EDGE('',*,*,#8185,.T.);
#11503=ORIENTED_EDGE('',*,*,#8181,.T.);
#11504=ORIENTED_EDGE('',*,*,#8186,.T.);
#11505=ORIENTED_EDGE('',*,*,#8187,.F.);
#11506=ORIENTED_EDGE('',*,*,#8188,.T.);
#11507=ORIENTED_EDGE('',*,*,#8184,.T.);
#11508=ORIENTED_EDGE('',*,*,#8189,.T.);
#11509=ORIENTED_EDGE('',*,*,#8190,.F.);
#11510=ORIENTED_EDGE('',*,*,#8191,.T.);
#11511=ORIENTED_EDGE('',*,*,#8187,.T.);
#11512=ORIENTED_EDGE('',*,*,#8192,.T.);
#11513=ORIENTED_EDGE('',*,*,#8193,.F.);
#11514=ORIENTED_EDGE('',*,*,#8194,.T.);
#11515=ORIENTED_EDGE('',*,*,#8190,.T.);
#11516=ORIENTED_EDGE('',*,*,#8195,.T.);
#11517=ORIENTED_EDGE('',*,*,#8196,.F.);
#11518=ORIENTED_EDGE('',*,*,#8197,.T.);
#11519=ORIENTED_EDGE('',*,*,#8193,.T.);
#11520=ORIENTED_EDGE('',*,*,#8198,.T.);
#11521=ORIENTED_EDGE('',*,*,#8199,.F.);
#11522=ORIENTED_EDGE('',*,*,#8200,.T.);
#11523=ORIENTED_EDGE('',*,*,#8196,.T.);
#11524=ORIENTED_EDGE('',*,*,#8201,.T.);
#11525=ORIENTED_EDGE('',*,*,#8202,.F.);
#11526=ORIENTED_EDGE('',*,*,#8203,.T.);
#11527=ORIENTED_EDGE('',*,*,#8199,.T.);
#11528=ORIENTED_EDGE('',*,*,#8204,.T.);
#11529=ORIENTED_EDGE('',*,*,#8205,.F.);
#11530=ORIENTED_EDGE('',*,*,#8206,.T.);
#11531=ORIENTED_EDGE('',*,*,#8202,.T.);
#11532=ORIENTED_EDGE('',*,*,#8207,.T.);
#11533=ORIENTED_EDGE('',*,*,#8208,.F.);
#11534=ORIENTED_EDGE('',*,*,#8209,.T.);
#11535=ORIENTED_EDGE('',*,*,#8205,.T.);
#11536=ORIENTED_EDGE('',*,*,#8210,.T.);
#11537=ORIENTED_EDGE('',*,*,#8211,.F.);
#11538=ORIENTED_EDGE('',*,*,#8212,.T.);
#11539=ORIENTED_EDGE('',*,*,#8213,.T.);
#11540=ORIENTED_EDGE('',*,*,#8214,.F.);
#11541=ORIENTED_EDGE('',*,*,#8215,.F.);
#11542=ORIENTED_EDGE('',*,*,#8216,.T.);
#11543=ORIENTED_EDGE('',*,*,#8211,.T.);
#11544=ORIENTED_EDGE('',*,*,#8217,.F.);
#11545=ORIENTED_EDGE('',*,*,#8218,.F.);
#11546=ORIENTED_EDGE('',*,*,#8219,.T.);
#11547=ORIENTED_EDGE('',*,*,#8215,.T.);
#11548=ORIENTED_EDGE('',*,*,#8220,.F.);
#11549=ORIENTED_EDGE('',*,*,#8221,.F.);
#11550=ORIENTED_EDGE('',*,*,#8222,.T.);
#11551=ORIENTED_EDGE('',*,*,#8218,.T.);
#11552=ORIENTED_EDGE('',*,*,#8223,.F.);
#11553=ORIENTED_EDGE('',*,*,#8224,.F.);
#11554=ORIENTED_EDGE('',*,*,#8225,.T.);
#11555=ORIENTED_EDGE('',*,*,#8221,.T.);
#11556=ORIENTED_EDGE('',*,*,#8226,.F.);
#11557=ORIENTED_EDGE('',*,*,#8227,.F.);
#11558=ORIENTED_EDGE('',*,*,#8228,.T.);
#11559=ORIENTED_EDGE('',*,*,#8224,.T.);
#11560=ORIENTED_EDGE('',*,*,#8229,.F.);
#11561=ORIENTED_EDGE('',*,*,#8230,.F.);
#11562=ORIENTED_EDGE('',*,*,#8231,.T.);
#11563=ORIENTED_EDGE('',*,*,#8227,.T.);
#11564=ORIENTED_EDGE('',*,*,#8232,.F.);
#11565=ORIENTED_EDGE('',*,*,#8233,.F.);
#11566=ORIENTED_EDGE('',*,*,#8234,.T.);
#11567=ORIENTED_EDGE('',*,*,#8230,.T.);
#11568=ORIENTED_EDGE('',*,*,#8235,.F.);
#11569=ORIENTED_EDGE('',*,*,#8236,.F.);
#11570=ORIENTED_EDGE('',*,*,#8237,.T.);
#11571=ORIENTED_EDGE('',*,*,#8233,.T.);
#11572=ORIENTED_EDGE('',*,*,#8238,.F.);
#11573=ORIENTED_EDGE('',*,*,#8239,.F.);
#11574=ORIENTED_EDGE('',*,*,#8240,.T.);
#11575=ORIENTED_EDGE('',*,*,#8236,.T.);
#11576=ORIENTED_EDGE('',*,*,#8241,.F.);
#11577=ORIENTED_EDGE('',*,*,#8242,.F.);
#11578=ORIENTED_EDGE('',*,*,#8243,.T.);
#11579=ORIENTED_EDGE('',*,*,#8239,.T.);
#11580=ORIENTED_EDGE('',*,*,#8244,.F.);
#11581=ORIENTED_EDGE('',*,*,#8245,.F.);
#11582=ORIENTED_EDGE('',*,*,#8246,.T.);
#11583=ORIENTED_EDGE('',*,*,#8242,.T.);
#11584=ORIENTED_EDGE('',*,*,#8247,.F.);
#11585=ORIENTED_EDGE('',*,*,#8248,.F.);
#11586=ORIENTED_EDGE('',*,*,#8249,.T.);
#11587=ORIENTED_EDGE('',*,*,#8245,.T.);
#11588=ORIENTED_EDGE('',*,*,#8250,.F.);
#11589=ORIENTED_EDGE('',*,*,#8251,.F.);
#11590=ORIENTED_EDGE('',*,*,#8252,.T.);
#11591=ORIENTED_EDGE('',*,*,#8248,.T.);
#11592=ORIENTED_EDGE('',*,*,#8253,.F.);
#11593=ORIENTED_EDGE('',*,*,#8254,.F.);
#11594=ORIENTED_EDGE('',*,*,#8255,.T.);
#11595=ORIENTED_EDGE('',*,*,#8251,.T.);
#11596=ORIENTED_EDGE('',*,*,#8256,.F.);
#11597=ORIENTED_EDGE('',*,*,#8257,.F.);
#11598=ORIENTED_EDGE('',*,*,#8258,.T.);
#11599=ORIENTED_EDGE('',*,*,#8254,.T.);
#11600=ORIENTED_EDGE('',*,*,#8259,.F.);
#11601=ORIENTED_EDGE('',*,*,#8260,.F.);
#11602=ORIENTED_EDGE('',*,*,#8261,.T.);
#11603=ORIENTED_EDGE('',*,*,#8257,.T.);
#11604=ORIENTED_EDGE('',*,*,#8262,.F.);
#11605=ORIENTED_EDGE('',*,*,#8263,.F.);
#11606=ORIENTED_EDGE('',*,*,#8264,.T.);
#11607=ORIENTED_EDGE('',*,*,#8260,.T.);
#11608=ORIENTED_EDGE('',*,*,#8265,.F.);
#11609=ORIENTED_EDGE('',*,*,#8266,.F.);
#11610=ORIENTED_EDGE('',*,*,#8267,.T.);
#11611=ORIENTED_EDGE('',*,*,#8263,.T.);
#11612=ORIENTED_EDGE('',*,*,#8268,.F.);
#11613=ORIENTED_EDGE('',*,*,#8269,.F.);
#11614=ORIENTED_EDGE('',*,*,#8213,.F.);
#11615=ORIENTED_EDGE('',*,*,#8270,.F.);
#11616=ORIENTED_EDGE('',*,*,#8271,.F.);
#11617=ORIENTED_EDGE('',*,*,#8272,.F.);
#11618=ORIENTED_EDGE('',*,*,#8273,.T.);
#11619=ORIENTED_EDGE('',*,*,#8274,.F.);
#11620=ORIENTED_EDGE('',*,*,#8273,.F.);
#11621=ORIENTED_EDGE('',*,*,#8270,.T.);
#11622=ORIENTED_EDGE('',*,*,#8212,.F.);
#11623=ORIENTED_EDGE('',*,*,#8216,.F.);
#11624=ORIENTED_EDGE('',*,*,#8219,.F.);
#11625=ORIENTED_EDGE('',*,*,#8222,.F.);
#11626=ORIENTED_EDGE('',*,*,#8225,.F.);
#11627=ORIENTED_EDGE('',*,*,#8228,.F.);
#11628=ORIENTED_EDGE('',*,*,#8231,.F.);
#11629=ORIENTED_EDGE('',*,*,#8234,.F.);
#11630=ORIENTED_EDGE('',*,*,#8237,.F.);
#11631=ORIENTED_EDGE('',*,*,#8240,.F.);
#11632=ORIENTED_EDGE('',*,*,#8243,.F.);
#11633=ORIENTED_EDGE('',*,*,#8246,.F.);
#11634=ORIENTED_EDGE('',*,*,#8249,.F.);
#11635=ORIENTED_EDGE('',*,*,#8252,.F.);
#11636=ORIENTED_EDGE('',*,*,#8255,.F.);
#11637=ORIENTED_EDGE('',*,*,#8258,.F.);
#11638=ORIENTED_EDGE('',*,*,#8261,.F.);
#11639=ORIENTED_EDGE('',*,*,#8264,.F.);
#11640=ORIENTED_EDGE('',*,*,#8267,.F.);
#11641=ORIENTED_EDGE('',*,*,#8275,.F.);
#11642=ORIENTED_EDGE('',*,*,#8276,.F.);
#11643=ORIENTED_EDGE('',*,*,#8154,.F.);
#11644=ORIENTED_EDGE('',*,*,#8158,.F.);
#11645=ORIENTED_EDGE('',*,*,#8161,.F.);
#11646=ORIENTED_EDGE('',*,*,#8164,.F.);
#11647=ORIENTED_EDGE('',*,*,#8167,.F.);
#11648=ORIENTED_EDGE('',*,*,#8170,.F.);
#11649=ORIENTED_EDGE('',*,*,#8173,.F.);
#11650=ORIENTED_EDGE('',*,*,#8176,.F.);
#11651=ORIENTED_EDGE('',*,*,#8179,.F.);
#11652=ORIENTED_EDGE('',*,*,#8182,.F.);
#11653=ORIENTED_EDGE('',*,*,#8185,.F.);
#11654=ORIENTED_EDGE('',*,*,#8188,.F.);
#11655=ORIENTED_EDGE('',*,*,#8191,.F.);
#11656=ORIENTED_EDGE('',*,*,#8194,.F.);
#11657=ORIENTED_EDGE('',*,*,#8197,.F.);
#11658=ORIENTED_EDGE('',*,*,#8200,.F.);
#11659=ORIENTED_EDGE('',*,*,#8203,.F.);
#11660=ORIENTED_EDGE('',*,*,#8206,.F.);
#11661=ORIENTED_EDGE('',*,*,#8209,.F.);
#11662=ORIENTED_EDGE('',*,*,#8277,.F.);
#11663=ORIENTED_EDGE('',*,*,#8266,.T.);
#11664=ORIENTED_EDGE('',*,*,#8278,.F.);
#11665=ORIENTED_EDGE('',*,*,#8279,.F.);
#11666=ORIENTED_EDGE('',*,*,#8275,.T.);
#11667=ORIENTED_EDGE('',*,*,#8269,.T.);
#11668=ORIENTED_EDGE('',*,*,#8272,.T.);
#11669=ORIENTED_EDGE('',*,*,#8280,.F.);
#11670=ORIENTED_EDGE('',*,*,#8210,.F.);
#11671=ORIENTED_EDGE('',*,*,#8207,.F.);
#11672=ORIENTED_EDGE('',*,*,#8204,.F.);
#11673=ORIENTED_EDGE('',*,*,#8201,.F.);
#11674=ORIENTED_EDGE('',*,*,#8198,.F.);
#11675=ORIENTED_EDGE('',*,*,#8195,.F.);
#11676=ORIENTED_EDGE('',*,*,#8192,.F.);
#11677=ORIENTED_EDGE('',*,*,#8189,.F.);
#11678=ORIENTED_EDGE('',*,*,#8186,.F.);
#11679=ORIENTED_EDGE('',*,*,#8183,.F.);
#11680=ORIENTED_EDGE('',*,*,#8180,.F.);
#11681=ORIENTED_EDGE('',*,*,#8177,.F.);
#11682=ORIENTED_EDGE('',*,*,#8174,.F.);
#11683=ORIENTED_EDGE('',*,*,#8171,.F.);
#11684=ORIENTED_EDGE('',*,*,#8168,.F.);
#11685=ORIENTED_EDGE('',*,*,#8165,.F.);
#11686=ORIENTED_EDGE('',*,*,#8162,.F.);
#11687=ORIENTED_EDGE('',*,*,#8159,.F.);
#11688=ORIENTED_EDGE('',*,*,#8156,.F.);
#11689=ORIENTED_EDGE('',*,*,#8281,.F.);
#11690=ORIENTED_EDGE('',*,*,#8278,.T.);
#11691=ORIENTED_EDGE('',*,*,#8268,.T.);
#11692=ORIENTED_EDGE('',*,*,#8265,.T.);
#11693=ORIENTED_EDGE('',*,*,#8262,.T.);
#11694=ORIENTED_EDGE('',*,*,#8259,.T.);
#11695=ORIENTED_EDGE('',*,*,#8256,.T.);
#11696=ORIENTED_EDGE('',*,*,#8253,.T.);
#11697=ORIENTED_EDGE('',*,*,#8250,.T.);
#11698=ORIENTED_EDGE('',*,*,#8247,.T.);
#11699=ORIENTED_EDGE('',*,*,#8244,.T.);
#11700=ORIENTED_EDGE('',*,*,#8241,.T.);
#11701=ORIENTED_EDGE('',*,*,#8238,.T.);
#11702=ORIENTED_EDGE('',*,*,#8235,.T.);
#11703=ORIENTED_EDGE('',*,*,#8232,.T.);
#11704=ORIENTED_EDGE('',*,*,#8229,.T.);
#11705=ORIENTED_EDGE('',*,*,#8226,.T.);
#11706=ORIENTED_EDGE('',*,*,#8223,.T.);
#11707=ORIENTED_EDGE('',*,*,#8220,.T.);
#11708=ORIENTED_EDGE('',*,*,#8217,.T.);
#11709=ORIENTED_EDGE('',*,*,#8214,.T.);
#11710=ORIENTED_EDGE('',*,*,#8208,.T.);
#11711=ORIENTED_EDGE('',*,*,#8280,.T.);
#11712=ORIENTED_EDGE('',*,*,#8271,.T.);
#11713=ORIENTED_EDGE('',*,*,#8277,.T.);
#11714=ORIENTED_EDGE('',*,*,#8282,.F.);
#11715=ORIENTED_EDGE('',*,*,#8283,.T.);
#11716=ORIENTED_EDGE('',*,*,#8284,.T.);
#11717=ORIENTED_EDGE('',*,*,#8285,.F.);
#11718=ORIENTED_EDGE('',*,*,#8286,.F.);
#11719=ORIENTED_EDGE('',*,*,#8287,.T.);
#11720=ORIENTED_EDGE('',*,*,#8288,.T.);
#11721=ORIENTED_EDGE('',*,*,#8283,.F.);
#11722=ORIENTED_EDGE('',*,*,#8289,.F.);
#11723=ORIENTED_EDGE('',*,*,#8290,.T.);
#11724=ORIENTED_EDGE('',*,*,#8291,.T.);
#11725=ORIENTED_EDGE('',*,*,#8287,.F.);
#11726=ORIENTED_EDGE('',*,*,#8292,.F.);
#11727=ORIENTED_EDGE('',*,*,#8293,.T.);
#11728=ORIENTED_EDGE('',*,*,#8294,.T.);
#11729=ORIENTED_EDGE('',*,*,#8290,.F.);
#11730=ORIENTED_EDGE('',*,*,#8295,.F.);
#11731=ORIENTED_EDGE('',*,*,#8296,.T.);
#11732=ORIENTED_EDGE('',*,*,#8297,.T.);
#11733=ORIENTED_EDGE('',*,*,#8293,.F.);
#11734=ORIENTED_EDGE('',*,*,#8298,.F.);
#11735=ORIENTED_EDGE('',*,*,#8285,.T.);
#11736=ORIENTED_EDGE('',*,*,#8299,.T.);
#11737=ORIENTED_EDGE('',*,*,#8296,.F.);
#11738=ORIENTED_EDGE('',*,*,#8299,.F.);
#11739=ORIENTED_EDGE('',*,*,#8284,.F.);
#11740=ORIENTED_EDGE('',*,*,#8288,.F.);
#11741=ORIENTED_EDGE('',*,*,#8291,.F.);
#11742=ORIENTED_EDGE('',*,*,#8294,.F.);
#11743=ORIENTED_EDGE('',*,*,#8297,.F.);
#11744=ORIENTED_EDGE('',*,*,#8300,.T.);
#11745=ORIENTED_EDGE('',*,*,#8276,.T.);
#11746=ORIENTED_EDGE('',*,*,#8279,.T.);
#11747=ORIENTED_EDGE('',*,*,#8281,.T.);
#11748=ORIENTED_EDGE('',*,*,#8155,.F.);
#11749=ORIENTED_EDGE('',*,*,#8300,.F.);
#11750=ORIENTED_EDGE('',*,*,#8301,.T.);
#11751=ORIENTED_EDGE('',*,*,#8302,.T.);
#11752=ORIENTED_EDGE('',*,*,#8301,.F.);
#11753=ORIENTED_EDGE('',*,*,#8302,.F.);
#11754=ORIENTED_EDGE('',*,*,#8282,.T.);
#11755=ORIENTED_EDGE('',*,*,#8298,.T.);
#11756=ORIENTED_EDGE('',*,*,#8295,.T.);
#11757=ORIENTED_EDGE('',*,*,#8292,.T.);
#11758=ORIENTED_EDGE('',*,*,#8289,.T.);
#11759=ORIENTED_EDGE('',*,*,#8286,.T.);
#11760=ORIENTED_EDGE('',*,*,#8274,.T.);
#13496=PLANE('',#15126);
#13497=PLANE('',#15127);
#13498=PLANE('',#15128);
#13499=PLANE('',#15129);
#13500=PLANE('',#15130);
#13501=PLANE('',#15131);
#13502=PLANE('',#15132);
#13503=PLANE('',#15133);
#13504=PLANE('',#15137);
#13505=PLANE('',#15138);
#13957=ADVANCED_FACE('',(#2711),#1896,.T.);
#13958=ADVANCED_FACE('',(#2712),#1897,.T.);
#13959=ADVANCED_FACE('',(#2713),#1898,.T.);
#13960=ADVANCED_FACE('',(#2714),#1899,.T.);
#13961=ADVANCED_FACE('',(#2715),#1900,.T.);
#13962=ADVANCED_FACE('',(#2716),#1901,.T.);
#13963=ADVANCED_FACE('',(#2717),#1902,.T.);
#13964=ADVANCED_FACE('',(#2718),#1903,.T.);
#13965=ADVANCED_FACE('',(#2719),#1904,.T.);
#13966=ADVANCED_FACE('',(#2720),#1905,.T.);
#13967=ADVANCED_FACE('',(#2721),#1906,.T.);
#13968=ADVANCED_FACE('',(#2722),#1907,.T.);
#13969=ADVANCED_FACE('',(#2723),#1908,.T.);
#13970=ADVANCED_FACE('',(#2724),#1909,.T.);
#13971=ADVANCED_FACE('',(#2725),#1910,.T.);
#13972=ADVANCED_FACE('',(#2726),#1911,.T.);
#13973=ADVANCED_FACE('',(#2727),#1912,.T.);
#13974=ADVANCED_FACE('',(#2728),#1913,.T.);
#13975=ADVANCED_FACE('',(#2729),#1914,.T.);
#13976=ADVANCED_FACE('',(#2730),#1915,.T.);
#13977=ADVANCED_FACE('',(#2731),#1916,.T.);
#13978=ADVANCED_FACE('',(#2732),#1917,.T.);
#13979=ADVANCED_FACE('',(#2733),#1918,.T.);
#13980=ADVANCED_FACE('',(#2734),#1919,.T.);
#13981=ADVANCED_FACE('',(#2735),#1920,.T.);
#13982=ADVANCED_FACE('',(#2736),#1921,.T.);
#13983=ADVANCED_FACE('',(#2737),#1922,.T.);
#13984=ADVANCED_FACE('',(#2738),#1923,.T.);
#13985=ADVANCED_FACE('',(#2739),#1924,.T.);
#13986=ADVANCED_FACE('',(#2740),#1925,.T.);
#13987=ADVANCED_FACE('',(#2741),#1926,.T.);
#13988=ADVANCED_FACE('',(#2742),#1927,.T.);
#13989=ADVANCED_FACE('',(#2743),#1928,.T.);
#13990=ADVANCED_FACE('',(#2744),#1929,.T.);
#13991=ADVANCED_FACE('',(#2745),#1930,.T.);
#13992=ADVANCED_FACE('',(#2746),#1931,.T.);
#13993=ADVANCED_FACE('',(#2747),#1932,.T.);
#13994=ADVANCED_FACE('',(#2748),#1933,.T.);
#13995=ADVANCED_FACE('',(#2749),#255,.T.);
#13996=ADVANCED_FACE('',(#2750),#271,.F.);
#13997=ADVANCED_FACE('',(#2751),#1934,.T.);
#13998=ADVANCED_FACE('',(#2752),#272,.F.);
#13999=ADVANCED_FACE('',(#2753),#1935,.T.);
#14000=ADVANCED_FACE('',(#2754),#13496,.F.);
#14001=ADVANCED_FACE('',(#2755),#13497,.F.);
#14002=ADVANCED_FACE('',(#2756),#13498,.F.);
#14003=ADVANCED_FACE('',(#2757),#13499,.F.);
#14004=ADVANCED_FACE('',(#2758),#13500,.F.);
#14005=ADVANCED_FACE('',(#2759),#13501,.F.);
#14006=ADVANCED_FACE('',(#2760),#13502,.F.);
#14007=ADVANCED_FACE('',(#2761,#2279),#13503,.T.);
#14008=ADVANCED_FACE('',(#2762),#1936,.T.);
#14009=ADVANCED_FACE('',(#2763,#2280),#13504,.F.);
#14010=ADVANCED_FACE('',(#2764),#13505,.T.);
#14316=CLOSED_SHELL('',(#13957,#13958,#13959,#13960,#13961,#13962,#13963,
#13964,#13965,#13966,#13967,#13968,#13969,#13970,#13971,#13972,#13973,#13974,
#13975,#13976,#13977,#13978,#13979,#13980,#13981,#13982,#13983,#13984,#13985,
#13986,#13987,#13988,#13989,#13990,#13991,#13992,#13993,#13994,#13995,#13996,
#13997,#13998,#13999,#14000,#14001,#14002,#14003,#14004,#14005,#14006,#14007,
#14008,#14009,#14010));
#15079=AXIS2_PLACEMENT_3D('',#44031,#17162,#17163);
#15080=AXIS2_PLACEMENT_3D('',#44032,#17164,#17165);
#15081=AXIS2_PLACEMENT_3D('',#44048,#17167,#17168);
#15082=AXIS2_PLACEMENT_3D('',#44059,#17169,#17170);
#15083=AXIS2_PLACEMENT_3D('',#44107,#17172,#17173);
#15084=AXIS2_PLACEMENT_3D('',#44155,#17175,#17176);
#15085=AXIS2_PLACEMENT_3D('',#44209,#17178,#17179);
#15086=AXIS2_PLACEMENT_3D('',#44257,#17181,#17182);
#15087=AXIS2_PLACEMENT_3D('',#44305,#17184,#17185);
#15088=AXIS2_PLACEMENT_3D('',#44359,#17187,#17188);
#15089=AXIS2_PLACEMENT_3D('',#44407,#17190,#17191);
#15090=AXIS2_PLACEMENT_3D('',#44455,#17193,#17194);
#15091=AXIS2_PLACEMENT_3D('',#44503,#17196,#17197);
#15092=AXIS2_PLACEMENT_3D('',#44557,#17199,#17200);
#15093=AXIS2_PLACEMENT_3D('',#44605,#17202,#17203);
#15094=AXIS2_PLACEMENT_3D('',#44653,#17205,#17206);
#15095=AXIS2_PLACEMENT_3D('',#44707,#17208,#17209);
#15096=AXIS2_PLACEMENT_3D('',#44755,#17211,#17212);
#15097=AXIS2_PLACEMENT_3D('',#44803,#17214,#17215);
#15098=AXIS2_PLACEMENT_3D('',#44857,#17217,#17218);
#15099=AXIS2_PLACEMENT_3D('',#44905,#17220,#17221);
#15100=AXIS2_PLACEMENT_3D('',#44953,#17223,#17224);
#15101=AXIS2_PLACEMENT_3D('',#44970,#17226,#17227);
#15102=AXIS2_PLACEMENT_3D('',#44980,#17228,#17229);
#15103=AXIS2_PLACEMENT_3D('',#45005,#17231,#17232);
#15104=AXIS2_PLACEMENT_3D('',#45029,#17234,#17235);
#15105=AXIS2_PLACEMENT_3D('',#45054,#17237,#17238);
#15106=AXIS2_PLACEMENT_3D('',#45079,#17240,#17241);
#15107=AXIS2_PLACEMENT_3D('',#45103,#17243,#17244);
#15108=AXIS2_PLACEMENT_3D('',#45128,#17246,#17247);
#15109=AXIS2_PLACEMENT_3D('',#45153,#17249,#17250);
#15110=AXIS2_PLACEMENT_3D('',#45177,#17252,#17253);
#15111=AXIS2_PLACEMENT_3D('',#45202,#17255,#17256);
#15112=AXIS2_PLACEMENT_3D('',#45227,#17258,#17259);
#15113=AXIS2_PLACEMENT_3D('',#45251,#17261,#17262);
#15114=AXIS2_PLACEMENT_3D('',#45275,#17264,#17265);
#15115=AXIS2_PLACEMENT_3D('',#45300,#17267,#17268);
#15116=AXIS2_PLACEMENT_3D('',#45325,#17270,#17271);
#15117=AXIS2_PLACEMENT_3D('',#45349,#17273,#17274);
#15118=AXIS2_PLACEMENT_3D('',#45374,#17276,#17277);
#15119=AXIS2_PLACEMENT_3D('',#45399,#17279,#17280);
#15120=AXIS2_PLACEMENT_3D('',#45423,#17282,#17283);
#15121=AXIS2_PLACEMENT_3D('',#45744,#17284,#17285);
#15122=AXIS2_PLACEMENT_3D('',#45784,#17287,#17288);
#15123=AXIS2_PLACEMENT_3D('',#46433,#17289,#17290);
#15124=AXIS2_PLACEMENT_3D('',#46444,#17291,#17292);
#15125=AXIS2_PLACEMENT_3D('',#47097,#17293,#17294);
#15126=AXIS2_PLACEMENT_3D('',#47098,#17295,#17296);
#15127=AXIS2_PLACEMENT_3D('',#47107,#17301,#17302);
#15128=AXIS2_PLACEMENT_3D('',#47113,#17306,#17307);
#15129=AXIS2_PLACEMENT_3D('',#47119,#17311,#17312);
#15130=AXIS2_PLACEMENT_3D('',#47125,#17316,#17317);
#15131=AXIS2_PLACEMENT_3D('',#47131,#17321,#17322);
#15132=AXIS2_PLACEMENT_3D('',#47134,#17325,#17326);
#15133=AXIS2_PLACEMENT_3D('',#47135,#17327,#17328);
#15134=AXIS2_PLACEMENT_3D('',#47137,#17329,#17330);
#15135=AXIS2_PLACEMENT_3D('',#47138,#17331,#17332);
#15136=AXIS2_PLACEMENT_3D('',#47141,#17334,#17335);
#15137=AXIS2_PLACEMENT_3D('',#47142,#17336,#17337);
#15138=AXIS2_PLACEMENT_3D('',#47143,#17338,#17339);
#17162=DIRECTION('axis',(0.,0.,1.));
#17163=DIRECTION('refdir',(1.,0.,0.));
#17164=DIRECTION('center_axis',(0.,0.,1.));
#17165=DIRECTION('ref_axis',(1.,0.,0.));
#17166=DIRECTION('',(0.,0.,-1.));
#17167=DIRECTION('center_axis',(0.,0.,-1.));
#17168=DIRECTION('ref_axis',(1.,0.,0.));
#17169=DIRECTION('center_axis',(0.,0.,1.));
#17170=DIRECTION('ref_axis',(1.,0.,0.));
#17171=DIRECTION('',(0.,0.,-1.));
#17172=DIRECTION('center_axis',(0.,0.,1.));
#17173=DIRECTION('ref_axis',(1.,0.,0.));
#17174=DIRECTION('',(0.,0.,-1.));
#17175=DIRECTION('center_axis',(0.,0.,1.));
#17176=DIRECTION('ref_axis',(1.,0.,0.));
#17177=DIRECTION('',(0.,0.,-1.));
#17178=DIRECTION('center_axis',(0.,0.,1.));
#17179=DIRECTION('ref_axis',(1.,0.,0.));
#17180=DIRECTION('',(0.,0.,-1.));
#17181=DIRECTION('center_axis',(0.,0.,1.));
#17182=DIRECTION('ref_axis',(1.,0.,0.));
#17183=DIRECTION('',(0.,0.,-1.));
#17184=DIRECTION('center_axis',(0.,0.,1.));
#17185=DIRECTION('ref_axis',(1.,0.,0.));
#17186=DIRECTION('',(0.,0.,-1.));
#17187=DIRECTION('center_axis',(0.,0.,1.));
#17188=DIRECTION('ref_axis',(1.,0.,0.));
#17189=DIRECTION('',(0.,0.,-1.));
#17190=DIRECTION('center_axis',(0.,0.,1.));
#17191=DIRECTION('ref_axis',(1.,0.,0.));
#17192=DIRECTION('',(0.,0.,-1.));
#17193=DIRECTION('center_axis',(0.,0.,1.));
#17194=DIRECTION('ref_axis',(1.,0.,0.));
#17195=DIRECTION('',(0.,0.,-1.));
#17196=DIRECTION('center_axis',(0.,0.,1.));
#17197=DIRECTION('ref_axis',(1.,0.,0.));
#17198=DIRECTION('',(0.,0.,-1.));
#17199=DIRECTION('center_axis',(0.,0.,1.));
#17200=DIRECTION('ref_axis',(1.,0.,0.));
#17201=DIRECTION('',(0.,0.,-1.));
#17202=DIRECTION('center_axis',(0.,0.,1.));
#17203=DIRECTION('ref_axis',(1.,0.,0.));
#17204=DIRECTION('',(0.,0.,-1.));
#17205=DIRECTION('center_axis',(0.,0.,1.));
#17206=DIRECTION('ref_axis',(1.,0.,0.));
#17207=DIRECTION('',(0.,0.,-1.));
#17208=DIRECTION('center_axis',(0.,0.,1.));
#17209=DIRECTION('ref_axis',(1.,0.,0.));
#17210=DIRECTION('',(0.,0.,-1.));
#17211=DIRECTION('center_axis',(0.,0.,1.));
#17212=DIRECTION('ref_axis',(1.,0.,0.));
#17213=DIRECTION('',(0.,0.,-1.));
#17214=DIRECTION('center_axis',(0.,0.,1.));
#17215=DIRECTION('ref_axis',(1.,0.,0.));
#17216=DIRECTION('',(0.,0.,-1.));
#17217=DIRECTION('center_axis',(0.,0.,1.));
#17218=DIRECTION('ref_axis',(1.,0.,0.));
#17219=DIRECTION('',(0.,0.,-1.));
#17220=DIRECTION('center_axis',(0.,0.,1.));
#17221=DIRECTION('ref_axis',(1.,0.,0.));
#17222=DIRECTION('',(0.,0.,-1.));
#17223=DIRECTION('center_axis',(0.,0.,1.));
#17224=DIRECTION('ref_axis',(0.997281310794726,-0.0736884464455154,0.));
#17225=DIRECTION('',(0.,0.,1.));
#17226=DIRECTION('center_axis',(0.,0.,-1.));
#17227=DIRECTION('ref_axis',(1.,1.00674340327557E-13,0.));
#17228=DIRECTION('center_axis',(0.,0.,1.));
#17229=DIRECTION('ref_axis',(1.,1.00674340327557E-13,0.));
#17230=DIRECTION('',(0.,0.,1.));
#17231=DIRECTION('center_axis',(0.,0.,1.));
#17232=DIRECTION('ref_axis',(1.,1.00674340327557E-13,0.));
#17233=DIRECTION('',(0.,0.,1.));
#17234=DIRECTION('center_axis',(0.,0.,1.));
#17235=DIRECTION('ref_axis',(1.,1.00674340327557E-13,0.));
#17236=DIRECTION('',(0.,0.,1.));
#17237=DIRECTION('center_axis',(0.,0.,1.));
#17238=DIRECTION('ref_axis',(1.,1.00674340327557E-13,0.));
#17239=DIRECTION('',(0.,0.,1.));
#17240=DIRECTION('center_axis',(0.,0.,1.));
#17241=DIRECTION('ref_axis',(1.,1.00674340327557E-13,0.));
#17242=DIRECTION('',(0.,0.,1.));
#17243=DIRECTION('center_axis',(0.,0.,1.));
#17244=DIRECTION('ref_axis',(1.,1.00674340327557E-13,0.));
#17245=DIRECTION('',(0.,0.,1.));
#17246=DIRECTION('center_axis',(0.,0.,1.));
#17247=DIRECTION('ref_axis',(1.,1.00674340327557E-13,0.));
#17248=DIRECTION('',(0.,0.,1.));
#17249=DIRECTION('center_axis',(0.,0.,1.));
#17250=DIRECTION('ref_axis',(1.,1.00674340327557E-13,0.));
#17251=DIRECTION('',(0.,0.,1.));
#17252=DIRECTION('center_axis',(0.,0.,1.));
#17253=DIRECTION('ref_axis',(1.,1.00674340327557E-13,0.));
#17254=DIRECTION('',(0.,0.,1.));
#17255=DIRECTION('center_axis',(0.,0.,1.));
#17256=DIRECTION('ref_axis',(1.,1.00674340327557E-13,0.));
#17257=DIRECTION('',(0.,0.,1.));
#17258=DIRECTION('center_axis',(0.,0.,1.));
#17259=DIRECTION('ref_axis',(1.,1.00674340327557E-13,0.));
#17260=DIRECTION('',(0.,0.,1.));
#17261=DIRECTION('center_axis',(0.,0.,1.));
#17262=DIRECTION('ref_axis',(1.,1.00674340327557E-13,0.));
#17263=DIRECTION('',(0.,0.,1.));
#17264=DIRECTION('center_axis',(0.,0.,1.));
#17265=DIRECTION('ref_axis',(1.,1.00674340327557E-13,0.));
#17266=DIRECTION('',(0.,0.,1.));
#17267=DIRECTION('center_axis',(0.,0.,1.));
#17268=DIRECTION('ref_axis',(1.,1.00674340327557E-13,0.));
#17269=DIRECTION('',(0.,0.,1.));
#17270=DIRECTION('center_axis',(0.,0.,1.));
#17271=DIRECTION('ref_axis',(1.,1.00674340327557E-13,0.));
#17272=DIRECTION('',(0.,0.,1.));
#17273=DIRECTION('center_axis',(0.,0.,1.));
#17274=DIRECTION('ref_axis',(1.,1.00674340327557E-13,0.));
#17275=DIRECTION('',(0.,0.,1.));
#17276=DIRECTION('center_axis',(0.,0.,1.));
#17277=DIRECTION('ref_axis',(1.,1.00674340327557E-13,0.));
#17278=DIRECTION('',(0.,0.,1.));
#17279=DIRECTION('center_axis',(0.,0.,1.));
#17280=DIRECTION('ref_axis',(1.,1.00674340327557E-13,0.));
#17281=DIRECTION('',(0.,0.,1.));
#17282=DIRECTION('center_axis',(0.,0.,-1.));
#17283=DIRECTION('ref_axis',(1.,0.,0.));
#17284=DIRECTION('center_axis',(0.,0.,-1.));
#17285=DIRECTION('ref_axis',(1.,0.,0.));
#17286=DIRECTION('',(0.707106781186547,8.65956056235493E-17,0.707106781186548));
#17287=DIRECTION('center_axis',(0.,0.,1.));
#17288=DIRECTION('ref_axis',(1.,0.,0.));
#17289=DIRECTION('center_axis',(0.,0.,1.));
#17290=DIRECTION('ref_axis',(1.,1.00674340327557E-13,0.));
#17291=DIRECTION('center_axis',(0.,0.,-1.));
#17292=DIRECTION('ref_axis',(1.,1.00674340327557E-13,0.));
#17293=DIRECTION('center_axis',(0.,0.,1.));
#17294=DIRECTION('ref_axis',(1.,0.,0.));
#17295=DIRECTION('center_axis',(-2.40370335797945E-16,-1.,0.));
#17296=DIRECTION('ref_axis',(1.,-2.40370335797945E-16,0.));
#17297=DIRECTION('',(1.,-2.40370335797945E-16,0.));
#17298=DIRECTION('',(0.,0.,1.));
#17299=DIRECTION('',(1.,-2.40370335797945E-16,0.));
#17300=DIRECTION('',(0.,0.,1.));
#17301=DIRECTION('center_axis',(-0.866025403784439,-0.5,0.));
#17302=DIRECTION('ref_axis',(0.5,-0.866025403784439,0.));
#17303=DIRECTION('',(0.5,-0.866025403784439,0.));
#17304=DIRECTION('',(0.,0.,1.));
#17305=DIRECTION('',(0.5,-0.866025403784439,0.));
#17306=DIRECTION('center_axis',(-0.866025403784439,0.5,0.));
#17307=DIRECTION('ref_axis',(-0.5,-0.866025403784439,0.));
#17308=DIRECTION('',(-0.5,-0.866025403784439,0.));
#17309=DIRECTION('',(0.,0.,1.));
#17310=DIRECTION('',(-0.5,-0.866025403784439,0.));
#17311=DIRECTION('center_axis',(1.20185167898973E-16,1.,0.));
#17312=DIRECTION('ref_axis',(-1.,1.20185167898973E-16,0.));
#17313=DIRECTION('',(-1.,1.20185167898973E-16,0.));
#17314=DIRECTION('',(0.,0.,1.));
#17315=DIRECTION('',(-1.,1.20185167898973E-16,0.));
#17316=DIRECTION('center_axis',(0.866025403784439,0.5,0.));
#17317=DIRECTION('ref_axis',(-0.5,0.866025403784439,0.));
#17318=DIRECTION('',(-0.5,0.866025403784439,0.));
#17319=DIRECTION('',(0.,0.,1.));
#17320=DIRECTION('',(-0.5,0.866025403784439,0.));
#17321=DIRECTION('center_axis',(0.866025403784439,-0.5,0.));
#17322=DIRECTION('ref_axis',(0.5,0.866025403784439,0.));
#17323=DIRECTION('',(0.5,0.866025403784439,0.));
#17324=DIRECTION('',(0.5,0.866025403784439,0.));
#17325=DIRECTION('center_axis',(0.,0.,1.));
#17326=DIRECTION('ref_axis',(1.,0.,0.));
#17327=DIRECTION('center_axis',(0.,0.,1.));
#17328=DIRECTION('ref_axis',(1.,0.,0.));
#17329=DIRECTION('center_axis',(0.,0.,1.));
#17330=DIRECTION('ref_axis',(1.,0.,0.));
#17331=DIRECTION('center_axis',(0.,0.,1.));
#17332=DIRECTION('ref_axis',(1.,0.,0.));
#17333=DIRECTION('',(0.,0.,-1.));
#17334=DIRECTION('center_axis',(0.,0.,1.));
#17335=DIRECTION('ref_axis',(1.,0.,0.));
#17336=DIRECTION('center_axis',(0.,0.,1.));
#17337=DIRECTION('ref_axis',(1.,0.,0.));
#17338=DIRECTION('center_axis',(0.,0.,1.));
#17339=DIRECTION('ref_axis',(1.,0.,0.));
#44031=CARTESIAN_POINT('',(0.,0.,0.));
#44032=CARTESIAN_POINT('Origin',(0.,0.,0.));
#44033=CARTESIAN_POINT('',(-4.94697864382552,0.00278476180115707,0.322320454656892));
#44034=CARTESIAN_POINT('',(-4.94423617559418,0.00148231834052548,0.177679545343088));
#44035=CARTESIAN_POINT('',(-4.942,-6.05220448138622E-16,0.));
#44036=CARTESIAN_POINT('',(2.16917135428609,4.440502182833,0.));
#44037=CARTESIAN_POINT('Ctrl Pts',(-4.94697864382552,0.00278476180115707,
0.322320454656892));
#44038=CARTESIAN_POINT('Ctrl Pts',(-4.94837427497074,0.191084575140575,
0.316237515399425));
#44039=CARTESIAN_POINT('Ctrl Pts',(-4.93857638297692,0.379246871981659,
0.310154576141959));
#44040=CARTESIAN_POINT('Ctrl Pts',(-4.91710439111276,0.566072733558586,
0.304071636884492));
#44041=CARTESIAN_POINT('Ctrl Pts',(-4.73085624282078,2.18660104746097,0.251308196024277));
#44042=CARTESIAN_POINT('Ctrl Pts',(-3.66626808942587,3.70657817799375,0.198544755164062));
#44043=CARTESIAN_POINT('Ctrl Pts',(-2.20523483873771,4.43248249176653,0.145781314303847));
#44044=CARTESIAN_POINT('Ctrl Pts',(-0.85966080708188,5.10102168731156,0.097187542869231));
#44045=CARTESIAN_POINT('Ctrl Pts',(0.822175421307706,5.09603339682298,0.0485937714346156));
#44046=CARTESIAN_POINT('Ctrl Pts',(2.17571852337094,4.44456444733847,3.90312782094782E-17));
#44047=CARTESIAN_POINT('',(-2.16917135428615,4.44050218283297,0.));
#44048=CARTESIAN_POINT('Origin',(0.,0.,0.));
#44049=CARTESIAN_POINT('Ctrl Pts',(-2.16917135428615,4.44050218283297,1.94289029309402E-15));
#44050=CARTESIAN_POINT('Ctrl Pts',(-2.90569614448719,4.08071213863431,0.0263982667373533));
#44051=CARTESIAN_POINT('Ctrl Pts',(-3.54537901519776,3.53418981917855,0.0527965334747045));
#44052=CARTESIAN_POINT('Ctrl Pts',(-4.02261725675323,2.86672087533204,0.0791948002120558));
#44053=CARTESIAN_POINT('Ctrl Pts',(-4.49985549830871,2.1992519314855,0.105593066949408));
#44054=CARTESIAN_POINT('Ctrl Pts',(-4.81464911070909,1.41083636324821,0.13199133368676));
#44055=CARTESIAN_POINT('Ctrl Pts',(-4.91161341297729,0.598206782831744,
0.158389600424112));
#44056=CARTESIAN_POINT('Ctrl Pts',(-4.93523158039298,0.400269799547603,
0.164819582063771));
#44057=CARTESIAN_POINT('Ctrl Pts',(-4.94592610470609,0.200896217803435,
0.171249563703429));
#44058=CARTESIAN_POINT('Ctrl Pts',(-4.94423617559418,0.00148231834052548,
0.177679545343088));
#44059=CARTESIAN_POINT('Origin',(0.,0.,0.));
#44060=CARTESIAN_POINT('',(-4.93459216488855,0.00173983556611496,1.32232045465689));
#44061=CARTESIAN_POINT('',(-4.93449003509191,0.0016461999684793,1.17767954534309));
#44062=CARTESIAN_POINT('',(-4.942,-6.05220448138622E-16,0.));
#44063=CARTESIAN_POINT('Ctrl Pts',(-4.93459216488855,0.00173983556611496,
1.32232045465689));
#44064=CARTESIAN_POINT('Ctrl Pts',(-4.93685941200801,0.71330292763056,1.29948482722738));
#44065=CARTESIAN_POINT('Ctrl Pts',(-4.79300629668486,1.42399221307712,1.27664919979787));
#44066=CARTESIAN_POINT('Ctrl Pts',(-4.49846232996172,2.06549179869028,1.25381357236836));
#44067=CARTESIAN_POINT('Ctrl Pts',(-3.81789626200921,3.5477250130758,1.20105013150815));
#44068=CARTESIAN_POINT('Ctrl Pts',(-2.33282804601649,4.66057109067704,1.14828669064793));
#44069=CARTESIAN_POINT('Ctrl Pts',(-0.719110050159326,4.89750101325702,
1.09552324978772));
#44070=CARTESIAN_POINT('Ctrl Pts',(0.89460794569784,5.13443093583701,1.0427598089275));
#44071=CARTESIAN_POINT('Ctrl Pts',(2.63697572141945,4.49544470339575,0.989996368067287));
#44072=CARTESIAN_POINT('Ctrl Pts',(3.71488022775187,3.27143294682148,0.937232927207072));
#44073=CARTESIAN_POINT('Ctrl Pts',(4.79278473408429,2.04742119024721,0.884469486346857));
#44074=CARTESIAN_POINT('Ctrl Pts',(5.20622597102753,0.238383909539938,0.831706045486642));
#44075=CARTESIAN_POINT('Ctrl Pts',(4.76722694025552,-1.33245018266074,0.778942604626427));
#44076=CARTESIAN_POINT('Ctrl Pts',(4.32822790948351,-2.90328427486142,0.726179163766212));
#44077=CARTESIAN_POINT('Ctrl Pts',(3.03678861099627,-4.2359151785555,0.673415722905997));
#44078=CARTESIAN_POINT('Ctrl Pts',(1.48031593870399,-4.72357537917557,0.620652282045782));
#44079=CARTESIAN_POINT('Ctrl Pts',(-0.0761567335882804,-5.21123557979564,
0.567888841185567));
#44080=CARTESIAN_POINT('Ctrl Pts',(-1.89766277968558,-4.8539250773417,0.515125400325352));
#44081=CARTESIAN_POINT('Ctrl Pts',(-3.1544617311397,-3.81473007747874,0.462361959465137));
#44082=CARTESIAN_POINT('Ctrl Pts',(-4.26636809113457,-2.89534076044788,
0.415681457862388));
#44083=CARTESIAN_POINT('Ctrl Pts',(-4.93626856451128,-1.44222880258692,
0.36900095625964));
#44084=CARTESIAN_POINT('Ctrl Pts',(-4.94697864382552,0.00278476180115707,
0.322320454656892));
#44085=CARTESIAN_POINT('Ctrl Pts',(-4.94423617559418,0.00148231834052548,
0.177679545343088));
#44086=CARTESIAN_POINT('Ctrl Pts',(-4.93205010879707,-1.4364898912607,0.224046097178133));
#44087=CARTESIAN_POINT('Ctrl Pts',(-4.27589205183812,-2.87655855846778,
0.270412649013179));
#44088=CARTESIAN_POINT('Ctrl Pts',(-3.17793668728658,-3.7951739429827,0.316779200848224));
#44089=CARTESIAN_POINT('Ctrl Pts',(-1.92771999305178,-4.8411802984146,0.369575734322928));
#44090=CARTESIAN_POINT('Ctrl Pts',(-0.104675240574504,-5.21107779972881,
0.422372267797632));
#44091=CARTESIAN_POINT('Ctrl Pts',(1.45583984202071,-4.73188592100135,0.475168801272336));
#44092=CARTESIAN_POINT('Ctrl Pts',(3.01635492461593,-4.25269404227389,0.527965334747039));
#44093=CARTESIAN_POINT('Ctrl Pts',(4.31434033732908,-2.92441278350478,0.580761868221743));
#44094=CARTESIAN_POINT('Ctrl Pts',(4.76068268187915,-1.35442587380419,0.633558401696447));
#44095=CARTESIAN_POINT('Ctrl Pts',(5.20702502642923,0.215561035896397,0.686354935171151));
#44096=CARTESIAN_POINT('Ctrl Pts',(4.80172430281623,2.02725359652845,0.739151468645856));
#44097=CARTESIAN_POINT('Ctrl Pts',(3.72825744985575,3.25624139915875,0.791948002120559));
#44098=CARTESIAN_POINT('Ctrl Pts',(2.65479059689527,4.48522920178905,0.844744535595263));
#44099=CARTESIAN_POINT('Ctrl Pts',(0.9131576145873,5.13151224641759,0.897541069069967));
#44100=CARTESIAN_POINT('Ctrl Pts',(-0.702426516917608,4.90003317713487,
0.950337602544671));
#44101=CARTESIAN_POINT('Ctrl Pts',(-2.31801064842252,4.66855410785214,1.00313413601937));
#44102=CARTESIAN_POINT('Ctrl Pts',(-3.80754592912437,3.55931292465815,1.05593066949408));
#44103=CARTESIAN_POINT('Ctrl Pts',(-4.49264215512641,2.07804350324001,1.10872720296878));
#44104=CARTESIAN_POINT('Ctrl Pts',(-4.79088768013657,1.43319689701884,1.13171131709355));
#44105=CARTESIAN_POINT('Ctrl Pts',(-4.93667954029292,0.71784517544428,1.15469543121832));
#44106=CARTESIAN_POINT('Ctrl Pts',(-4.93449003509191,0.0016461999684793,
1.17767954534309));
#44107=CARTESIAN_POINT('Origin',(0.,0.,0.));
#44108=CARTESIAN_POINT('',(-4.9411817412373,-0.00444225127051057,2.32232045465689));
#44109=CARTESIAN_POINT('',(-4.94111085608669,-0.00445469630641156,2.17767954534309));
#44110=CARTESIAN_POINT('',(-4.942,-6.05220448138622E-16,0.));
#44111=CARTESIAN_POINT('Ctrl Pts',(-4.9411817412373,-0.00444225127051057,
2.32232045465689));
#44112=CARTESIAN_POINT('Ctrl Pts',(-4.93017412883888,1.22499555075574,2.28273213905534));
#44113=CARTESIAN_POINT('Ctrl Pts',(-4.46534239547945,2.46186324317617,2.24314382345379));
#44114=CARTESIAN_POINT('Ctrl Pts',(-3.63458175569093,3.36040592443024,2.20355550785224));
#44115=CARTESIAN_POINT('Ctrl Pts',(-2.52734116663296,4.55798664748753,2.15079206699202));
#44116=CARTESIAN_POINT('Ctrl Pts',(-0.770077330248272,5.15457871251208,
2.0980286261318));
#44117=CARTESIAN_POINT('Ctrl Pts',(0.837419729043101,4.87865187630481,2.04526518527159));
#44118=CARTESIAN_POINT('Ctrl Pts',(2.44491678833447,4.60272504009754,1.99250174441137));
#44119=CARTESIAN_POINT('Ctrl Pts',(3.90264707053253,3.45427930265847,1.93973830355116));
#44120=CARTESIAN_POINT('Ctrl Pts',(4.54714538443732,1.95601310903264,1.88697486269094));
#44121=CARTESIAN_POINT('Ctrl Pts',(5.19164369834212,0.45774691540682,1.83421142183073));
#44122=CARTESIAN_POINT('Ctrl Pts',(5.02291004395365,-1.39033973440576,1.78144798097051));
#44123=CARTESIAN_POINT('Ctrl Pts',(4.11774488359116,-2.74712173291455,1.7286845401103));
#44124=CARTESIAN_POINT('Ctrl Pts',(3.21257972322867,-4.10390373142335,1.67592109925008));
#44125=CARTESIAN_POINT('Ctrl Pts',(1.57098305689217,-4.96938107862837,1.62315765838987));
#44126=CARTESIAN_POINT('Ctrl Pts',(-0.0599057143251611,-4.94964036759779,
1.57039421752965));
#44127=CARTESIAN_POINT('Ctrl Pts',(-1.69079448554249,-4.92989965656721,
1.51763077666944));
#44128=CARTESIAN_POINT('Ctrl Pts',(-3.31097536164064,-4.02494088730103,
1.46486733580922));
#44129=CARTESIAN_POINT('Ctrl Pts',(-4.18303383973357,-2.64665132708304,
1.41210389494901));
#44130=CARTESIAN_POINT('Ctrl Pts',(-4.67767185058986,-1.86487530680844,
1.3821760815183));
#44131=CARTESIAN_POINT('Ctrl Pts',(-4.9316207664016,-0.930817306961143,
1.3522482680876));
#44132=CARTESIAN_POINT('Ctrl Pts',(-4.93459216488855,0.00173983556611496,
1.32232045465689));
#44133=CARTESIAN_POINT('Ctrl Pts',(-4.93449003509191,0.0016461999684793,
1.17767954534309));
#44134=CARTESIAN_POINT('Ctrl Pts',(-4.9316500541004,-0.927326919420464,
1.20749196469302));
#44135=CARTESIAN_POINT('Ctrl Pts',(-4.67984069516382,-1.85772549042789,
1.23730438404296));
#44136=CARTESIAN_POINT('Ctrl Pts',(-4.18882172046978,-2.63753729589231,
1.26711680339289));
#44137=CARTESIAN_POINT('Ctrl Pts',(-3.31924788850886,-4.01855101396421,
1.3199133368676));
#44138=CARTESIAN_POINT('Ctrl Pts',(-1.69944305328478,-4.92728079046571,
1.3727098703423));
#44139=CARTESIAN_POINT('Ctrl Pts',(-0.0675730918879967,-4.94957507244757,
1.42550640381701));
#44140=CARTESIAN_POINT('Ctrl Pts',(1.56429686950879,-4.97186935442943,1.47830293729171));
#44141=CARTESIAN_POINT('Ctrl Pts',(3.20823195707828,-4.10772814189165,1.53109947076641));
#44142=CARTESIAN_POINT('Ctrl Pts',(4.11520771620268,-2.7509467593832,1.58389600424112));
#44143=CARTESIAN_POINT('Ctrl Pts',(5.02218347532707,-1.39416537687474,1.63669253771582));
#44144=CARTESIAN_POINT('Ctrl Pts',(5.19219990600637,0.455256175604397,1.68948907119053));
#44145=CARTESIAN_POINT('Ctrl Pts',(4.54776321553941,1.95463753781542,1.74228560466523));
#44146=CARTESIAN_POINT('Ctrl Pts',(3.90332652507246,3.45401890002643,1.79508213813993));
#44147=CARTESIAN_POINT('Ctrl Pts',(2.44443671345924,4.60336007196933,1.84787867161464));
#44148=CARTESIAN_POINT('Ctrl Pts',(0.835860696338233,4.878943390804,1.90067520508934));
#44149=CARTESIAN_POINT('Ctrl Pts',(-0.772715320782773,5.15452670963867,
1.95347173856405));
#44150=CARTESIAN_POINT('Ctrl Pts',(-2.53097754341157,4.55635217536511,2.00626827203875));
#44151=CARTESIAN_POINT('Ctrl Pts',(-3.63776731536415,3.3569886406566,2.05906480551345));
#44152=CARTESIAN_POINT('Ctrl Pts',(-4.4666195916167,2.45880976243686,2.09860305212333));
#44153=CARTESIAN_POINT('Ctrl Pts',(-4.93011266597958,1.22347167947137,2.13814129873321));
#44154=CARTESIAN_POINT('Ctrl Pts',(-4.94111085608669,-0.00445469630641156,
2.17767954534309));
#44155=CARTESIAN_POINT('Origin',(0.,0.,0.));
#44156=CARTESIAN_POINT('',(-4.94903399601206,0.00195803074323202,3.32232045465689));
#44157=CARTESIAN_POINT('',(-4.94919334226918,0.00181972978148383,3.17767954534309));
#44158=CARTESIAN_POINT('',(-4.942,-6.05220448138622E-16,0.));
#44159=CARTESIAN_POINT('Ctrl Pts',(-4.94903399601206,0.00195803074323202,
3.32232045465689));
#44160=CARTESIAN_POINT('Ctrl Pts',(-4.949593728633,0.112604296590692,3.31874289174351));
#44161=CARTESIAN_POINT('Ctrl Pts',(-4.94620248790589,0.223215646212416,
3.31516532883013));
#44162=CARTESIAN_POINT('Ctrl Pts',(-4.93875055399973,0.333552745210412,
3.31158776591675));
#44163=CARTESIAN_POINT('Ctrl Pts',(-4.82884621871006,1.96085186995656,3.25882432505653));
#44164=CARTESIAN_POINT('Ctrl Pts',(-3.83567522857514,3.52849703407851,3.20606088419632));
#44165=CARTESIAN_POINT('Ctrl Pts',(-2.41126381713223,4.32299910001284,3.15329744333611));
#44166=CARTESIAN_POINT('Ctrl Pts',(-0.986852405689299,5.11750116594718,
3.10053400247589));
#44167=CARTESIAN_POINT('Ctrl Pts',(0.868799427061646,5.13886013369387,3.04777056161567));
#44168=CARTESIAN_POINT('Ctrl Pts',(2.31112083361857,4.37735478907724,2.99500712075546));
#44169=CARTESIAN_POINT('Ctrl Pts',(3.75344224017549,3.61584944446061,2.94224367989524));
#44170=CARTESIAN_POINT('Ctrl Pts',(4.78243322053839,2.07147978748068,2.88948023903503));
#44171=CARTESIAN_POINT('Ctrl Pts',(4.92976460259391,0.447141508486386,2.83671679817481));
#44172=CARTESIAN_POINT('Ctrl Pts',(5.07709598464943,-1.17719677050791,2.7839533573146));
#44173=CARTESIAN_POINT('Ctrl Pts',(4.34276776839756,-2.88150367151656,2.73118991645438));
#44174=CARTESIAN_POINT('Ctrl Pts',(3.06099802257449,-3.89009065317052,2.67842647559417));
#44175=CARTESIAN_POINT('Ctrl Pts',(1.77922827675142,-4.89867763482448,2.62566303473395));
#44176=CARTESIAN_POINT('Ctrl Pts',(-0.0499829986428499,-5.21154469712375,
2.57289959387374));
#44177=CARTESIAN_POINT('Ctrl Pts',(-1.59409909536903,-4.68629519517074,
2.52013615301352));
#44178=CARTESIAN_POINT('Ctrl Pts',(-3.13821519209522,-4.16104569321773,
2.46737271215331));
#44179=CARTESIAN_POINT('Ctrl Pts',(-4.39723611015331,-2.79767962701243,
2.41460927129309));
#44180=CARTESIAN_POINT('Ctrl Pts',(-4.79813789831673,-1.21671190336476,
2.36184583043288));
#44181=CARTESIAN_POINT('Ctrl Pts',(-4.89824378961878,-0.821941443944892,
2.34867070517422));
#44182=CARTESIAN_POINT('Ctrl Pts',(-4.94484511185421,-0.413603307842339,
2.33549557991555));
#44183=CARTESIAN_POINT('Ctrl Pts',(-4.9411817412373,-0.00444225127051057,
2.32232045465689));
#44184=CARTESIAN_POINT('Ctrl Pts',(-4.94111085608669,-0.00445469630641156,
2.17767954534309));
#44185=CARTESIAN_POINT('Ctrl Pts',(-4.94479885876604,-0.416212969241057,
2.19093783220791));
#44186=CARTESIAN_POINT('Ctrl Pts',(-4.89760609031032,-0.8271378330251,2.20419611907274));
#44187=CARTESIAN_POINT('Ctrl Pts',(-4.79624701605789,-1.22423691020985,
2.21745440593756));
#44188=CARTESIAN_POINT('Ctrl Pts',(-4.39261962352267,-2.80554639122433,
2.27025093941227));
#44189=CARTESIAN_POINT('Ctrl Pts',(-3.13004751717586,-4.16761281810985,
2.32304747288697));
#44190=CARTESIAN_POINT('Ctrl Pts',(-1.58383298272376,-4.68979872834667,
2.37584400636168));
#44191=CARTESIAN_POINT('Ctrl Pts',(-0.0376184482716604,-5.21198463858349,
2.42864053983638));
#44192=CARTESIAN_POINT('Ctrl Pts',(1.79223851428572,-4.89429003217164,2.48143707331108));
#44193=CARTESIAN_POINT('Ctrl Pts',(3.07195081718679,-3.88147571791622,2.53423360678579));
#44194=CARTESIAN_POINT('Ctrl Pts',(4.35166312008787,-2.86866140366079,2.58703014026049));
#44195=CARTESIAN_POINT('Ctrl Pts',(5.08123076333263,-1.1607273815618,2.6398266737352));
#44196=CARTESIAN_POINT('Ctrl Pts',(4.92822027622649,0.464093861851888,2.6926232072099));
#44197=CARTESIAN_POINT('Ctrl Pts',(4.77520978912036,2.08891510526557,2.7454197406846));
#44198=CARTESIAN_POINT('Ctrl Pts',(3.73962117166333,3.63062356999396,2.79821627415931));
#44199=CARTESIAN_POINT('Ctrl Pts',(2.29332840687238,4.38672799125455,2.85101280763401));
#44200=CARTESIAN_POINT('Ctrl Pts',(0.847035642081437,5.14283241251514,2.90380934110872));
#44201=CARTESIAN_POINT('Ctrl Pts',(-1.00996127004341,5.11333279030795,2.95660587458342));
#44202=CARTESIAN_POINT('Ctrl Pts',(-2.4315078970232,4.31167097450304,3.00940240805812));
#44203=CARTESIAN_POINT('Ctrl Pts',(-3.853054524003,3.51000915869812,3.06219894153283));
#44204=CARTESIAN_POINT('Ctrl Pts',(-4.83915086583772,1.93618514929547,3.11499547500753));
#44205=CARTESIAN_POINT('Ctrl Pts',(-4.94047465700387,0.307323593631802,
3.16779200848224));
#44206=CARTESIAN_POINT('Ctrl Pts',(-4.94679983692322,0.205641231723391,
3.17108785410252));
#44207=CARTESIAN_POINT('Ctrl Pts',(-4.94967711776464,0.103744392201655,
3.17438369972281));
#44208=CARTESIAN_POINT('Ctrl Pts',(-4.94919334226918,0.00181972978148383,
3.17767954534309));
#44209=CARTESIAN_POINT('Origin',(0.,0.,0.));
#44210=CARTESIAN_POINT('',(-4.93570031758673,0.00282778719561921,4.32232045465689));
#44211=CARTESIAN_POINT('',(-4.93596067211196,0.00302686994969232,4.17767954534309));
#44212=CARTESIAN_POINT('',(-4.942,-6.05220448138622E-16,0.));
#44213=CARTESIAN_POINT('Ctrl Pts',(-4.93570031758673,0.00282778719561921,
4.32232045465689));
#44214=CARTESIAN_POINT('Ctrl Pts',(-4.93901975399819,0.635970529567334,
4.30199020357146));
#44215=CARTESIAN_POINT('Ctrl Pts',(-4.82594024125747,1.26797266957629,4.28165995248604));
#44216=CARTESIAN_POINT('Ctrl Pts',(-4.59096240198504,1.85083188703807,4.26132970140062));
#44217=CARTESIAN_POINT('Ctrl Pts',(-3.98112048346584,3.36353616802088,4.2085662605404));
#44218=CARTESIAN_POINT('Ctrl Pts',(-2.55021179152983,4.54522999135323,4.15580281968019));
#44219=CARTESIAN_POINT('Ctrl Pts',(-0.94949200772219,4.85808392031181,4.10303937881998));
#44220=CARTESIAN_POINT('Ctrl Pts',(0.651227776085471,5.17093784927039,4.05027593795976));
#44221=CARTESIAN_POINT('Ctrl Pts',(2.42175865176475,4.61495188385518,3.99751249709954));
#44222=CARTESIAN_POINT('Ctrl Pts',(3.55627122044722,3.44317432848828,3.94474905623933));
#44223=CARTESIAN_POINT('Ctrl Pts',(4.69078378912967,2.27139677312141,3.89198561537911));
#44224=CARTESIAN_POINT('Ctrl Pts',(5.18927805081532,0.483827627802874,3.8392221745189));
#44225=CARTESIAN_POINT('Ctrl Pts',(4.82487214846976,-1.10594900598695,3.78645873365868));
#44226=CARTESIAN_POINT('Ctrl Pts',(4.46046624612419,-2.6957256397768,3.73369529279847));
#44227=CARTESIAN_POINT('Ctrl Pts',(3.23316017974738,-4.08770976203793,3.68093185193825));
#44228=CARTESIAN_POINT('Ctrl Pts',(1.7015430859675,-4.6483616008314,3.62816841107804));
#44229=CARTESIAN_POINT('Ctrl Pts',(0.169925992187646,-5.20901343962485,
3.57540497021783));
#44230=CARTESIAN_POINT('Ctrl Pts',(-1.66600212899526,-4.93833299495065,
3.52264152935761));
#44231=CARTESIAN_POINT('Ctrl Pts',(-2.97064734936451,-3.95951622992839,
3.4698780884974));
#44232=CARTESIAN_POINT('Ctrl Pts',(-4.18683263839842,-3.04706698189228,
3.42069221055056));
#44233=CARTESIAN_POINT('Ctrl Pts',(-4.94133855052495,-1.51925455419597,
3.37150633260372));
#44234=CARTESIAN_POINT('Ctrl Pts',(-4.94903399601206,0.00195803074323202,
3.32232045465689));
#44235=CARTESIAN_POINT('Ctrl Pts',(-4.94919334226918,0.00181972978148383,
3.17767954534309));
#44236=CARTESIAN_POINT('Ctrl Pts',(-4.94192746196068,-1.52899860347891,
3.22718023319751));
#44237=CARTESIAN_POINT('Ctrl Pts',(-4.17649517400323,-3.06609305497157,
3.27668092105193));
#44238=CARTESIAN_POINT('Ctrl Pts',(-2.94711271903068,-3.97709242316291,
3.32618160890635));
#44239=CARTESIAN_POINT('Ctrl Pts',(-1.63587574939375,-4.94874778236929,
3.37897814238105));
#44240=CARTESIAN_POINT('Ctrl Pts',(0.203149430377691,-5.20815939885737,
3.43177467585576));
#44241=CARTESIAN_POINT('Ctrl Pts',(1.73199722462222,-4.63712444206039,3.48457120933046));
#44242=CARTESIAN_POINT('Ctrl Pts',(3.26084501886676,-4.06608948526341,3.53736774280516));
#44243=CARTESIAN_POINT('Ctrl Pts',(4.47951542758438,-2.66460795518137,3.59016427627987));
#44244=CARTESIAN_POINT('Ctrl Pts',(4.83271212906113,-1.07127541230128,3.64296080975457));
#44245=CARTESIAN_POINT('Ctrl Pts',(5.18590883053788,0.522057130578818,3.69575734322927));
#44246=CARTESIAN_POINT('Ctrl Pts',(4.67363182477377,2.30724068625696,3.74855387670398));
#44247=CARTESIAN_POINT('Ctrl Pts',(3.52930397676422,3.47084297428374,3.80135041017868));
#44248=CARTESIAN_POINT('Ctrl Pts',(2.38497612875467,4.63444526231052,3.85414694365339));
#44249=CARTESIAN_POINT('Ctrl Pts',(0.6085974384997,5.17646628268592,3.90694347712809));
#44250=CARTESIAN_POINT('Ctrl Pts',(-0.990411824257063,4.84993009504558,
3.95974001060279));
#44251=CARTESIAN_POINT('Ctrl Pts',(-2.58942108701383,4.52339390740524,4.0125365440775));
#44252=CARTESIAN_POINT('Ctrl Pts',(-4.01106092227238,3.32830051174915,4.0653330775522));
#44253=CARTESIAN_POINT('Ctrl Pts',(-4.60755047572122,1.80920317532792,4.11812961102691));
#44254=CARTESIAN_POINT('Ctrl Pts',(-4.831813392182,1.23806626759189,4.1379795891323));
#44255=CARTESIAN_POINT('Ctrl Pts',(-4.93943770829377,0.621129986103563,
4.1578295672377));
#44256=CARTESIAN_POINT('Ctrl Pts',(-4.93596067211196,0.00302686994969232,
4.17767954534309));
#44257=CARTESIAN_POINT('Origin',(0.,0.,0.));
#44258=CARTESIAN_POINT('',(-4.93897027655035,-0.00418490057281118,5.32232045465689));
#44259=CARTESIAN_POINT('',(-4.93838471541483,-0.00406162586984615,5.17767954534309));
#44260=CARTESIAN_POINT('',(-4.942,-6.05220448138622E-16,0.));
#44261=CARTESIAN_POINT('Ctrl Pts',(-4.93897027655035,-0.00418490057281118,
5.32232045465689));
#44262=CARTESIAN_POINT('Ctrl Pts',(-4.92960049919577,1.1487585810669,5.28523751539942));
#44263=CARTESIAN_POINT('Ctrl Pts',(-4.5267508630109,2.30760372029857,5.24815457614196));
#44264=CARTESIAN_POINT('Ctrl Pts',(-3.78916668346253,3.18507932319436,5.21107163688449));
#44265=CARTESIAN_POINT('Ctrl Pts',(-2.73969541672107,4.43359502898083,5.15830819602428));
#44266=CARTESIAN_POINT('Ctrl Pts',(-1.01255385125843,5.11247792715855,5.10554475516406));
#44267=CARTESIAN_POINT('Ctrl Pts',(0.606176578608286,4.91274509878472,5.05278131430385));
#44268=CARTESIAN_POINT('Ctrl Pts',(2.224907008475,4.71301227041089,5.00001787344363));
#44269=CARTESIAN_POINT('Ctrl Pts',(3.73522630274578,3.63466371548551,4.94725443258342));
#44270=CARTESIAN_POINT('Ctrl Pts',(4.44973628814144,2.16849289048282,4.8944909917232));
#44271=CARTESIAN_POINT('Ctrl Pts',(5.1642462735371,0.702322065480126,4.84172755086299));
#44272=CARTESIAN_POINT('Ctrl Pts',(5.08294695005765,-1.15167102959988,4.78896411000277));
#44273=CARTESIAN_POINT('Ctrl Pts',(4.24284043151724,-2.54967047338244,4.73620066914256));
#44274=CARTESIAN_POINT('Ctrl Pts',(3.40273391297681,-3.94766991716502,4.68343722828234));
#44275=CARTESIAN_POINT('Ctrl Pts',(1.80382019937538,-4.88967570965013,4.63067378742212));
#44276=CARTESIAN_POINT('Ctrl Pts',(0.173819826494171,-4.94694866740537,
4.57791034656191));
#44277=CARTESIAN_POINT('Ctrl Pts',(-1.45618054638702,-5.0042216251606,4.5251469057017));
#44278=CARTESIAN_POINT('Ctrl Pts',(-3.11726757854798,-4.17676174818597,
4.47238346484148));
#44279=CARTESIAN_POINT('Ctrl Pts',(-4.05342352207729,-2.84117444038203,
4.41962002398127));
#44280=CARTESIAN_POINT('Ctrl Pts',(-4.62886975682389,-2.02020151085742,
4.38718683420648));
#44281=CARTESIAN_POINT('Ctrl Pts',(-4.93040476513016,-1.00723542508793,
4.35475364443168));
#44282=CARTESIAN_POINT('Ctrl Pts',(-4.93570031758673,0.00282778719561921,
4.32232045465689));
#44283=CARTESIAN_POINT('Ctrl Pts',(-4.93596067211196,0.00302686994969232,
4.17767954534309));
#44284=CARTESIAN_POINT('Ctrl Pts',(-4.9301895642308,-1.0228870344476,4.2106261007124));
#44285=CARTESIAN_POINT('Ctrl Pts',(-4.61834948018582,-2.05201540819261,
4.24357265608171));
#44286=CARTESIAN_POINT('Ctrl Pts',(-4.02575926717865,-2.88027773583012,
4.27651921145102));
#44287=CARTESIAN_POINT('Ctrl Pts',(-3.07613923354808,-4.20756003338059,
4.32931574492572));
#44288=CARTESIAN_POINT('Ctrl Pts',(-1.40555989464781,-5.01902335129515,
4.38211227840043));
#44289=CARTESIAN_POINT('Ctrl Pts',(0.224766745275694,-4.94491834338594,
4.43490881187513));
#44290=CARTESIAN_POINT('Ctrl Pts',(1.85509338519918,-4.87081333547673,4.48770534534984));
#44291=CARTESIAN_POINT('Ctrl Pts',(3.44516732614589,-3.91114000174376,4.54050187882454));
#44292=CARTESIAN_POINT('Ctrl Pts',(4.270459451601,-2.50318069379225,4.59329841229924));
#44293=CARTESIAN_POINT('Ctrl Pts',(5.09575157705613,-1.09522138584072,4.64609494577394));
#44294=CARTESIAN_POINT('Ctrl Pts',(5.15626188701963,0.761023896329388,4.69889147924865));
#44295=CARTESIAN_POINT('Ctrl Pts',(4.42441840505647,2.21974306847382,4.75168801272335));
#44296=CARTESIAN_POINT('Ctrl Pts',(3.69257492309331,3.67846224061823,4.80448454619806));
#44297=CARTESIAN_POINT('Ctrl Pts',(2.16837764920352,4.73965530273698,4.85728107967276));
#44298=CARTESIAN_POINT('Ctrl Pts',(0.54633850223222,4.91978167747611,4.91007761314747));
#44299=CARTESIAN_POINT('Ctrl Pts',(-1.0757006447391,5.09990805221523,4.96287414662217));
#44300=CARTESIAN_POINT('Ctrl Pts',(-2.79558166479192,4.39896773957469,5.01567068009687));
#44301=CARTESIAN_POINT('Ctrl Pts',(-3.82962787248045,3.13634944983863,5.06846721357158));
#44302=CARTESIAN_POINT('Ctrl Pts',(-4.54262037450559,2.26575259758193,5.10487132416208));
#44303=CARTESIAN_POINT('Ctrl Pts',(-4.92954384104421,1.12811506301544,5.14127543475258));
#44304=CARTESIAN_POINT('Ctrl Pts',(-4.93838471541483,-0.00406162586984614,
5.17767954534309));
#44305=CARTESIAN_POINT('Origin',(0.,0.,0.));
#44306=CARTESIAN_POINT('',(-4.94990673126105,0.000609106175146774,6.32232045465689));
#44307=CARTESIAN_POINT('',(-4.95002176789587,9.24615926348992E-5,6.1776795453431));
#44308=CARTESIAN_POINT('',(-4.942,-6.05220448138622E-16,0.));
#44309=CARTESIAN_POINT('Ctrl Pts',(-4.94990673126105,0.000609106175146774,
6.32232045465689));
#44310=CARTESIAN_POINT('Ctrl Pts',(-4.94996465668772,0.0337538979231002,
6.3212482680876));
#44311=CARTESIAN_POINT('Ctrl Pts',(-4.94966035453883,0.0668975980773335,
6.3201760815183));
#44312=CARTESIAN_POINT('Ctrl Pts',(-4.94899057048952,0.100033910748547,
6.31910389494901));
#44313=CARTESIAN_POINT('Ctrl Pts',(-4.91602978541085,1.73070708277234,6.26634045408879));
#44314=CARTESIAN_POINT('Ctrl Pts',(-3.99797098316147,3.34348977495136,6.21357701322858));
#44315=CARTESIAN_POINT('Ctrl Pts',(-2.61265424963019,4.20434920314469,6.16081357236836));
#44316=CARTESIAN_POINT('Ctrl Pts',(-1.22733751609891,5.06520863133802,6.10805013150815));
#44317=CARTESIAN_POINT('Ctrl Pts',(0.625237148714281,5.17414479554567,6.05528669064793));
#44318=CARTESIAN_POINT('Ctrl Pts',(2.10189939976769,4.48157710670587,6.00252324978771));
#44319=CARTESIAN_POINT('Ctrl Pts',(3.57856165082109,3.78900941786606,5.9497598089275));
#44320=CARTESIAN_POINT('Ctrl Pts',(4.67931148811471,2.29493787597879,5.89699636806729));
#44321=CARTESIAN_POINT('Ctrl Pts',(4.90315986233076,0.679365744295384,5.84423292720707));
#44322=CARTESIAN_POINT('Ctrl Pts',(5.12700823654681,-0.936206387388013,
5.79146948634686));
#44323=CARTESIAN_POINT('Ctrl Pts',(4.4739551476853,-2.67327910886755,5.73870604548664));
#44324=CARTESIAN_POINT('Ctrl Pts',(3.24122748150885,-3.74125097570411,5.68594260462643));
#44325=CARTESIAN_POINT('Ctrl Pts',(2.00849981533238,-4.80922284254067,5.63317916376621));
#44326=CARTESIAN_POINT('Ctrl Pts',(0.196097571840956,-5.20809385473422,
5.580415722906));
#44327=CARTESIAN_POINT('Ctrl Pts',(-1.37109275233711,-4.7563241179068,5.52765228204578));
#44328=CARTESIAN_POINT('Ctrl Pts',(-2.93828307651517,-4.30455438107937,
5.47488884118557));
#44329=CARTESIAN_POINT('Ctrl Pts',(-4.26026148137987,-3.00214389523098,
5.42212540032535));
#44330=CARTESIAN_POINT('Ctrl Pts',(-4.73535019980207,-1.44186439560917,
5.36936195946513));
#44331=CARTESIAN_POINT('Ctrl Pts',(-4.87653942645625,-0.978172778920024,
5.35368145786239));
#44332=CARTESIAN_POINT('Ctrl Pts',(-4.94293228203772,-0.49170645290201,
5.33800095625964));
#44333=CARTESIAN_POINT('Ctrl Pts',(-4.93897027655035,-0.00418490057281118,
5.32232045465689));
#44334=CARTESIAN_POINT('Ctrl Pts',(-4.93838471541483,-0.00406162586984614,
5.17767954534309));
#44335=CARTESIAN_POINT('Ctrl Pts',(-4.94236567660296,-0.513869962422989,
5.19407196822729));
#44336=CARTESIAN_POINT('Ctrl Pts',(-4.86968605256145,-1.02257104983416,
5.21046439111149));
#44337=CARTESIAN_POINT('Ctrl Pts',(-4.71559692470099,-1.50528507494596,
5.22685681399569));
#44338=CARTESIAN_POINT('Ctrl Pts',(-4.21930837390877,-3.06000504316299,
5.27965334747039));
#44339=CARTESIAN_POINT('Ctrl Pts',(-2.8785198770001,-4.34514871276549,5.3324498809451));
#44340=CARTESIAN_POINT('Ctrl Pts',(-1.30417176812337,-4.7751307324871,5.3852464144198));
#44341=CARTESIAN_POINT('Ctrl Pts',(0.270176340753341,-5.2051127522087,5.4380429478945));
#44342=CARTESIAN_POINT('Ctrl Pts',(2.07808406159809,-4.77993312204945,5.49083948136921));
#44343=CARTESIAN_POINT('Ctrl Pts',(3.29576468259939,-3.69332812921623,5.54363601484391));
#44344=CARTESIAN_POINT('Ctrl Pts',(4.51344530360071,-2.606723136383,5.59643254831862));
#44345=CARTESIAN_POINT('Ctrl Pts',(5.14089882475856,-0.858692780875764,
5.64922908179332));
#44346=CARTESIAN_POINT('Ctrl Pts',(4.892221343433,0.754259796075777,5.70202561526803));
#44347=CARTESIAN_POINT('Ctrl Pts',(4.64354386210744,2.36721237302732,5.75482214874273));
#44348=CARTESIAN_POINT('Ctrl Pts',(3.51873537829851,3.84508717142316,5.80761868221743));
#44349=CARTESIAN_POINT('Ctrl Pts',(2.03032331340283,4.51447945572607,5.86041521569213));
#44350=CARTESIAN_POINT('Ctrl Pts',(0.54191124850715,5.18387174002898,5.91321174916684));
#44351=CARTESIAN_POINT('Ctrl Pts',(-1.31010439747531,5.04478151023892,5.96600828264154));
#44352=CARTESIAN_POINT('Ctrl Pts',(-2.68183880585053,4.16058627269715,6.01880481611625));
#44353=CARTESIAN_POINT('Ctrl Pts',(-4.05357321422575,3.27639103515538,6.07160134959095));
#44354=CARTESIAN_POINT('Ctrl Pts',(-4.94502638499377,1.6470907898619,6.12439788306566));
#44355=CARTESIAN_POINT('Ctrl Pts',(-4.95000099524402,0.0150884128829395,
6.17719441654037));
#44356=CARTESIAN_POINT('Ctrl Pts',(-4.95001623189281,0.0100897806679753,
6.17735612614128));
#44357=CARTESIAN_POINT('Ctrl Pts',(-4.950023152263,0.00509112310363388,
6.17751783574219));
#44358=CARTESIAN_POINT('Ctrl Pts',(-4.95002176789587,9.24615926348992E-5,
6.1776795453431));
#44359=CARTESIAN_POINT('Origin',(0.,0.,0.));
#44360=CARTESIAN_POINT('',(-4.93729272679059,0.00368592931905526,7.32232045465689));
#44361=CARTESIAN_POINT('',(-4.93812703863464,0.00398950918922817,7.17767954534309));
#44362=CARTESIAN_POINT('',(-4.942,-6.05220448138622E-16,0.));
#44363=CARTESIAN_POINT('Ctrl Pts',(-4.93729272679059,0.00368592931905526,
7.32232045465689));
#44364=CARTESIAN_POINT('Ctrl Pts',(-4.94116559210242,0.558353954818944,
7.30449557991555));
#44365=CARTESIAN_POINT('Ctrl Pts',(-4.85488370936681,1.1118525040865,7.28667070517422));
#44366=CARTESIAN_POINT('Ctrl Pts',(-4.67321739836765,1.63203970469098,7.26884583043288));
#44367=CARTESIAN_POINT('Ctrl Pts',(-4.13546665420853,3.17184668755196,7.21608238957266));
#44368=CARTESIAN_POINT('Ctrl Pts',(-2.76193831173125,4.41977291493536,7.16331894871245));
#44369=CARTESIAN_POINT('Ctrl Pts',(-1.17777228483381,4.80784430854112,7.11055550785224));
#44370=CARTESIAN_POINT('Ctrl Pts',(0.406393742063621,5.19591570214688,7.05779206699202));
#44371=CARTESIAN_POINT('Ctrl Pts',(2.2011974533812,4.72413226197502,7.0050286261318));
#44372=CARTESIAN_POINT('Ctrl Pts',(3.38976204879511,3.60721883209798,6.95226518527158));
#44373=CARTESIAN_POINT('Ctrl Pts',(4.57832664420902,2.49030540222094,6.89950174441137));
#44374=CARTESIAN_POINT('Ctrl Pts',(5.16065212371926,0.728261982638741,6.84673830355116));
#44375=CARTESIAN_POINT('Ctrl Pts',(4.8717021652758,-0.876944960040814,6.79397486269094));
#44376=CARTESIAN_POINT('Ctrl Pts',(4.58275220683234,-2.48215190272036,6.74121142183073));
#44377=CARTESIAN_POINT('Ctrl Pts',(3.4225268104352,-3.93052236849726,6.68844798097051));
#44378=CARTESIAN_POINT('Ctrl Pts',(1.91908439466629,-4.56285322317541,6.63568454011029));
#44379=CARTESIAN_POINT('Ctrl Pts',(0.415641978897348,-5.19518407785358,
6.58292109925008));
#44380=CARTESIAN_POINT('Ctrl Pts',(-1.43101745624338,-5.01147532143298,
6.53015765838987));
#44381=CARTESIAN_POINT('Ctrl Pts',(-2.78041578985976,-4.09533911728839,
6.47739421752966));
#44382=CARTESIAN_POINT('Ctrl Pts',(-4.10239349384425,-3.1978193816249,6.42570296323874));
#44383=CARTESIAN_POINT('Ctrl Pts',(-4.94711408486409,-1.59733653848074,
6.37401170894781));
#44384=CARTESIAN_POINT('Ctrl Pts',(-4.94990673126105,0.000609106175146774,
6.32232045465689));
#44385=CARTESIAN_POINT('Ctrl Pts',(-4.95002176789587,9.24615926348992E-5,
6.1776795453431));
#44386=CARTESIAN_POINT('Ctrl Pts',(-4.94957117052949,-1.62692081873173,
6.23031436921689));
#44387=CARTESIAN_POINT('Ctrl Pts',(-4.06928678123987,-3.25435222218023,
6.28294919309067));
#44388=CARTESIAN_POINT('Ctrl Pts',(-2.70715303041471,-4.14415974390912,
6.33558401696446));
#44389=CARTESIAN_POINT('Ctrl Pts',(-1.34083440560272,-5.03670101505779,
6.38838055043917));
#44390=CARTESIAN_POINT('Ctrl Pts',(0.510298893753757,-5.18707904869072,
6.44117708391388));
#44391=CARTESIAN_POINT('Ctrl Pts',(2.00276409681877,-4.52677296598962,6.49397361738859));
#44392=CARTESIAN_POINT('Ctrl Pts',(3.49522929988377,-3.86646688328851,6.54677015086329));
#44393=CARTESIAN_POINT('Ctrl Pts',(4.62902640665733,-2.39547668425338,6.59956668433799));
#44394=CARTESIAN_POINT('Ctrl Pts',(4.88753226227565,-0.784070085091338,
6.65236321781269));
#44395=CARTESIAN_POINT('Ctrl Pts',(5.14603811789397,0.827336514070738,6.7051597512874));
#44396=CARTESIAN_POINT('Ctrl Pts',(4.52925272235704,2.57915951335971,6.7579562847621));
#44397=CARTESIAN_POINT('Ctrl Pts',(3.31821896685987,3.67316762496513,6.81075281823681));
#44398=CARTESIAN_POINT('Ctrl Pts',(2.10718521136272,4.76717573657052,6.86354935171151));
#44399=CARTESIAN_POINT('Ctrl Pts',(0.301903095905328,5.20336896049236,6.91634588518622));
#44400=CARTESIAN_POINT('Ctrl Pts',(-1.27503704449112,4.78299258292295,6.96914241866092));
#44401=CARTESIAN_POINT('Ctrl Pts',(-2.85197718488759,4.36261620535354,7.02193895213562));
#44402=CARTESIAN_POINT('Ctrl Pts',(-4.20057535022311,3.0856702262929,7.07473548561032));
#44403=CARTESIAN_POINT('Ctrl Pts',(-4.70633267235205,1.53400465783913,7.12753201908503));
#44404=CARTESIAN_POINT('Ctrl Pts',(-4.86645984309908,1.04273383179117,7.14424786117105));
#44405=CARTESIAN_POINT('Ctrl Pts',(-4.94209974418837,0.523924819599999,
7.16096370325707));
#44406=CARTESIAN_POINT('Ctrl Pts',(-4.93812703863464,0.00398950918922817,
7.17767954534309));
#44407=CARTESIAN_POINT('Origin',(0.,0.,0.));
#44408=CARTESIAN_POINT('',(-4.9370364718937,-0.00357917755902493,8.32232045465689));
#44409=CARTESIAN_POINT('',(-4.93615302863258,-0.00314627141571121,8.17767954534309));
#44410=CARTESIAN_POINT('',(-4.942,-6.05220448138622E-16,0.));
#44411=CARTESIAN_POINT('Ctrl Pts',(-4.9370364718937,-0.00357917755902493,
8.32232045465689));
#44412=CARTESIAN_POINT('Ctrl Pts',(-4.92976643593387,1.07253365977557,8.28774289174351));
#44413=CARTESIAN_POINT('Ctrl Pts',(-4.58366254169201,2.15290343310709,8.25316532883013));
#44414=CARTESIAN_POINT('Ctrl Pts',(-3.93530233070663,3.00265049848112,8.21858776591675));
#44415=CARTESIAN_POINT('Ctrl Pts',(-2.94594065318929,4.29931733247173,8.16582432505654));
#44416=CARTESIAN_POINT('Ctrl Pts',(-1.25277317118212,5.05897768713911,8.11306088419632));
#44417=CARTESIAN_POINT('Ctrl Pts',(0.373581453010537,4.93588404929253,8.06029744333611));
#44418=CARTESIAN_POINT('Ctrl Pts',(1.99993607720318,4.81279041144596,8.00753400247589));
#44419=CARTESIAN_POINT('Ctrl Pts',(3.55947784358134,3.80694278108544,7.95477056161567));
#44420=CARTESIAN_POINT('Ctrl Pts',(4.34240574156256,2.37613695433122,7.90200712075546));
#44421=CARTESIAN_POINT('Ctrl Pts',(5.12533363954378,0.945331127576992,7.84924367989524));
#44422=CARTESIAN_POINT('Ctrl Pts',(5.13164766912806,-0.910432895570919,
7.79648023903503));
#44423=CARTESIAN_POINT('Ctrl Pts',(4.35847409863575,-2.34653318357428,7.74371679817482));
#44424=CARTESIAN_POINT('Ctrl Pts',(3.58530052814345,-3.78263347157761,7.6909533573146));
#44425=CARTESIAN_POINT('Ctrl Pts',(2.03263935757455,-4.7990700244364,7.63818991645438));
#44426=CARTESIAN_POINT('Ctrl Pts',(0.407160002087725,-4.93322766379111,
7.58542647559417));
#44427=CARTESIAN_POINT('Ctrl Pts',(-1.21831935339912,-5.06738530314582,
7.53266303473395));
#44428=CARTESIAN_POINT('Ctrl Pts',(-2.91661689380388,-4.31926402899647,
7.47989959387374));
#44429=CARTESIAN_POINT('Ctrl Pts',(-3.9147790910858,-3.02935952275251,7.42713615301352));
#44430=CARTESIAN_POINT('Ctrl Pts',(-4.57573590812677,-2.1752186035157,7.39219758689465));
#44431=CARTESIAN_POINT('Ctrl Pts',(-4.92970151716189,-1.08351977418085,
7.35725902077577));
#44432=CARTESIAN_POINT('Ctrl Pts',(-4.93729272679059,0.00368592931905526,
7.32232045465689));
#44433=CARTESIAN_POINT('Ctrl Pts',(-4.93812703863464,0.00398950918922817,
7.17767954534309));
#44434=CARTESIAN_POINT('Ctrl Pts',(-4.9295520615366,-1.11827674461206,7.21376023673177));
#44435=CARTESIAN_POINT('Ctrl Pts',(-4.55006154683992,-2.24579042752333,
7.24984092812046));
#44436=CARTESIAN_POINT('Ctrl Pts',(-3.84867674353058,-3.11294472114867,
7.28592161950915));
#44437=CARTESIAN_POINT('Ctrl Pts',(-2.82234701365785,-4.38184337383585,
7.33871815298385));
#44438=CARTESIAN_POINT('Ctrl Pts',(-1.10677107499002,-5.09325552136332,
7.39151468645855));
#44439=CARTESIAN_POINT('Ctrl Pts',(0.516336029677229,-4.92302088331724,
7.44431121993325));
#44440=CARTESIAN_POINT('Ctrl Pts',(2.13944313434447,-4.75278624527117,7.49710775340795));
#44441=CARTESIAN_POINT('Ctrl Pts',(3.67008140501115,-3.70090482165158,7.54990428688267));
#44442=CARTESIAN_POINT('Ctrl Pts',(4.41080403428737,-2.24667427194838,7.60270082035737));
#44443=CARTESIAN_POINT('Ctrl Pts',(5.15152666356361,-0.792443722245162,
7.65549735383208));
#44444=CARTESIAN_POINT('Ctrl Pts',(5.10233365144936,1.06413595354166,7.70829388730677));
#44445=CARTESIAN_POINT('Ctrl Pts',(4.28564016284837,2.47710030230944,7.76109042078147));
#44446=CARTESIAN_POINT('Ctrl Pts',(3.46894667424739,3.89006465107721,7.81388695425618));
#44447=CARTESIAN_POINT('Ctrl Pts',(1.88475270915971,4.85941367282593,7.86668348773089));
#44448=CARTESIAN_POINT('Ctrl Pts',(0.254908128790928,4.94345621594819,7.91948002120559));
#44449=CARTESIAN_POINT('Ctrl Pts',(-1.37493645157786,5.02749875907046,7.9722765546803));
#44450=CARTESIAN_POINT('Ctrl Pts',(-3.05043164722777,4.22623482356622,8.02507308815499));
#44451=CARTESIAN_POINT('Ctrl Pts',(-4.00812550651364,2.90476633090432,8.0778696216297));
#44452=CARTESIAN_POINT('Ctrl Pts',(-4.61162062728013,2.07203697816232,8.11113959620083));
#44453=CARTESIAN_POINT('Ctrl Pts',(-4.93008062183261,1.03273713844183,8.14440957077196));
#44454=CARTESIAN_POINT('Ctrl Pts',(-4.93615302863258,-0.00314627141571121,
8.17767954534309));
#44455=CARTESIAN_POINT('Origin',(0.,0.,0.));
#44456=CARTESIAN_POINT('',(-4.94983422880388,-0.000811751590238941,9.32232045465689));
#44457=CARTESIAN_POINT('',(-4.94934061074693,-0.00165165342605634,9.1776795453431));
#44458=CARTESIAN_POINT('',(-4.942,-6.05220448138622E-16,0.));
#44459=CARTESIAN_POINT('Ctrl Pts',(-4.94983422880388,-0.000811751590238941,
9.32232045465689));
#44460=CARTESIAN_POINT('Ctrl Pts',(-4.94619904315733,1.58603660082692,9.27099020357146));
#44461=CARTESIAN_POINT('Ctrl Pts',(-4.11486910012118,3.17616060693066,9.21965995248604));
#44462=CARTESIAN_POINT('Ctrl Pts',(-2.80821896129528,4.07632441244751,9.16832970140062));
#44463=CARTESIAN_POINT('Ctrl Pts',(-1.46508589907443,5.00162165359779,9.1155662605404));
#44464=CARTESIAN_POINT('Ctrl Pts',(0.38028069926283,5.19789211576897,9.06280281968019));
#44465=CARTESIAN_POINT('Ctrl Pts',(1.88799112724405,4.575806371946,9.01003937881998));
#44466=CARTESIAN_POINT('Ctrl Pts',(3.39570155522527,3.95372062812305,8.95727593795976));
#44467=CARTESIAN_POINT('Ctrl Pts',(4.56575581285046,2.51327867830594,8.90451249709954));
#44468=CARTESIAN_POINT('Ctrl Pts',(4.86562202928207,0.910075116822231,8.85174905623933));
#44469=CARTESIAN_POINT('Ctrl Pts',(5.16548824571368,-0.693128444661515,
8.79898561537912));
#44470=CARTESIAN_POINT('Ctrl Pts',(4.5951664209517,-2.45909361781186,8.7462221745189));
#44471=CARTESIAN_POINT('Ctrl Pts',(3.4142296015798,-3.58406901130408,8.69345873365869));
#44472=CARTESIAN_POINT('Ctrl Pts',(2.23329278220791,-4.70904440479628,8.64069529279847));
#44473=CARTESIAN_POINT('Ctrl Pts',(0.441740968226092,-5.19303001863033,
8.58793185193825));
#44474=CARTESIAN_POINT('Ctrl Pts',(-1.14502909018537,-4.81574738049279,
8.53516841107804));
#44475=CARTESIAN_POINT('Ctrl Pts',(-2.73179914859682,-4.43846474235526,
8.48240497021782));
#44476=CARTESIAN_POINT('Ctrl Pts',(-4.11378745143793,-3.19991385224615,
8.42964152935761));
#44477=CARTESIAN_POINT('Ctrl Pts',(-4.66200366634471,-1.66380175053471,
8.3768780884974));
#44478=CARTESIAN_POINT('Ctrl Pts',(-4.85095633907095,-1.1343528226608,8.35869221055056));
#44479=CARTESIAN_POINT('Ctrl Pts',(-4.94086010709221,-0.569554771785043,
8.34050633260373));
#44480=CARTESIAN_POINT('Ctrl Pts',(-4.9370364718937,-0.00357917755902493,
8.32232045465689));
#44481=CARTESIAN_POINT('Ctrl Pts',(-4.93615302863258,-0.00314627141571121,
8.17767954534309));
#44482=CARTESIAN_POINT('Ctrl Pts',(-4.93971699916741,-0.611119036064889,
8.19720610424667));
#44483=CARTESIAN_POINT('Ctrl Pts',(-4.83567403422615,-1.21791495642756,
8.21673266315024));
#44484=CARTESIAN_POINT('Ctrl Pts',(-4.61849424808279,-1.78108068136924,
8.23625922205381));
#44485=CARTESIAN_POINT('Ctrl Pts',(-4.03127660744421,-3.30378615116137,
8.28905575552852));
#44486=CARTESIAN_POINT('Ctrl Pts',(-2.61694880324517,-4.50752404092604,
8.34185228900322));
#44487=CARTESIAN_POINT('Ctrl Pts',(-1.01995990653351,-4.84380215349313,
8.39464882247793));
#44488=CARTESIAN_POINT('Ctrl Pts',(0.57702899017813,-5.18008026606022,8.44744535595263));
#44489=CARTESIAN_POINT('Ctrl Pts',(2.35667897940238,-4.64889860142975,8.50024188942734));
#44490=CARTESIAN_POINT('Ctrl Pts',(3.50807919667006,-3.4922940688051,8.55303842290204));
#44491=CARTESIAN_POINT('Ctrl Pts',(4.65947941393775,-2.33568953618045,8.60583495637674));
#44492=CARTESIAN_POINT('Ctrl Pts',(5.18262985924886,-0.553662135561577,
8.65863148985144));
#44493=CARTESIAN_POINT('Ctrl Pts',(4.83915310871477,1.04179398325038,8.71142802332615));
#44494=CARTESIAN_POINT('Ctrl Pts',(4.49567635818068,2.63725010206233,8.76422455680085));
#44495=CARTESIAN_POINT('Ctrl Pts',(3.28557241180142,4.04613493906739,8.81702109027556));
#44496=CARTESIAN_POINT('Ctrl Pts',(1.76023420818717,4.62647955204043,8.86981762375026));
#44497=CARTESIAN_POINT('Ctrl Pts',(0.234896004572933,5.20682416501346,8.92261415722497));
#44498=CARTESIAN_POINT('Ctrl Pts',(-1.60567645627628,4.95862855395447,8.97541069069966));
#44499=CARTESIAN_POINT('Ctrl Pts',(-2.9228125287938,3.99498491044041,9.02820722417436));
#44500=CARTESIAN_POINT('Ctrl Pts',(-4.16579429986394,3.0855940679239,9.07803133123061));
#44501=CARTESIAN_POINT('Ctrl Pts',(-4.9426191442377,1.53904642191653,9.12785543828685));
#44502=CARTESIAN_POINT('Ctrl Pts',(-4.94934061074693,-0.00165165342605634,
9.1776795453431));
#44503=CARTESIAN_POINT('Origin',(0.,0.,0.));
#44504=CARTESIAN_POINT('',(-4.93927523449924,0.00424456982664218,10.3223204546569));
#44505=CARTESIAN_POINT('',(-4.94081497674544,0.00444099958366976,10.1776795453431));
#44506=CARTESIAN_POINT('',(-4.942,-6.05220448138622E-16,0.));
#44507=CARTESIAN_POINT('Ctrl Pts',(-4.93927523449924,0.00424456982664218,
10.3223204546569));
#44508=CARTESIAN_POINT('Ctrl Pts',(-4.94321947186548,0.480467662900444,
10.3070009562597));
#44509=CARTESIAN_POINT('Ctrl Pts',(-4.8799048924926,0.955663934034991,10.2916814578624));
#44510=CARTESIAN_POINT('Ctrl Pts',(-4.7450520171049,1.40960838712838,10.2763619594652));
#44511=CARTESIAN_POINT('Ctrl Pts',(-4.28059152820107,2.97308459787111,10.2235985186049));
#44512=CARTESIAN_POINT('Ctrl Pts',(-2.96750623957443,4.28446059329433,10.1708350777447));
#44513=CARTESIAN_POINT('Ctrl Pts',(-1.40342635577711,4.74688412687777,10.1180716368845));
#44514=CARTESIAN_POINT('Ctrl Pts',(0.160653528020168,5.2093076604612,10.0653081960243));
#44515=CARTESIAN_POINT('Ctrl Pts',(1.9757280069881,4.82277873220489,10.0125447551641));
#44516=CARTESIAN_POINT('Ctrl Pts',(3.21569435837255,3.76321993027579,9.95978131430385));
#44517=CARTESIAN_POINT('Ctrl Pts',(4.455660709757,2.70366112834667,9.90701787344364));
#44518=CARTESIAN_POINT('Ctrl Pts',(5.12051893355795,0.971072452744719,9.85425443258342));
#44519=CARTESIAN_POINT('Ctrl Pts',(4.90766922172796,-0.64598549534651,9.8014909917232));
#44520=CARTESIAN_POINT('Ctrl Pts',(4.69481950989796,-2.26304344343773,9.74872755086298));
#44521=CARTESIAN_POINT('Ctrl Pts',(3.60426186243706,-3.76457066401824,9.69596411000277));
#44522=CARTESIAN_POINT('Ctrl Pts',(2.13234651308336,-4.4671705584447,9.64320066914255));
#44523=CARTESIAN_POINT('Ctrl Pts',(0.660431163729675,-5.16977045287116,
9.59043722828234));
#44524=CARTESIAN_POINT('Ctrl Pts',(-1.19284188751682,-5.07344302114356,
9.53767378742213));
#44525=CARTESIAN_POINT('Ctrl Pts',(-2.58398443596702,-4.22203018520405,
9.48491034656191));
#44526=CARTESIAN_POINT('Ctrl Pts',(-3.97512698441724,-3.37061734926452,
9.43214690570169));
#44527=CARTESIAN_POINT('Ctrl Pts',(-4.90413903007116,-1.76411910911306,
9.37938346484148));
#44528=CARTESIAN_POINT('Ctrl Pts',(-4.94819528984589,-0.133707978972622,
9.32662002398126));
#44529=CARTESIAN_POINT('Ctrl Pts',(-4.94939197035033,-0.089421849745139,
9.32518683420647));
#44530=CARTESIAN_POINT('Ctrl Pts',(-4.94993572666894,-0.0451180774845514,
9.32375364443168));
#44531=CARTESIAN_POINT('Ctrl Pts',(-4.94983422880388,-0.000811751590238941,
9.32232045465689));
#44532=CARTESIAN_POINT('Ctrl Pts',(-4.94934061074693,-0.00165165342605634,
9.1776795453431));
#44533=CARTESIAN_POINT('Ctrl Pts',(-4.94974160267239,-0.0935672327028531,
9.18065197176156));
#44534=CARTESIAN_POINT('Ctrl Pts',(-4.94740170081727,-0.185461992629528,
9.18362439818002));
#44535=CARTESIAN_POINT('Ctrl Pts',(-4.9422563677255,-0.277199402591944,
9.18659682459849));
#44536=CARTESIAN_POINT('Ctrl Pts',(-4.85086444995379,-1.90664839614095,
9.23939335807319));
#44537=CARTESIAN_POINT('Ctrl Pts',(-3.87438093022463,-3.48645470726985,
9.29218989154789));
#44538=CARTESIAN_POINT('Ctrl Pts',(-2.45774784765697,-4.29676774220554,
9.34498642502259));
#44539=CARTESIAN_POINT('Ctrl Pts',(-1.04111476508925,-5.10708077714125,
9.3977829584973));
#44540=CARTESIAN_POINT('Ctrl Pts',(0.815667880316977,-5.14790053588371,
9.450579491972));
#44541=CARTESIAN_POINT('Ctrl Pts',(2.2665431508298,-4.40062718922509,9.50337602544671));
#44542=CARTESIAN_POINT('Ctrl Pts',(3.71741842134259,-3.65335384256648,9.55617255892141));
#44543=CARTESIAN_POINT('Ctrl Pts',(4.76238631696197,-2.11798739050681,9.60896909239612));
#44544=CARTESIAN_POINT('Ctrl Pts',(4.92529937908085,-0.494129071747753,
9.66176562587082));
#44545=CARTESIAN_POINT('Ctrl Pts',(5.08821244119973,1.12972924701132,9.71456215934552));
#44546=CARTESIAN_POINT('Ctrl Pts',(4.36907066981809,2.8420794324698,9.76735869282023));
#44547=CARTESIAN_POINT('Ctrl Pts',(3.09555640642893,3.86267628047412,9.82015522629493));
#44548=CARTESIAN_POINT('Ctrl Pts',(1.82204214303977,4.88327312847843,9.87295175976963));
#44549=CARTESIAN_POINT('Ctrl Pts',(-0.00584461235687284,5.21211663902861,
9.92574829324434));
#44550=CARTESIAN_POINT('Ctrl Pts',(-1.55521355102309,4.69936680030775,9.97854482671904));
#44551=CARTESIAN_POINT('Ctrl Pts',(-3.10458248968932,4.18661696158688,10.0313413601937));
#44552=CARTESIAN_POINT('Ctrl Pts',(-4.37543361162511,2.83227377359494,10.0841378936684));
#44553=CARTESIAN_POINT('Ctrl Pts',(-4.78869407209101,1.25345386713711,10.1369344271432));
#44554=CARTESIAN_POINT('Ctrl Pts',(-4.89500374307923,0.847308491854974,
10.1505161332098));
#44555=CARTESIAN_POINT('Ctrl Pts',(-4.9445618440258,0.426308236753005,10.1640978392764));
#44556=CARTESIAN_POINT('Ctrl Pts',(-4.94081497674544,0.00444099958366976,
10.1776795453431));
#44557=CARTESIAN_POINT('Origin',(0.,0.,0.));
#44558=CARTESIAN_POINT('',(-4.93550942083981,-0.00268364051190351,11.3223204546569));
#44559=CARTESIAN_POINT('',(-4.93464332849729,-0.00183839903596135,11.1776795453431));
#44560=CARTESIAN_POINT('',(-4.942,-6.05220448138622E-16,0.));
#44561=CARTESIAN_POINT('Ctrl Pts',(-4.93550942083981,-0.00268364051190351,
11.3223204546569));
#44562=CARTESIAN_POINT('Ctrl Pts',(-4.93055147786098,0.996233778963576,
11.2902482680876));
#44563=CARTESIAN_POINT('Ctrl Pts',(-4.63616667462007,1.99783803363001,11.2581760815183));
#44564=CARTESIAN_POINT('Ctrl Pts',(-4.07266300921302,2.81352633957493,11.226103894949));
#44565=CARTESIAN_POINT('Ctrl Pts',(-3.14561700753245,4.15545298365024,11.1733404540888));
#44566=CARTESIAN_POINT('Ctrl Pts',(-1.49019904742592,4.99419689804637,11.1205770132286));
#44567=CARTESIAN_POINT('Ctrl Pts',(0.140153312490383,4.94801692591001,11.0678135723684));
#44568=CARTESIAN_POINT('Ctrl Pts',(1.77050567240668,4.90183695377364,11.0150501315081));
#44569=CARTESIAN_POINT('Ctrl Pts',(3.37579243213274,3.97073309510478,10.9622866906479));
#44570=CARTESIAN_POINT('Ctrl Pts',(4.22539246378791,2.57848268891964,10.9095232497877));
#44571=CARTESIAN_POINT('Ctrl Pts',(5.07499249544306,1.18623228273452,10.8567598089275));
#44572=CARTESIAN_POINT('Ctrl Pts',(5.16890579902736,-0.667164670966868,
10.8039963680673));
#44573=CARTESIAN_POINT('Ctrl Pts',(4.46438920521479,-2.13816357523356,10.7512329272071));
#44574=CARTESIAN_POINT('Ctrl Pts',(3.75987261140222,-3.60916247950026,10.6984694863469));
#44575=CARTESIAN_POINT('Ctrl Pts',(2.25692612019279,-4.69776333433226,10.6457060454866));
#44576=CARTESIAN_POINT('Ctrl Pts',(0.639592289029041,-4.90850650951066,
10.5929426046264));
#44577=CARTESIAN_POINT('Ctrl Pts',(-0.977741542134707,-5.11924968468906,
10.5401791637662));
#44578=CARTESIAN_POINT('Ctrl Pts',(-2.70946271325277,-4.45213518021386,
10.487415722906));
#44579=CARTESIAN_POINT('Ctrl Pts',(-3.76740545422127,-3.21078971494518,
10.4346522820458));
#44580=CARTESIAN_POINT('Ctrl Pts',(-4.51818187206105,-2.32986027932856,
10.3972083395828));
#44581=CARTESIAN_POINT('Ctrl Pts',(-4.92963472322582,-1.15974067526383,
10.3597643971199));
#44582=CARTESIAN_POINT('Ctrl Pts',(-4.93927523449924,0.00424456982664218,
10.3223204546569));
#44583=CARTESIAN_POINT('Ctrl Pts',(-4.94081497674544,0.00444099958366976,
10.1776795453431));
#44584=CARTESIAN_POINT('Ctrl Pts',(-4.92999654546744,-1.21362768880717,
10.2168943727512));
#44585=CARTESIAN_POINT('Ctrl Pts',(-4.47479284917987,-2.43892410978247,
10.2561092001592));
#44586=CARTESIAN_POINT('Ctrl Pts',(-3.65816585751927,-3.33475037626519,
10.2953240275673));
#44587=CARTESIAN_POINT('Ctrl Pts',(-2.5587073834856,-4.54083808828599,10.348120561042));
#44588=CARTESIAN_POINT('Ctrl Pts',(-0.804120636422241,-5.14971688740386,
10.4009170945167));
#44589=CARTESIAN_POINT('Ctrl Pts',(0.806103773459557,-4.88394658237934,
10.4537136279914));
#44590=CARTESIAN_POINT('Ctrl Pts',(2.41632818334133,-4.61817627735482,10.5065101614661));
#44591=CARTESIAN_POINT('Ctrl Pts',(3.88219025604155,-3.47775686818796,10.5593066949408));
#44592=CARTESIAN_POINT('Ctrl Pts',(4.53575894457716,-1.9823290114935,10.6121032284155));
#44593=CARTESIAN_POINT('Ctrl Pts',(5.18932763311279,-0.486901154799003,
10.6648997618902));
#44594=CARTESIAN_POINT('Ctrl Pts',(5.03060293748377,1.3635351494231,10.7176962953649));
#44595=CARTESIAN_POINT('Ctrl Pts',(4.13190895564446,2.72581472139719,10.7704928288396));
#44596=CARTESIAN_POINT('Ctrl Pts',(3.23321497380518,4.08809429337122,10.8232893623143));
#44597=CARTESIAN_POINT('Ctrl Pts',(1.5945517057557,4.96221713309726,10.876085895789));
#44598=CARTESIAN_POINT('Ctrl Pts',(-0.0374116408992591,4.94988261297637,
10.9288824292637));
#44599=CARTESIAN_POINT('Ctrl Pts',(-1.66937498755429,4.93754809285548,10.9816789627384));
#44600=CARTESIAN_POINT('Ctrl Pts',(-3.29463841281478,4.03875621288757,11.0344754962131));
#44601=CARTESIAN_POINT('Ctrl Pts',(-4.17263844793783,2.66304823386876,11.0872720296878));
#44602=CARTESIAN_POINT('Ctrl Pts',(-4.67379383761091,1.87780513509723,11.1174078682396));
#44603=CARTESIAN_POINT('Ctrl Pts',(-4.93148820012105,0.937181102537252,
11.1475437067913));
#44604=CARTESIAN_POINT('Ctrl Pts',(-4.93464332849729,-0.00183839903596135,
11.1776795453431));
#44605=CARTESIAN_POINT('Origin',(0.,0.,0.));
#44606=CARTESIAN_POINT('',(-4.9488440041135,-0.00213750530709822,12.3223204546569));
#44607=CARTESIAN_POINT('',(-4.94745353480859,-0.00311052193284108,12.1776795453431));
#44608=CARTESIAN_POINT('',(-4.942,-6.05220448138622E-16,0.));
#44609=CARTESIAN_POINT('Ctrl Pts',(-4.9488440041135,-0.00213750530709822,
12.3223204546569));
#44610=CARTESIAN_POINT('Ctrl Pts',(-4.94061448411462,1.50806390763245,12.2734955799156));
#44611=CARTESIAN_POINT('Ctrl Pts',(-4.19858957372796,3.0252638763299,12.2246707051742));
#44612=CARTESIAN_POINT('Ctrl Pts',(-2.99752188376984,3.93921020084163,12.1758458304329));
#44613=CARTESIAN_POINT('Ctrl Pts',(-1.69956742174719,4.92688201973019,12.1230823895727));
#44614=CARTESIAN_POINT('Ctrl Pts',(0.13447629685455,5.21004913441221,12.0703189487124));
#44615=CARTESIAN_POINT('Ctrl Pts',(1.669872996944,4.65983246739314,12.0175555078522));
#44616=CARTESIAN_POINT('Ctrl Pts',(3.20526969703341,4.10961580037408,11.964792066992));
#44617=CARTESIAN_POINT('Ctrl Pts',(4.44201937861055,2.72601535165399,11.9120286261318));
#44618=CARTESIAN_POINT('Ctrl Pts',(4.81723479316035,1.13875519654544,11.8592651852716));
#44619=CARTESIAN_POINT('Ctrl Pts',(5.19245020771016,-0.44850495856316,11.8065017444114));
#44620=CARTESIAN_POINT('Ctrl Pts',(4.70613135523258,-2.23942482006024,11.7537383035512));
#44621=CARTESIAN_POINT('Ctrl Pts',(3.57961864506819,-3.4188952610418,11.7009748626909));
#44622=CARTESIAN_POINT('Ctrl Pts',(2.45310593490382,-4.59836570202334,11.6482114218307));
#44623=CARTESIAN_POINT('Ctrl Pts',(0.686399367052665,-5.16638672248939,
11.5954479809705));
#44624=CARTESIAN_POINT('Ctrl Pts',(-0.916412232973623,-4.86443245089807,
11.5426845401103));
#44625=CARTESIAN_POINT('Ctrl Pts',(-2.51922383299994,-4.56247817930674,
11.4899210992501));
#44626=CARTESIAN_POINT('Ctrl Pts',(-3.95814046520138,-3.39054861565802,
11.4371576583899));
#44627=CARTESIAN_POINT('Ctrl Pts',(-4.57826175967478,-1.88202914695641,
11.3843942175297));
#44628=CARTESIAN_POINT('Ctrl Pts',(-4.82144315925703,-1.29046120861066,
11.3637029632387));
#44629=CARTESIAN_POINT('Ctrl Pts',(-4.93870801968536,-0.647131573531266,
11.3430117089478));
#44630=CARTESIAN_POINT('Ctrl Pts',(-4.93550942083981,-0.00268364051190351,
11.3223204546569));
#44631=CARTESIAN_POINT('Ctrl Pts',(-4.93464332849729,-0.00183839903596135,
11.1776795453431));
#44632=CARTESIAN_POINT('Ctrl Pts',(-4.93701583263233,-0.707935706243941,
11.200340240266));
#44633=CARTESIAN_POINT('Ctrl Pts',(-4.79546387301719,-1.41312576132387,
11.223000935189));
#44634=CARTESIAN_POINT('Ctrl Pts',(-4.50527725011862,-2.05066194500317,
11.2456616301119));
#44635=CARTESIAN_POINT('Ctrl Pts',(-3.82917937219074,-3.53604006678678,
11.2984581635866));
#44636=CARTESIAN_POINT('Ctrl Pts',(-2.34624697134931,-4.65417223228435,
11.3512546970613));
#44637=CARTESIAN_POINT('Ctrl Pts',(-0.732189317617651,-4.89557313460714,
11.404051230536));
#44638=CARTESIAN_POINT('Ctrl Pts',(0.881868336113988,-5.13697403692992,
11.4568477640108));
#44639=CARTESIAN_POINT('Ctrl Pts',(2.62705124273586,-4.50164367607793,11.5096442974855));
#44640=CARTESIAN_POINT('Ctrl Pts',(3.70815372246008,-3.27907509577412,11.5624408309602));
#44641=CARTESIAN_POINT('Ctrl Pts',(4.78925620218431,-2.05650651547028,11.6152373644349));
#44642=CARTESIAN_POINT('Ctrl Pts',(5.20627825501086,-0.246699715714593,
11.6680338979096));
#44643=CARTESIAN_POINT('Ctrl Pts',(4.76920065502008,1.32569326213742,11.7208304313843));
#44644=CARTESIAN_POINT('Ctrl Pts',(4.33212305502932,2.89808623998941,11.773626964859));
#44645=CARTESIAN_POINT('Ctrl Pts',(3.04094580222125,4.23306539593773,11.8264234983337));
#44646=CARTESIAN_POINT('Ctrl Pts',(1.48400349530759,4.72233746560275,11.8792200318084));
#44647=CARTESIAN_POINT('Ctrl Pts',(-0.0729388116060994,5.21160953526778,
11.9320165652831));
#44648=CARTESIAN_POINT('Ctrl Pts',(-1.89564617262539,4.85517451864949,11.9848130987578));
#44649=CARTESIAN_POINT('Ctrl Pts',(-3.15358830890438,3.81544470423333,12.0376096322325));
#44650=CARTESIAN_POINT('Ctrl Pts',(-4.26603410872305,2.89597231227191,12.0842996032694));
#44651=CARTESIAN_POINT('Ctrl Pts',(-4.93680336098554,1.44212692063929,12.1309895743062));
#44652=CARTESIAN_POINT('Ctrl Pts',(-4.94745353480859,-0.00311052193284108,
12.1776795453431));
#44653=CARTESIAN_POINT('Origin',(0.,0.,0.));
#44654=CARTESIAN_POINT('',(-4.94151427280004,0.00444821020356132,13.3223204546569));
#44655=CARTESIAN_POINT('',(-4.94372929093918,0.00429917225691094,13.1776795453431));
#44656=CARTESIAN_POINT('',(-4.942,-6.05220448138622E-16,0.));
#44657=CARTESIAN_POINT('Ctrl Pts',(-4.94151427280004,0.00444821020356132,
13.3223204546569));
#44658=CARTESIAN_POINT('Ctrl Pts',(-4.94510334294322,0.402329751972593,
13.3095063326037));
#44659=CARTESIAN_POINT('Ctrl Pts',(-4.90105411066494,0.799426659282486,
13.2966922105506));
#44660=CARTESIAN_POINT('Ctrl Pts',(-4.80630608075059,1.18403391346491,13.2838780884974));
#44661=CARTESIAN_POINT('Ctrl Pts',(-4.41617150483,2.76769310027955,13.2311146476372));
#44662=CARTESIAN_POINT('Ctrl Pts',(-3.16645719817481,4.13959474701713,13.178351206777));
#44663=CARTESIAN_POINT('Ctrl Pts',(-1.62595105536246,4.67533930486966,13.1255877659167));
#44664=CARTESIAN_POINT('Ctrl Pts',(-0.0854449125500667,5.21108386272221,
13.0728243250565));
#44665=CARTESIAN_POINT('Ctrl Pts',(1.74585306641946,4.91067133168968,13.0200608841963));
#44666=CARTESIAN_POINT('Ctrl Pts',(3.03445628684691,3.91082977043353,12.9672974433361));
#44667=CARTESIAN_POINT('Ctrl Pts',(4.3230595072743,2.91098820917742,12.9145340024759));
#44668=CARTESIAN_POINT('Ctrl Pts',(5.06896796915959,1.21171761769772,12.8617705616157));
#44669=CARTESIAN_POINT('Ctrl Pts',(4.9326931179398,-0.41358560700714,12.8090071207555));
#44670=CARTESIAN_POINT('Ctrl Pts',(4.79641826672,-2.03888883171205,12.7562436798952));
#44671=CARTESIAN_POINT('Ctrl Pts',(3.77796010239502,-3.59022468964221,12.703480239035));
#44672=CARTESIAN_POINT('Ctrl Pts',(2.34085390812233,-4.36152696093034,12.6507167981748));
#44673=CARTESIAN_POINT('Ctrl Pts',(0.903747713849633,-5.13282923221848,
12.5979533573146));
#44674=CARTESIAN_POINT('Ctrl Pts',(-0.952006510370724,-5.12409791686467,
12.5451899164544));
#44675=CARTESIAN_POINT('Ctrl Pts',(-2.38179129282902,-4.33930693630882,
12.4924264755942));
#44676=CARTESIAN_POINT('Ctrl Pts',(-3.81157607528729,-3.55451595575297,
12.4396630347339));
#44677=CARTESIAN_POINT('Ctrl Pts',(-4.81539141598345,-1.99366530999509,
12.3868995938737));
#44678=CARTESIAN_POINT('Ctrl Pts',(-4.93636648360977,-0.367151725568608,
12.3341361530135));
#44679=CARTESIAN_POINT('Ctrl Pts',(-4.94539675712518,-0.245739414485935,
12.3301975868946));
#44680=CARTESIAN_POINT('Ctrl Pts',(-4.94950785648002,-0.123961230389695,
12.3262590207758));
#44681=CARTESIAN_POINT('Ctrl Pts',(-4.9488440041135,-0.00213750530709822,
12.3223204546569));
#44682=CARTESIAN_POINT('Ctrl Pts',(-4.94745353480859,-0.00311052193284108,
12.1776795453431));
#44683=CARTESIAN_POINT('Ctrl Pts',(-4.94884646673765,-0.192132542820318,
12.1837861077809));
#44684=CARTESIAN_POINT('Ctrl Pts',(-4.93894745560412,-0.381007316833933,
12.1898926702188));
#44685=CARTESIAN_POINT('Ctrl Pts',(-4.91726778514412,-0.568520045648731,
12.1959992326566));
#44686=CARTESIAN_POINT('Ctrl Pts',(-4.72982821356618,-2.18973036890068,
12.2487957661313));
#44687=CARTESIAN_POINT('Ctrl Pts',(-3.6617721588716,-3.70912640319057,12.301592299606));
#44688=CARTESIAN_POINT('Ctrl Pts',(-2.19976737250484,-4.4343839504472,12.3543888330807));
#44689=CARTESIAN_POINT('Ctrl Pts',(-0.737762586138102,-5.15964149770382,
12.4071853665554));
#44690=CARTESIAN_POINT('Ctrl Pts',(1.1181909319008,-5.09076055792721,12.4599819000301));
#44691=CARTESIAN_POINT('Ctrl Pts',(2.52241404198307,-4.25912724791444,12.5127784335048));
#44692=CARTESIAN_POINT('Ctrl Pts',(3.92663715206537,-3.42749393790165,12.5655749669795));
#44693=CARTESIAN_POINT('Ctrl Pts',(4.87912985419102,-1.83310825765268,12.6183715004542));
#44694=CARTESIAN_POINT('Ctrl Pts',(4.94588170520655,-0.202463999821435,
12.6711680339289));
#44695=CARTESIAN_POINT('Ctrl Pts',(5.01263355622208,1.42818025800979,12.7239645674036));
#44696=CARTESIAN_POINT('Ctrl Pts',(4.1936445561275,3.09508309342328,12.7767611008784));
#44697=CARTESIAN_POINT('Ctrl Pts',(2.86209318500527,4.03870772815599,12.8295576343531));
#44698=CARTESIAN_POINT('Ctrl Pts',(1.53054181388302,4.98233236288871,12.8823541678278));
#44699=CARTESIAN_POINT('Ctrl Pts',(-0.313571928266912,5.20267879694063,
12.9351507013025));
#44700=CARTESIAN_POINT('Ctrl Pts',(-1.82996378449454,4.59934452509909,12.9879472347772));
#44701=CARTESIAN_POINT('Ctrl Pts',(-3.34635564072214,3.99601025325757,13.0407437682519));
#44702=CARTESIAN_POINT('Ctrl Pts',(-4.53502561102745,2.56899527552262,13.0935403017266));
#44703=CARTESIAN_POINT('Ctrl Pts',(-4.85434730874721,0.968529668713999,
13.1463368352013));
#44704=CARTESIAN_POINT('Ctrl Pts',(-4.917535847558,0.651823714081653,13.1567844052486));
#44705=CARTESIAN_POINT('Ctrl Pts',(-4.94668250438369,0.328325791222804,
13.1672319752958));
#44706=CARTESIAN_POINT('Ctrl Pts',(-4.94372929093918,0.00429917225691095,
13.1776795453431));
#44707=CARTESIAN_POINT('Origin',(0.,0.,0.));
#44708=CARTESIAN_POINT('',(-4.93448587773112,-0.00157506815688546,14.3223204546569));
#44709=CARTESIAN_POINT('',(-4.93400159721632,-0.000305393655117946,14.1776795453431));
#44710=CARTESIAN_POINT('',(-4.942,-6.05220448138622E-16,0.));
#44711=CARTESIAN_POINT('Ctrl Pts',(-4.93448587773112,-0.00157506815688546,
14.3223204546569));
#44712=CARTESIAN_POINT('Ctrl Pts',(-4.9318360603942,0.919788438910237,14.2927536444317));
#44713=CARTESIAN_POINT('Ctrl Pts',(-4.68434909382344,1.84247391790569,14.2631868342065));
#44714=CARTESIAN_POINT('Ctrl Pts',(-4.20094243104244,2.61812855704659,14.2336200239813));
#44715=CARTESIAN_POINT('Ctrl Pts',(-3.3382792398224,4.00232277240241,14.180856583121));
#44716=CARTESIAN_POINT('Ctrl Pts',(-1.72430206586684,4.91828000860559,14.1280931422608));
#44717=CARTESIAN_POINT('Ctrl Pts',(-0.0935873430086671,4.94911667465072,
14.0753297014006));
#44718=CARTESIAN_POINT('Ctrl Pts',(1.53712737984951,4.97995334069586,14.0225662605404));
#44719=CARTESIAN_POINT('Ctrl Pts',(3.18457965161027,4.12566943658293,13.9698028196802));
#44720=CARTESIAN_POINT('Ctrl Pts',(4.09895737196505,2.77507890210349,13.91703937882));
#44721=CARTESIAN_POINT('Ctrl Pts',(5.01333509231982,1.42448836762405,13.8642759379598));
#44722=CARTESIAN_POINT('Ctrl Pts',(5.19463826126858,-0.422408797221965,
13.8115124970995));
#44723=CARTESIAN_POINT('Ctrl Pts',(4.56034958089476,-1.92502627258323,13.7587490562393));
#44724=CARTESIAN_POINT('Ctrl Pts',(3.92606090052093,-3.42764374794451,13.7059856153791));
#44725=CARTESIAN_POINT('Ctrl Pts',(2.47618037082453,-4.58598153382108,13.6532221745189));
#44726=CARTESIAN_POINT('Ctrl Pts',(0.870598407947765,-4.87284032799863,
13.6004587336587));
#44727=CARTESIAN_POINT('Ctrl Pts',(-0.734983554928979,-5.15969912217617,
13.5476952927985));
#44728=CARTESIAN_POINT('Ctrl Pts',(-2.49626695098606,-4.57507892465472,
13.4949318519383));
#44729=CARTESIAN_POINT('Ctrl Pts',(-3.61163122642161,-3.38506046244813,
13.442168411078));
#44730=CARTESIAN_POINT('Ctrl Pts',(-4.45611828600162,-2.48404972171741,
13.402219092271));
#44731=CARTESIAN_POINT('Ctrl Pts',(-4.93032498439027,-1.23598765372993,
13.3622697734639));
#44732=CARTESIAN_POINT('Ctrl Pts',(-4.94151427280004,0.00444821020356132,
13.3223204546569));
#44733=CARTESIAN_POINT('Ctrl Pts',(-4.94372929093918,0.00429917225691095,
13.1776795453431));
#44734=CARTESIAN_POINT('Ctrl Pts',(-4.93175851423331,-1.30913460937943,
13.2200285087705));
#44735=CARTESIAN_POINT('Ctrl Pts',(-4.39236571089229,-2.63125521653574,
13.262377472198));
#44736=CARTESIAN_POINT('Ctrl Pts',(-3.45489131803353,-3.54492080217556,
13.3047264356254));
#44737=CARTESIAN_POINT('Ctrl Pts',(-2.28614020446586,-4.68398943037421,
13.3575229691001));
#44738=CARTESIAN_POINT('Ctrl Pts',(-0.498664552196314,-5.18821045088918,
13.4103195025748));
#44739=CARTESIAN_POINT('Ctrl Pts',(1.09305895224904,-4.82783177420557,13.4631160360495));
#44740=CARTESIAN_POINT('Ctrl Pts',(2.68478245669437,-4.46745309752197,13.5159125695242));
#44741=CARTESIAN_POINT('Ctrl Pts',(4.08075381331552,-3.2424747236398,13.5687091029989));
#44742=CARTESIAN_POINT('Ctrl Pts',(4.64488820407174,-1.71106723561516,13.6215056364736));
#44743=CARTESIAN_POINT('Ctrl Pts',(5.20902259482797,-0.179659747590474,
13.6743021699483));
#44744=CARTESIAN_POINT('Ctrl Pts',(4.94132001971923,1.6581768545767,13.727098703423));
#44745=CARTESIAN_POINT('Ctrl Pts',(3.9637611647886,2.96501853984655,13.7798952368977));
#44746=CARTESIAN_POINT('Ctrl Pts',(2.98620230985801,4.27186022511634,13.8326917703724));
#44747=CARTESIAN_POINT('Ctrl Pts',(1.29878717510559,5.04770699348884,13.8854883038471));
#44748=CARTESIAN_POINT('Ctrl Pts',(-0.32960087817538,4.93903844632007,13.9382848373218));
#44749=CARTESIAN_POINT('Ctrl Pts',(-1.95798893145639,4.8303698991513,13.9910813707965));
#44750=CARTESIAN_POINT('Ctrl Pts',(-3.52734990326595,3.8371860364412,14.0438779042712));
#44751=CARTESIAN_POINT('Ctrl Pts',(-4.32259269702876,2.41203853383676,14.0966744377459));
#44752=CARTESIAN_POINT('Ctrl Pts',(-4.72930328852039,1.68317611811527,14.1236761402783));
#44753=CARTESIAN_POINT('Ctrl Pts',(-4.93353545879958,0.841329253368597,
14.1506778428107));
#44754=CARTESIAN_POINT('Ctrl Pts',(-4.93400159721632,-0.000305393655117946,
14.1776795453431));
#44755=CARTESIAN_POINT('Origin',(0.,0.,0.));
#44756=CARTESIAN_POINT('',(-4.94718090754756,-0.00323194414963146,15.3223204546569));
#44757=CARTESIAN_POINT('',(-4.9448369857261,-0.0040807615555026,15.1776795453431));
#44758=CARTESIAN_POINT('',(-4.942,-6.05220448138622E-16,0.));
#44759=CARTESIAN_POINT('Ctrl Pts',(-4.94718090754756,-0.00323194414963146,
15.3223204546569));
#44760=CARTESIAN_POINT('Ctrl Pts',(-4.93629962156844,1.4307451373895,15.2760009562597));
#44761=CARTESIAN_POINT('Ctrl Pts',(-4.27737587184649,2.87344030248637,15.2296814578624));
#44762=CARTESIAN_POINT('Ctrl Pts',(-3.18014090814091,3.79331230684891,15.1833619594651));
#44763=CARTESIAN_POINT('Ctrl Pts',(-1.93025923583274,4.84115638505733,15.1305985186049));
#44764=CARTESIAN_POINT('Ctrl Pts',(-0.111627961864901,5.21058874364864,
15.0778350777447));
#44765=CARTESIAN_POINT('Ctrl Pts',(1.44803137056367,4.73346803090561,15.0250716368845));
#44766=CARTESIAN_POINT('Ctrl Pts',(3.00769070299228,4.25634731816257,14.9723081960243));
#44767=CARTESIAN_POINT('Ctrl Pts',(4.30837809388161,2.93267353408514,14.9195447551641));
#44768=CARTESIAN_POINT('Ctrl Pts',(4.75810604814116,1.36489607082845,14.8667813143038));
#44769=CARTESIAN_POINT('Ctrl Pts',(5.20783400240071,-0.202881392428214,
14.8140178734436));
#44770=CARTESIAN_POINT('Ctrl Pts',(4.80660252003052,-2.01476253486414,14.7612544325834));
#44771=CARTESIAN_POINT('Ctrl Pts',(3.73702582619445,-3.2460980306936,14.7084909917232));
#44772=CARTESIAN_POINT('Ctrl Pts',(2.66744913235836,-4.47743352652308,14.655727550863));
#44773=CARTESIAN_POINT('Ctrl Pts',(0.929527227056376,-5.12822337574609,
14.6029641100028));
#44774=CARTESIAN_POINT('Ctrl Pts',(-0.685751952425607,-4.90227077075043,
14.5502006691425));
#44775=CARTESIAN_POINT('Ctrl Pts',(-2.30103113190757,-4.67631816575478,
14.4974372282823));
#44776=CARTESIAN_POINT('Ctrl Pts',(-3.79366758556953,-3.57362310654048,
14.4446737874221));
#44777=CARTESIAN_POINT('Ctrl Pts',(-4.48431120815826,-2.09605997967911,
14.3919103465619));
#44778=CARTESIAN_POINT('Ctrl Pts',(-4.78794199402862,-1.44647220574097,
14.3687137159269));
#44779=CARTESIAN_POINT('Ctrl Pts',(-4.93656479099726,-0.724430485809702,
14.3455170852919));
#44780=CARTESIAN_POINT('Ctrl Pts',(-4.93448587773112,-0.00157506815688546,
14.3223204546569));
#44781=CARTESIAN_POINT('Ctrl Pts',(-4.93400159721632,-0.000305393655117946,
14.1776795453431));
#44782=CARTESIAN_POINT('Ctrl Pts',(-4.93444690105008,-0.804322229598714,
14.2034743762854));
#44783=CARTESIAN_POINT('Ctrl Pts',(-4.74893420650715,-1.60814539448429,
14.2292692072277));
#44784=CARTESIAN_POINT('Ctrl Pts',(-4.37634095459745,-2.31308827376533,
14.2550640381701));
#44785=CARTESIAN_POINT('Ctrl Pts',(-3.61372180268731,-3.75595643626419,
14.3078605716448));
#44786=CARTESIAN_POINT('Ctrl Pts',(-2.06735888315097,-4.78458161876317,
14.3606571051195));
#44787=CARTESIAN_POINT('Ctrl Pts',(-0.44186405756573,-4.93026304245127,
14.4134536385942));
#44788=CARTESIAN_POINT('Ctrl Pts',(1.18363076801951,-5.07594446613938,14.4662501720689));
#44789=CARTESIAN_POINT('Ctrl Pts',(2.88825749965368,-4.33868213101661,14.5190467055436));
#44790=CARTESIAN_POINT('Ctrl Pts',(3.89529018284092,-3.05441514934954,14.5718432390183));
#44791=CARTESIAN_POINT('Ctrl Pts',(4.90232286602818,-1.77014816768244,14.624639772493));
#44792=CARTESIAN_POINT('Ctrl Pts',(5.21176150076849,0.0611234605289337,
14.6774363059677));
#44793=CARTESIAN_POINT('Ctrl Pts',(4.682608052441,1.60496708387405,14.7302328394424));
#44794=CARTESIAN_POINT('Ctrl Pts',(4.15345460411353,3.1488107072191,14.7830293729171));
#44795=CARTESIAN_POINT('Ctrl Pts',(2.78570907271829,4.40522632569788,14.8358259063918));
#44796=CARTESIAN_POINT('Ctrl Pts',(1.20259496734194,4.80171873996239,14.8886224398665));
#44797=CARTESIAN_POINT('Ctrl Pts',(-0.380519138034476,5.19821115422692,
14.9414189733412));
#44798=CARTESIAN_POINT('Ctrl Pts',(-2.17900181739205,4.73478036427711,14.9942155068159));
#44799=CARTESIAN_POINT('Ctrl Pts',(-3.3733609497546,3.62259208519558,15.0470120402906));
#44800=CARTESIAN_POINT('Ctrl Pts',(-4.35867771010103,2.70506424759102,15.0905678753081));
#44801=CARTESIAN_POINT('Ctrl Pts',(-4.93283752130763,1.34600230443831,15.1341237103256));
#44802=CARTESIAN_POINT('Ctrl Pts',(-4.9448369857261,-0.0040807615555026,
15.1776795453431));
#44803=CARTESIAN_POINT('Origin',(0.,0.,0.));
#44804=CARTESIAN_POINT('',(-4.94384666289092,0.00426556420662083,16.3223204546569));
#44805=CARTESIAN_POINT('',(-4.94650740111161,0.00354971811832453,16.1776795453431));
#44806=CARTESIAN_POINT('',(-4.942,-6.05220448138622E-16,0.));
#44807=CARTESIAN_POINT('Ctrl Pts',(-4.94384666289092,0.00426556420662083,
16.3223204546569));
#44808=CARTESIAN_POINT('Ctrl Pts',(-4.94674943417405,0.323967179430384,
16.3120117089478));
#44809=CARTESIAN_POINT('Ctrl Pts',(-4.91837466800284,0.643155833620532,
16.3017029632387));
#44810=CARTESIAN_POINT('Ctrl Pts',(-4.85684297990262,0.955819257318147,
16.2913942175296));
#44811=CARTESIAN_POINT('Ctrl Pts',(-4.5419042203555,2.55613015167716,16.2386307766694));
#44812=CARTESIAN_POINT('Ctrl Pts',(-3.35834756654112,3.98549839996768,16.1858673358092));
#44813=CARTESIAN_POINT('Ctrl Pts',(-1.84485020909617,4.59336938114029,16.133103894949));
#44814=CARTESIAN_POINT('Ctrl Pts',(-0.331352851651252,5.20124036231289,
16.0803404540888));
#44815=CARTESIAN_POINT('Ctrl Pts',(1.51208520942422,4.98761407636759,16.0275770132286));
#44816=CARTESIAN_POINT('Ctrl Pts',(2.84645196705723,4.04971920709069,15.9748135723683));
#44817=CARTESIAN_POINT('Ctrl Pts',(4.18081872469025,3.11182433781378,15.9220501315081));
#44818=CARTESIAN_POINT('Ctrl Pts',(5.00611417888079,1.44966088520527,15.8692866906479));
#44819=CARTESIAN_POINT('Ctrl Pts',(4.94671805190497,-0.180263500133812,
15.8165232497877));
#44820=CARTESIAN_POINT('Ctrl Pts',(4.88732192492914,-1.81018788547292,15.7637598089275));
#44821=CARTESIAN_POINT('Ctrl Pts',(3.94323421678691,-3.40787320354259,15.7109963680673));
#44822=CARTESIAN_POINT('Ctrl Pts',(2.54414165016166,-4.24615799663446,15.6582329272071));
#44823=CARTESIAN_POINT('Ctrl Pts',(1.14504908353641,-5.08444278972633,15.6054694863468));
#44824=CARTESIAN_POINT('Ctrl Pts',(-0.709048341571857,-5.16332705784039,
15.5527060454866));
#44825=CARTESIAN_POINT('Ctrl Pts',(-2.17428721330366,-4.44690786540681,
15.4999426046264));
#44826=CARTESIAN_POINT('Ctrl Pts',(-3.63952608503543,-3.73048867297323,
15.4471791637662));
#44827=CARTESIAN_POINT('Ctrl Pts',(-4.71590640339076,-2.21876601999203,
15.394415722906));
#44828=CARTESIAN_POINT('Ctrl Pts',(-4.91353052724419,-0.59977679458864,
15.3416522820458));
#44829=CARTESIAN_POINT('Ctrl Pts',(-4.93766614961155,-0.402051376257967,
15.3352083395828));
#44830=CARTESIAN_POINT('Ctrl Pts',(-4.94869470590891,-0.202726026045579,
15.3287643971199));
#44831=CARTESIAN_POINT('Ctrl Pts',(-4.94718090754756,-0.00323194414963146,
15.3223204546569));
#44832=CARTESIAN_POINT('Ctrl Pts',(-4.9448369857261,-0.0040807615555026,
15.1776795453431));
#44833=CARTESIAN_POINT('Ctrl Pts',(-4.94738276248126,-0.290511052698514,
15.1869202438003));
#44834=CARTESIAN_POINT('Ctrl Pts',(-4.92462524198781,-0.576537197232804,
15.1961609422575));
#44835=CARTESIAN_POINT('Ctrl Pts',(-4.8751224347969,-0.857857073631679,
15.2054016407147));
#44836=CARTESIAN_POINT('Ctrl Pts',(-4.59228920210912,-2.46517218516427,
15.2581981741894));
#44837=CARTESIAN_POINT('Ctrl Pts',(-3.436387151366,-3.91885664001626,15.3109947076642));
#44838=CARTESIAN_POINT('Ctrl Pts',(-1.93411172090367,-4.55652821395913,
15.3637912411389));
#44839=CARTESIAN_POINT('Ctrl Pts',(-0.431836290441309,-5.19419978790203,
15.4165877746136));
#44840=CARTESIAN_POINT('Ctrl Pts',(1.41681251974025,-5.01585848093576,15.4693843080882));
#44841=CARTESIAN_POINT('Ctrl Pts',(2.76948401487652,-4.1027668473702,15.522180841563));
#44842=CARTESIAN_POINT('Ctrl Pts',(4.12215551001273,-3.18967521380468,15.5749773750377));
#44843=CARTESIAN_POINT('Ctrl Pts',(4.97884969010367,-1.54183325363995,15.6277739085124));
#44844=CARTESIAN_POINT('Ctrl Pts',(4.94920742712676,0.0899074861556964,
15.6805704419871));
#44845=CARTESIAN_POINT('Ctrl Pts',(4.91956516414985,1.72164822595137,15.7333669754618));
#44846=CARTESIAN_POINT('Ctrl Pts',(4.00358645810502,3.33728774537801,15.7861635089365));
#44847=CARTESIAN_POINT('Ctrl Pts',(2.61864387578884,4.200647779537,15.8389600424112));
#44848=CARTESIAN_POINT('Ctrl Pts',(1.23370129347265,5.06400781369599,15.8917565758859));
#44849=CARTESIAN_POINT('Ctrl Pts',(-0.620205165114908,5.17508836258739,
15.9445531093606));
#44850=CARTESIAN_POINT('Ctrl Pts',(-2.09832911795802,4.48327474299608,15.9973496428353));
#44851=CARTESIAN_POINT('Ctrl Pts',(-3.57645307080114,3.79146112340477,16.05014617631));
#44852=CARTESIAN_POINT('Ctrl Pts',(-4.67879451789979,2.29675333533074,16.1029427097847));
#44853=CARTESIAN_POINT('Ctrl Pts',(-4.90306331235317,0.680226188554136,
16.1557392432594));
#44854=CARTESIAN_POINT('Ctrl Pts',(-4.93412927302912,0.456303065875542,
16.1630526772873));
#44855=CARTESIAN_POINT('Ctrl Pts',(-4.94834669148062,0.23004246166547,16.1703661113152));
#44856=CARTESIAN_POINT('Ctrl Pts',(-4.94650740111161,0.00354971811832453,
16.1776795453431));
#44857=CARTESIAN_POINT('Origin',(0.,0.,0.));
#44858=CARTESIAN_POINT('',(-4.93403031428168,-0.000341981052076612,17.3223204546569));
#44859=CARTESIAN_POINT('',(-4.93428824426153,0.00126466874552048,17.1776795453431));
#44860=CARTESIAN_POINT('',(-4.942,-6.05220448138622E-16,0.));
#44861=CARTESIAN_POINT('Ctrl Pts',(-4.93403031428168,-0.000341981052076612,
17.3223204546569));
#44862=CARTESIAN_POINT('Ctrl Pts',(-4.93350394108414,0.843143514252388,
17.2952590207758));
#44863=CARTESIAN_POINT('Ctrl Pts',(-4.72829119907115,1.68686850434222,17.2681975868947));
#44864=CARTESIAN_POINT('Ctrl Pts',(-4.31985335744029,2.41689215977968,17.2411361530135));
#44865=CARTESIAN_POINT('Ctrl Pts',(-3.52349548532491,3.84026684640702,17.1883727121533));
#44866=CARTESIAN_POINT('Ctrl Pts',(-1.9545602926493,4.83139633972401,17.1356092712931));
#44867=CARTESIAN_POINT('Ctrl Pts',(-0.327119944589159,4.9391812045894,17.0828458304329));
#44868=CARTESIAN_POINT('Ctrl Pts',(1.30032040347096,5.04696606945479,17.0300823895727));
#44869=CARTESIAN_POINT('Ctrl Pts',(2.98626590691563,4.2714063058686,16.9773189487124));
#44870=CARTESIAN_POINT('Ctrl Pts',(3.96338272054503,2.96548703306019,16.9245555078522));
#44871=CARTESIAN_POINT('Ctrl Pts',(4.94049953417446,1.65956776025175,16.871792066992));
#44872=CARTESIAN_POINT('Ctrl Pts',(5.20878765798859,-0.176711021778891,
16.8190286261318));
#44873=CARTESIAN_POINT('Ctrl Pts',(4.64614108062899,-1.70759643201752,16.7662651852716));
#44874=CARTESIAN_POINT('Ctrl Pts',(4.0834945032694,-3.2384818422561,16.7135017444114));
#44875=CARTESIAN_POINT('Ctrl Pts',(2.68991322473609,-4.46397388070265,16.6607383035511));
#44876=CARTESIAN_POINT('Ctrl Pts',(1.09966334943406,-4.82630869971703,16.6079748626909));
#44877=CARTESIAN_POINT('Ctrl Pts',(-0.490586525867957,-5.18864351873141,
16.5552114218307));
#44878=CARTESIAN_POINT('Ctrl Pts',(-2.27750499793871,-4.68782111831362,
16.5024479809705));
#44879=CARTESIAN_POINT('Ctrl Pts',(-3.44780380133416,-3.551783147891,16.4496845401103));
#44880=CARTESIAN_POINT('Ctrl Pts',(-4.38945351416312,-2.63770050035899,
16.4072298449592));
#44881=CARTESIAN_POINT('Ctrl Pts',(-4.93189212706316,-1.31236741876541,
16.364775149808));
#44882=CARTESIAN_POINT('Ctrl Pts',(-4.94384666289092,0.00426556420662083,
16.3223204546569));
#44883=CARTESIAN_POINT('Ctrl Pts',(-4.94650740111161,0.00354971811832453,
16.1776795453431));
#44884=CARTESIAN_POINT('Ctrl Pts',(-4.93506863972457,-1.40503507794796,
16.2231626447899));
#44885=CARTESIAN_POINT('Ctrl Pts',(-4.30259793428105,-2.82259842281934,
16.2686457442367));
#44886=CARTESIAN_POINT('Ctrl Pts',(-3.23956236772638,-3.74272269838241,
16.3141288436835));
#44887=CARTESIAN_POINT('Ctrl Pts',(-2.00559648683807,-4.81079793306321,
16.3669253771582));
#44888=CARTESIAN_POINT('Ctrl Pts',(-0.191468583253334,-5.20860189694556,
16.4197219106329));
#44889=CARTESIAN_POINT('Ctrl Pts',(1.37620035566145,-4.75487224416495,16.4725184441076));
#44890=CARTESIAN_POINT('Ctrl Pts',(2.94386929457619,-4.30114259138436,16.5253149775823));
#44891=CARTESIAN_POINT('Ctrl Pts',(4.265079268821,-2.99587932194087,16.578111511057));
#44892=CARTESIAN_POINT('Ctrl Pts',(4.73781104997921,-1.43383540748133,16.6309080445317));
#44893=CARTESIAN_POINT('Ctrl Pts',(5.21054283113743,0.128208506978224,16.6837045780064));
#44894=CARTESIAN_POINT('Ctrl Pts',(4.83479641920902,1.94703306645383,16.7365011114811));
#44895=CARTESIAN_POINT('Ctrl Pts',(3.78178347511922,3.19387716968194,16.7892976449558));
#44896=CARTESIAN_POINT('Ctrl Pts',(2.72877053102942,4.44072127291004,16.8420941784306));
#44897=CARTESIAN_POINT('Ctrl Pts',(0.998491054778278,5.11558491989063,16.8948907119053));
#44898=CARTESIAN_POINT('Ctrl Pts',(-0.620640115192454,4.91096152429156,
16.94768724538));
#44899=CARTESIAN_POINT('Ctrl Pts',(-2.23977128516316,4.70633812869249,17.0004837788547));
#44900=CARTESIAN_POINT('Ctrl Pts',(-3.74775414885348,3.62222769051368,17.0532803123294));
#44901=CARTESIAN_POINT('Ctrl Pts',(-4.45746504028889,2.1526130784761,17.1060768458041));
#44902=CARTESIAN_POINT('Ctrl Pts',(-4.77830186027552,1.48824892058866,17.1299444123171));
#44903=CARTESIAN_POINT('Ctrl Pts',(-4.93600022440261,0.745101393327629,
17.1538119788301));
#44904=CARTESIAN_POINT('Ctrl Pts',(-4.93428824426153,0.00126466874552048,
17.1776795453431));
#44905=CARTESIAN_POINT('Origin',(0.,0.,0.));
#44906=CARTESIAN_POINT('',(-4.94522242777803,-0.0039236424385497,18.3223204546569));
#44907=CARTESIAN_POINT('',(-4.94192999916445,-0.00446510791632448,18.1776795453431));
#44908=CARTESIAN_POINT('',(-4.942,-6.05220448138622E-16,0.));
#44909=CARTESIAN_POINT('Ctrl Pts',(-4.94522242777803,-0.0039236424385497,
18.3223204546569));
#44910=CARTESIAN_POINT('Ctrl Pts',(-4.93329330491003,1.35399213993734,18.2785063326037));
#44911=CARTESIAN_POINT('Ctrl Pts',(-4.3513066594067,2.72080403156538,18.2346922105506));
#44912=CARTESIAN_POINT('Ctrl Pts',(-3.35561026819536,3.63892235657103,18.1908780884974));
#44913=CARTESIAN_POINT('Ctrl Pts',(-2.15653642646331,4.74457230855067,18.1381146476372));
#44914=CARTESIAN_POINT('Ctrl Pts',(-0.35748677154393,5.19951173147208,18.085351206777));
#44915=CARTESIAN_POINT('Ctrl Pts',(1.22293027595834,4.79656649826054,18.0325877659168));
#44916=CARTESIAN_POINT('Ctrl Pts',(2.80334732346066,4.39362126504898,17.9798243250565));
#44917=CARTESIAN_POINT('Ctrl Pts',(4.16513176354582,3.13279137570437,17.9270608841963));
#44918=CARTESIAN_POINT('Ctrl Pts',(4.68838366687364,1.58798426669984,17.8742974433361));
#44919=CARTESIAN_POINT('Ctrl Pts',(5.21163557020145,0.0431771576953521,
17.8215340024759));
#44920=CARTESIAN_POINT('Ctrl Pts',(4.89635493677199,-1.78560717096906,17.7687705616157));
#44921=CARTESIAN_POINT('Ctrl Pts',(3.88609177304056,-3.06605780050668,17.7160071207555));
#44922=CARTESIAN_POINT('Ctrl Pts',(2.87582860930912,-4.34650843004432,17.6632436798953));
#44923=CARTESIAN_POINT('Ctrl Pts',(1.17058291527568,-5.07862536045516,17.610480239035));
#44924=CARTESIAN_POINT('Ctrl Pts',(-0.453558190725748,-4.92918049163674,
17.5577167981748));
#44925=CARTESIAN_POINT('Ctrl Pts',(-2.0776992967272,-4.77973562281832,17.5049533573146));
#44926=CARTESIAN_POINT('Ctrl Pts',(-3.62073581469659,-3.74872895477065,
17.4521899164544));
#44927=CARTESIAN_POINT('Ctrl Pts',(-4.38036379790372,-2.30541568077795,
17.3994264755942));
#44928=CARTESIAN_POINT('Ctrl Pts',(-4.75039204866972,-1.6023522103828,17.3737244686151));
#44929=CARTESIAN_POINT('Ctrl Pts',(-4.93453024520391,-0.801455114314277,
17.348022461636));
#44930=CARTESIAN_POINT('Ctrl Pts',(-4.93403031428168,-0.000341981052076612,
17.3223204546569));
#44931=CARTESIAN_POINT('Ctrl Pts',(-4.93428824426153,0.00126466874552048,
17.1776795453431));
#44932=CARTESIAN_POINT('Ctrl Pts',(-4.93221321843459,-0.900311452079429,
17.2066085123048));
#44933=CARTESIAN_POINT('Ctrl Pts',(-4.69594942149747,-1.80290006851385,
17.2355374792665));
#44934=CARTESIAN_POINT('Ctrl Pts',(-4.23213525097133,-2.56744414176908,
17.2644664462282));
#44935=CARTESIAN_POINT('Ctrl Pts',(-3.38565565103777,-3.96276796408032,
17.3172629797029));
#44936=CARTESIAN_POINT('Ctrl Pts',(-1.78125753199004,-4.89829682280636,
17.3700595131776));
#44937=CARTESIAN_POINT('Ctrl Pts',(-0.149997058388728,-4.94775064594635,
17.4228560466523));
#44938=CARTESIAN_POINT('Ctrl Pts',(1.48126341521252,-4.99720446908635,17.475652580127));
#44939=CARTESIAN_POINT('Ctrl Pts',(3.13938624336737,-4.16058325664038,17.5284491136017));
#44940=CARTESIAN_POINT('Ctrl Pts',(4.06883557073125,-2.81909846013186,17.5812456470764));
#44941=CARTESIAN_POINT('Ctrl Pts',(4.99828489809513,-1.47761366362332,17.6340421805511));
#44942=CARTESIAN_POINT('Ctrl Pts',(5.19906072466804,0.368734716947733,17.6868387140258));
#44943=CARTESIAN_POINT('Ctrl Pts',(4.57967756755998,1.87864175098721,17.7396352475005));
#44944=CARTESIAN_POINT('Ctrl Pts',(3.9602944104519,3.38854878502672,17.7924317809752));
#44945=CARTESIAN_POINT('Ctrl Pts',(2.52075226966277,4.56201447253459,17.8452283144499));
#44946=CARTESIAN_POINT('Ctrl Pts',(0.916990219673444,4.86434504442812,17.8980248479246));
#44947=CARTESIAN_POINT('Ctrl Pts',(-0.68677183031584,5.16667561632164,17.9508213813993));
#44948=CARTESIAN_POINT('Ctrl Pts',(-2.45475378950534,4.59787107260088,18.003617914874));
#44949=CARTESIAN_POINT('Ctrl Pts',(-3.58136314295608,3.4171025376229,18.0564144483487));
#44950=CARTESIAN_POINT('Ctrl Pts',(-4.44390962426003,2.51309109660283,18.0968361473469));
#44951=CARTESIAN_POINT('Ctrl Pts',(-4.93050729338922,1.25036908149785,18.137257846345));
#44952=CARTESIAN_POINT('Ctrl Pts',(-4.94192999916445,-0.00446510791632448,
18.1776795453431));
#44953=CARTESIAN_POINT('Origin',(0.,0.,-1.84858989190501));
#44954=CARTESIAN_POINT('',(-4.37485075966118,-0.00347109768167049,18.651410108095));
#44955=CARTESIAN_POINT('',(-4.37798451307649,0.0018411544964702,18.848589891905));
#44956=CARTESIAN_POINT('',(-4.372,-4.40683631492666E-13,-1.84858989190501));
#44957=CARTESIAN_POINT('',(-4.32479004603203,0.640761311052912,19.628));
#44958=CARTESIAN_POINT('Ctrl Pts',(-4.37485075966118,-0.00347109768167011,
18.651410108095));
#44959=CARTESIAN_POINT('Ctrl Pts',(-4.37700632796887,-0.248843725443851,
18.660359426902));
#44960=CARTESIAN_POINT('Ctrl Pts',(-4.24678226663423,-1.93862138449445,
18.7220721865693));
#44961=CARTESIAN_POINT('Ctrl Pts',(-2.04533412033072,-4.73987705500777,
18.8365483870968));
#44962=CARTESIAN_POINT('Ctrl Pts',(2.85792925831606,-4.29723869811459,18.9948387096774));
#44963=CARTESIAN_POINT('Ctrl Pts',(5.16462833680317,0.0542185969503185,
19.1531290322581));
#44964=CARTESIAN_POINT('Ctrl Pts',(2.76051461044002,4.36178489183685,19.3114193548387));
#44965=CARTESIAN_POINT('Ctrl Pts',(-1.32005059452733,4.63359119197125,19.4433279569892));
#44966=CARTESIAN_POINT('Ctrl Pts',(-3.63987183575178,2.72812739966123,19.5488548387097));
#44967=CARTESIAN_POINT('Ctrl Pts',(-4.21857665773145,1.35764386397051,19.6016182795699));
#44968=CARTESIAN_POINT('Ctrl Pts',(-4.32479004603219,0.640761311051878,
19.628));
#44969=CARTESIAN_POINT('',(-0.803308159453264,4.29756675351946,19.628));
#44970=CARTESIAN_POINT('Origin',(0.,0.,19.628));
#44971=CARTESIAN_POINT('Ctrl Pts',(-4.37798451307649,0.00184115449647014,
18.848589891905));
#44972=CARTESIAN_POINT('Ctrl Pts',(-4.37034287302321,-1.32832166361097,
18.8972071273712));
#44973=CARTESIAN_POINT('Ctrl Pts',(-3.01402217294637,-4.11556359956004,
18.9986208963121));
#44974=CARTESIAN_POINT('Ctrl Pts',(1.72525842040716,-4.86940713488401,19.1528311987277));
#44975=CARTESIAN_POINT('Ctrl Pts',(5.02276837180745,-1.19521866677756,19.3112207991518));
#44976=CARTESIAN_POINT('Ctrl Pts',(3.95306672650205,2.75529758855723,19.4432121328385));
#44977=CARTESIAN_POINT('Ctrl Pts',(1.3947178009747,4.32991044428859,19.548805199788));
#44978=CARTESIAN_POINT('Ctrl Pts',(-0.0904913830656236,4.43080762341373,
19.6016017332627));
#44979=CARTESIAN_POINT('Ctrl Pts',(-0.803308159453631,4.29756675351939,
19.628));
#44980=CARTESIAN_POINT('Origin',(0.,0.,-1.84858989190501));
#44981=CARTESIAN_POINT('',(-4.36494952125445,-0.000302537669007011,17.651410108095));
#44982=CARTESIAN_POINT('',(-4.37193807291522,-0.0039501116577445,17.848589891905));
#44983=CARTESIAN_POINT('',(-4.372,-4.40683631492666E-13,-1.84858989190501));
#44984=CARTESIAN_POINT('Ctrl Pts',(-4.36494952125446,-0.000302537669007175,
17.651410108095));
#44985=CARTESIAN_POINT('Ctrl Pts',(-4.36539179118401,-0.709016948559791,
17.6771121150741));
#44986=CARTESIAN_POINT('Ctrl Pts',(-3.86807546336294,-2.87206193474975,
17.7555775629134));
#44987=CARTESIAN_POINT('Ctrl Pts',(-0.472995886023615,-5.14054336213398,
17.8868064516129));
#44988=CARTESIAN_POINT('Ctrl Pts',(4.05270272242283,-3.19751510246813,18.0450967741935));
#44989=CARTESIAN_POINT('Ctrl Pts',(4.88945318540557,1.65605334244537,18.2033870967742));
#44990=CARTESIAN_POINT('Ctrl Pts',(1.27529601904452,5.00227852023644,18.3616774193548));
#44991=CARTESIAN_POINT('Ctrl Pts',(-3.22941067771149,3.86313894204385,18.5110184231284));
#44992=CARTESIAN_POINT('Ctrl Pts',(-4.36429751701074,1.19782550299575,18.6075959860418));
#44993=CARTESIAN_POINT('Ctrl Pts',(-4.37485075966118,-0.00347109768167011,
18.651410108095));
#44994=CARTESIAN_POINT('Ctrl Pts',(-4.37193807291522,-0.00395011165774454,
17.848589891905));
#44995=CARTESIAN_POINT('Ctrl Pts',(-4.37503172333717,-0.34380114135277,
17.8609647263816));
#44996=CARTESIAN_POINT('Ctrl Pts',(-4.18383382909851,-2.13016311819971,
17.9261360943329));
#44997=CARTESIAN_POINT('Ctrl Pts',(-1.7333097832156,-4.86367572142824,18.0441039957589));
#44998=CARTESIAN_POINT('Ctrl Pts',(3.13645552043595,-4.10159948955856,18.202493596183));
#44999=CARTESIAN_POINT('Ctrl Pts',(5.14796384574126,0.398543369117654,18.3608831966071));
#45000=CARTESIAN_POINT('Ctrl Pts',(2.46797524199195,4.53507188733415,18.5192727970312));
#45001=CARTESIAN_POINT('Ctrl Pts',(-2.46096278237594,4.53951629179981,18.6776623974553));
#45002=CARTESIAN_POINT('Ctrl Pts',(-4.32286248336998,1.67443240118537,18.7874347624133));
#45003=CARTESIAN_POINT('Ctrl Pts',(-4.37864141367461,0.116186340178791,
18.8444105938965));
#45004=CARTESIAN_POINT('Ctrl Pts',(-4.37798451307649,0.00184115449647014,
18.848589891905));
#45005=CARTESIAN_POINT('Origin',(0.,0.,-1.84858989190501));
#45006=CARTESIAN_POINT('',(-4.37363367263438,0.00377358290378073,16.651410108095));
#45007=CARTESIAN_POINT('',(-4.36517770212695,0.0011188044825361,16.848589891905));
#45008=CARTESIAN_POINT('',(-4.372,-4.40683631492666E-13,-1.84858989190501));
#45009=CARTESIAN_POINT('Ctrl Pts',(-4.37363367263438,0.00377358290378063,
16.651410108095));
#45010=CARTESIAN_POINT('Ctrl Pts',(-4.36305794810196,-1.16100169057931,
16.6938648032461));
#45011=CARTESIAN_POINT('Ctrl Pts',(-3.28678615689719,-3.7906423093463,16.7890829392575));
#45012=CARTESIAN_POINT('Ctrl Pts',(1.14681571606612,-5.03325475486043,16.937064516129));
#45013=CARTESIAN_POINT('Ctrl Pts',(4.84536125415653,-1.78081574711759,17.0953548387097));
#45014=CARTESIAN_POINT('Ctrl Pts',(4.13332826509411,3.09264287390914,17.2536451612903));
#45015=CARTESIAN_POINT('Ctrl Pts',(-0.341147903092961,5.15096781506579,
17.411935483871));
#45016=CARTESIAN_POINT('Ctrl Pts',(-3.82897189620604,2.94763574423766,17.5445237994725));
#45017=CARTESIAN_POINT('Ctrl Pts',(-4.36448385884661,0.745897095166127,
17.6243486742139));
#45018=CARTESIAN_POINT('Ctrl Pts',(-4.36494952125446,-0.000302537669007175,
17.651410108095));
#45019=CARTESIAN_POINT('Ctrl Pts',(-4.36517770212695,0.0011188044825361,
16.848589891905));
#45020=CARTESIAN_POINT('Ctrl Pts',(-4.36334200546248,-0.796471401961387,
16.8775188588667));
#45021=CARTESIAN_POINT('Ctrl Pts',(-3.77287007871479,-3.05222639411641,
16.9592443593031));
#45022=CARTESIAN_POINT('Ctrl Pts',(-0.156460816144074,-5.16096436253732,
17.0937663932142));
#45023=CARTESIAN_POINT('Ctrl Pts',(4.24417435465306,-2.94058317628852,17.2521559936383));
#45024=CARTESIAN_POINT('Ctrl Pts',(4.7770306357801,1.95960002071087,17.4105455940624));
#45025=CARTESIAN_POINT('Ctrl Pts',(0.956505601666415,5.07396180892462,17.5689351944865));
#45026=CARTESIAN_POINT('Ctrl Pts',(-3.36909691713057,3.68230599805327,17.7149499604341));
#45027=CARTESIAN_POINT('Ctrl Pts',(-4.36183283826352,1.10615411256716,17.8081681929069));
#45028=CARTESIAN_POINT('Ctrl Pts',(-4.37193807291522,-0.00395011165774454,
17.848589891905));
#45029=CARTESIAN_POINT('Origin',(0.,0.,-1.84858989190501));
#45030=CARTESIAN_POINT('',(-4.37658335244799,-0.00285917843438755,15.651410108095));
#45031=CARTESIAN_POINT('',(-4.37598752684337,0.00314030101388529,15.848589891905));
#45032=CARTESIAN_POINT('',(-4.372,-4.40683631492666E-13,-1.84858989190501));
#45033=CARTESIAN_POINT('Ctrl Pts',(-4.37658335244799,-0.00285917843438723,
15.651410108095));
#45034=CARTESIAN_POINT('Ctrl Pts',(-4.37792255245523,-0.179344027897961,
15.657854050558));
#45035=CARTESIAN_POINT('Ctrl Pts',(-4.28827874574891,-1.79952736688815,
15.7170614338811));
#45036=CARTESIAN_POINT('Ctrl Pts',(-2.26751786562628,-4.63758557609733,
15.8290322580645));
#45037=CARTESIAN_POINT('Ctrl Pts',(2.65323118895075,-4.42822781393943,15.9873225806452));
#45038=CARTESIAN_POINT('Ctrl Pts',(5.15882697608013,-0.187992963311806,
16.1456129032258));
#45039=CARTESIAN_POINT('Ctrl Pts',(2.96850419640318,4.22336596918787,16.3039032258064));
#45040=CARTESIAN_POINT('Ctrl Pts',(-1.92395505269964,4.79032719267193,16.4621935483871));
#45041=CARTESIAN_POINT('Ctrl Pts',(-4.22261913325801,2.01425606870238,16.5780291758166));
#45042=CARTESIAN_POINT('Ctrl Pts',(-4.37620164431587,0.286601478848438,
16.6411013623859));
#45043=CARTESIAN_POINT('Ctrl Pts',(-4.37363367263438,0.00377358290378063,
16.651410108095));
#45044=CARTESIAN_POINT('Ctrl Pts',(-4.37598752684337,0.00314030101388495,
15.848589891905));
#45045=CARTESIAN_POINT('Ctrl Pts',(-4.36586808840044,-1.24298125471277,
15.8940729913518));
#45046=CARTESIAN_POINT('Ctrl Pts',(-3.15685416964687,-3.95275705920985,
15.9923526242733));
#45047=CARTESIAN_POINT('Ctrl Pts',(1.43550516966593,-4.9597746708902,16.1434287906695));
#45048=CARTESIAN_POINT('Ctrl Pts',(4.94197826197569,-1.49562391370258,16.3018183910937));
#45049=CARTESIAN_POINT('Ctrl Pts',(3.94475245484231,3.3315114408263,16.4602079915177));
#45050=CARTESIAN_POINT('Ctrl Pts',(-0.647385467154988,5.12259027405121,
16.6185975919419));
#45051=CARTESIAN_POINT('Ctrl Pts',(-3.91857823830144,2.77088302731469,16.7480582254043));
#45052=CARTESIAN_POINT('Ctrl Pts',(-4.36669222603978,0.659162948528226,
16.824722325392));
#45053=CARTESIAN_POINT('Ctrl Pts',(-4.36517770212695,0.0011188044825361,
16.848589891905));
#45054=CARTESIAN_POINT('Origin',(0.,0.,-1.84858989190501));
#45055=CARTESIAN_POINT('',(-4.36535254096326,-0.00139340307212889,14.651410108095));
#45056=CARTESIAN_POINT('',(-4.37450977369375,-0.00361009500681242,14.848589891905));
#45057=CARTESIAN_POINT('',(-4.372,-4.40683631492666E-13,-1.84858989190501));
#45058=CARTESIAN_POINT('Ctrl Pts',(-4.36535254096326,-0.00139340307212868,
14.651410108095));
#45059=CARTESIAN_POINT('Ctrl Pts',(-4.36719167669768,-0.640876180485729,
14.67460673873));
#45060=CARTESIAN_POINT('Ctrl Pts',(-3.93664196772952,-2.73257986740296,
14.7505668102252));
#45061=CARTESIAN_POINT('Ctrl Pts',(-0.715156117622299,-5.11247386069707,
14.8792903225806));
#45062=CARTESIAN_POINT('Ctrl Pts',(3.89726470591888,-3.38528655547465,15.0375806451613));
#45063=CARTESIAN_POINT('Ctrl Pts',(4.96212753934002,1.42342106576975,15.1958709677419));
#45064=CARTESIAN_POINT('Ctrl Pts',(1.5101211008729,4.93643307547415,15.3541612903226));
#45065=CARTESIAN_POINT('Ctrl Pts',(-3.1200112045152,3.99587919704142,15.5060076704403));
#45066=CARTESIAN_POINT('Ctrl Pts',(-4.36695709135924,1.26572596937806,15.6050906096977));
#45067=CARTESIAN_POINT('Ctrl Pts',(-4.37658335244799,-0.00285917843438723,
15.651410108095));
#45068=CARTESIAN_POINT('Ctrl Pts',(-4.37450977369375,-0.00361009500681263,
14.848589891905));
#45069=CARTESIAN_POINT('Ctrl Pts',(-4.37676192585348,-0.2570041121813,14.8578305903622));
#45070=CARTESIAN_POINT('Ctrl Pts',(-4.24160137044629,-1.95575914866763,
14.9198678222941));
#45071=CARTESIAN_POINT('Ctrl Pts',(-2.01745869282129,-4.75288338056742,
15.0347015877008));
#45072=CARTESIAN_POINT('Ctrl Pts',(2.88882981271105,-4.27956800578602,15.1930911881249));
#45073=CARTESIAN_POINT('Ctrl Pts',(5.16248437889336,0.0937818828261288,
15.351480788549));
#45074=CARTESIAN_POINT('Ctrl Pts',(2.73148949656154,4.38166693681219,15.5098703889731));
#45075=CARTESIAN_POINT('Ctrl Pts',(-2.18875273549729,4.67647318514471,15.6682599893972));
#45076=CARTESIAN_POINT('Ctrl Pts',(-4.27423782525496,1.84868256384714,15.7811664903745));
#45077=CARTESIAN_POINT('Ctrl Pts',(-4.37761467728721,0.203509842654685,
15.8412764578771));
#45078=CARTESIAN_POINT('Ctrl Pts',(-4.37598752684337,0.00314030101388495,
15.848589891905));
#45079=CARTESIAN_POINT('Origin',(0.,0.,-1.84858989190501));
#45080=CARTESIAN_POINT('',(-4.3715702955649,0.00393516289142377,13.651410108095));
#45081=CARTESIAN_POINT('',(-4.36492411635568,-0.000270170186619789,13.848589891905));
#45082=CARTESIAN_POINT('',(-4.372,-4.40683631492666E-13,-1.84858989190501));
#45083=CARTESIAN_POINT('Ctrl Pts',(-4.3715702955649,0.00393516289142415,
13.651410108095));
#45084=CARTESIAN_POINT('Ctrl Pts',(-4.36167155640512,-1.09343140876319,
13.691359426902));
#45085=CARTESIAN_POINT('Ctrl Pts',(-3.38808352462445,-3.65581253168041,
13.7840721865693));
#45086=CARTESIAN_POINT('Ctrl Pts',(0.907928552289056,-5.08178147829179,
13.9295483870968));
#45087=CARTESIAN_POINT('Ctrl Pts',(4.75589152831045,-2.00756893285326,14.0878387096774));
#45088=CARTESIAN_POINT('Ctrl Pts',(4.2747154125816,2.89407073006048,14.2461290322581));
#45089=CARTESIAN_POINT('Ctrl Pts',(-0.0976002483683332,5.16132845696157,
14.4044193548387));
#45090=CARTESIAN_POINT('Ctrl Pts',(-3.75335254656528,3.08663197095523,14.5395130467844));
#45091=CARTESIAN_POINT('Ctrl Pts',(-4.36300834804604,0.813701953645304,
14.6218432978698));
#45092=CARTESIAN_POINT('Ctrl Pts',(-4.36535254096326,-0.00139340307212868,
14.651410108095));
#45093=CARTESIAN_POINT('Ctrl Pts',(-4.36492411635568,-0.000270170186619789,
13.848589891905));
#45094=CARTESIAN_POINT('Ctrl Pts',(-4.36531805977148,-0.711553376731479,
13.8743847228474));
#45095=CARTESIAN_POINT('Ctrl Pts',(-3.86529136737144,-2.8781600308068,13.9529760872644));
#45096=CARTESIAN_POINT('Ctrl Pts',(-0.460905372910369,-5.14272362102755,
14.0843639851561));
#45097=CARTESIAN_POINT('Ctrl Pts',(4.06315051784514,-3.18603952805496,14.2427535855802));
#45098=CARTESIAN_POINT('Ctrl Pts',(4.88439639669049,1.67413017563193,14.4011431860043));
#45099=CARTESIAN_POINT('Ctrl Pts',(1.25441857601452,5.00863993928383,14.5595327864284));
#45100=CARTESIAN_POINT('Ctrl Pts',(-3.24025672884045,3.85045757200017,14.7086816883953));
#45101=CARTESIAN_POINT('Ctrl Pts',(-4.36389430254103,1.19075719850307,14.8050340568875));
#45102=CARTESIAN_POINT('Ctrl Pts',(-4.37450977369375,-0.00361009500681263,
14.848589891905));
#45103=CARTESIAN_POINT('Origin',(0.,0.,-1.84858989190501));
#45104=CARTESIAN_POINT('',(-4.37805463091546,-0.00189096989131645,12.651410108095));
#45105=CARTESIAN_POINT('',(-4.3735298381194,0.00380331467108683,12.848589891905));
#45106=CARTESIAN_POINT('',(-4.372,-4.40683631492666E-13,-1.84858989190501));
#45107=CARTESIAN_POINT('Ctrl Pts',(-4.37805463091546,-0.00189096989131629,
12.651410108095));
#45108=CARTESIAN_POINT('Ctrl Pts',(-4.37864191593093,-0.109663799931991,
12.6553486742139));
#45109=CARTESIAN_POINT('Ctrl Pts',(-4.32628239365674,-1.66064736718339,
12.7120506811929));
#45110=CARTESIAN_POINT('Ctrl Pts',(-2.4839194519693,-4.5253708583176,12.8215161290323));
#45111=CARTESIAN_POINT('Ctrl Pts',(2.44122672465452,-4.54854364912704,12.9798064516129));
#45112=CARTESIAN_POINT('Ctrl Pts',(5.14420067918421,-0.431319627959304,
13.1380967741936));
#45113=CARTESIAN_POINT('Ctrl Pts',(3.16456988475122,4.07852114052473,13.2963870967742));
#45114=CARTESIAN_POINT('Ctrl Pts',(-1.69566975348524,4.87581186432528,13.4546774193548));
#45115=CARTESIAN_POINT('Ctrl Pts',(-4.17531922896613,2.15372155886245,13.5730184231284));
#45116=CARTESIAN_POINT('Ctrl Pts',(-4.37474540982351,0.355925875277971,
13.6385959860418));
#45117=CARTESIAN_POINT('Ctrl Pts',(-4.3715702955649,0.00393516289142415,
13.651410108095));
#45118=CARTESIAN_POINT('Ctrl Pts',(-4.3735298381194,0.00380331467108686,
12.848589891905));
#45119=CARTESIAN_POINT('Ctrl Pts',(-4.36293974589787,-1.15814174670351,
12.8909388553325));
#45120=CARTESIAN_POINT('Ctrl Pts',(-3.29085772231164,-3.78595162322649,
12.9860843522346));
#45121=CARTESIAN_POINT('Ctrl Pts',(1.14016230868481,-5.03587826648703,13.1340263826114));
#45122=CARTESIAN_POINT('Ctrl Pts',(4.84505108113381,-1.78480251743019,13.2924159830355));
#45123=CARTESIAN_POINT('Ctrl Pts',(4.13457213027864,3.09279053680373,13.4508055834596));
#45124=CARTESIAN_POINT('Ctrl Pts',(-0.343804419177731,5.15187718471428,
13.6091951838838));
#45125=CARTESIAN_POINT('Ctrl Pts',(-3.8305579098897,2.94525464061577,13.7417899533655));
#45126=CARTESIAN_POINT('Ctrl Pts',(-4.36451174137436,0.744292087358565,
13.8215881893726));
#45127=CARTESIAN_POINT('Ctrl Pts',(-4.36492411635568,-0.000270170186619789,
13.848589891905));
#45128=CARTESIAN_POINT('Origin',(0.,0.,-1.84858989190501));
#45129=CARTESIAN_POINT('',(-4.3662580307389,-0.00237411499775451,11.651410108095));
#45130=CARTESIAN_POINT('',(-4.37682453544783,-0.00275176080394124,11.848589891905));
#45131=CARTESIAN_POINT('',(-4.372,-4.40683631492666E-13,-1.84858989190501));
#45132=CARTESIAN_POINT('Ctrl Pts',(-4.3662580307389,-0.00237411499775443,
11.651410108095));
#45133=CARTESIAN_POINT('Ctrl Pts',(-4.36908770984708,-0.57249276395778,
11.6721013623859));
#45134=CARTESIAN_POINT('Ctrl Pts',(-4.00080778508103,-2.59292231754593,
11.745556057537));
#45135=CARTESIAN_POINT('Ctrl Pts',(-0.955706815437237,-5.07301308219371,
11.8717741935484));
#45136=CARTESIAN_POINT('Ctrl Pts',(3.73310810644377,-3.5654931096253,12.030064516129));
#45137=CARTESIAN_POINT('Ctrl Pts',(5.02379164936073,1.1875835604264,12.1883548387097));
#45138=CARTESIAN_POINT('Ctrl Pts',(1.74147501164997,4.85964011352491,12.3466451612903));
#45139=CARTESIAN_POINT('Ctrl Pts',(-3.00493840101716,4.12681778354368,12.5009969177521));
#45140=CARTESIAN_POINT('Ctrl Pts',(-4.3707742866348,1.33412695349428,12.6025852333536));
#45141=CARTESIAN_POINT('Ctrl Pts',(-4.37805463091546,-0.00189096989131629,
12.651410108095));
#45142=CARTESIAN_POINT('Ctrl Pts',(-4.37682453544783,-0.0027517608039412,
11.848589891905));
#45143=CARTESIAN_POINT('Ctrl Pts',(-4.37805680950565,-0.169972374992373,
11.8546964543429));
#45144=CARTESIAN_POINT('Ctrl Pts',(-4.29358524369388,-1.7817038588778,11.9135995502554));
#45145=CARTESIAN_POINT('Ctrl Pts',(-2.29456228398659,-4.62547553554524,
12.0252991796426));
#45146=CARTESIAN_POINT('Ctrl Pts',(2.63111281568934,-4.44266646915302,12.1836887800668));
#45147=CARTESIAN_POINT('Ctrl Pts',(5.15901534120123,-0.211188811899807,
12.3420783804909));
#45148=CARTESIAN_POINT('Ctrl Pts',(2.98542980392062,4.2127483773522,12.500467980915));
#45149=CARTESIAN_POINT('Ctrl Pts',(-1.90882269345658,4.79754478144462,12.6588575813391));
#45150=CARTESIAN_POINT('Ctrl Pts',(-4.22005393336117,2.0228792487521,12.7748982183358));
#45151=CARTESIAN_POINT('Ctrl Pts',(-4.37614243406833,0.290457377422949,
12.8381423218578));
#45152=CARTESIAN_POINT('Ctrl Pts',(-4.3735298381194,0.00380331467108686,
12.848589891905));
#45153=CARTESIAN_POINT('Origin',(0.,0.,-1.84858989190501));
#45154=CARTESIAN_POINT('',(-4.36958950328423,0.00375500997191766,10.651410108095));
#45155=CARTESIAN_POINT('',(-4.36549183168559,-0.00162636191587406,10.848589891905));
#45156=CARTESIAN_POINT('',(-4.372,-4.40683631492666E-13,-1.84858989190501));
#45157=CARTESIAN_POINT('Ctrl Pts',(-4.36958950328423,0.00375500997191747,
10.651410108095));
#45158=CARTESIAN_POINT('Ctrl Pts',(-4.36106090852754,-1.0259785981898,10.688854050558));
#45159=CARTESIAN_POINT('Ctrl Pts',(-3.48414488794968,-3.51981628552574,
10.7790614338811));
#45160=CARTESIAN_POINT('Ctrl Pts',(0.667017186951725,-5.11897697997292,
10.9220322580645));
#45161=CARTESIAN_POINT('Ctrl Pts',(4.65581649466175,-2.22984528997355,11.0803225806452));
#45162=CARTESIAN_POINT('Ctrl Pts',(4.40657187915952,2.68904472312794,11.2386129032258));
#45163=CARTESIAN_POINT('Ctrl Pts',(0.14616290696869,5.16018155240764,11.3969032258064));
#45164=CARTESIAN_POINT('Ctrl Pts',(-3.67299362448513,3.22514497791193,11.5345022940962));
#45165=CARTESIAN_POINT('Ctrl Pts',(-4.36187192659012,0.881330247193059,
11.6193379215257));
#45166=CARTESIAN_POINT('Ctrl Pts',(-4.3662580307389,-0.00237411499775443,
11.651410108095));
#45167=CARTESIAN_POINT('Ctrl Pts',(-4.36549183168559,-0.00162636191587386,
10.848589891905));
#45168=CARTESIAN_POINT('Ctrl Pts',(-4.36759069612872,-0.626283874484138,
10.871250586828));
#45169=CARTESIAN_POINT('Ctrl Pts',(-3.95060522485931,-2.70364125089475,
10.9467078152256));
#45170=CARTESIAN_POINT('Ctrl Pts',(-0.763741663751577,-5.10653881568242,
11.074961577098));
#45171=CARTESIAN_POINT('Ctrl Pts',(3.86794975738412,-3.42038077988013,11.2333511775221));
#45172=CARTESIAN_POINT('Ctrl Pts',(4.97472054752429,1.38282156443299,11.3917407779462));
#45173=CARTESIAN_POINT('Ctrl Pts',(1.54795388466898,4.92583787552529,11.5501303783703));
#45174=CARTESIAN_POINT('Ctrl Pts',(-3.10298340129681,4.01633537157594,11.7024134163566));
#45175=CARTESIAN_POINT('Ctrl Pts',(-4.36740273051995,1.27579500142313,11.8018999208682));
#45176=CARTESIAN_POINT('Ctrl Pts',(-4.37682453544783,-0.0027517608039412,
11.848589891905));
#45177=CARTESIAN_POINT('Origin',(0.,0.,-1.84858989190501));
#45178=CARTESIAN_POINT('',(-4.37893064514985,-0.000718125850480163,9.65141010809499));
#45179=CARTESIAN_POINT('',(-4.37095165486262,0.00392878392899476,9.84858989190502));
#45180=CARTESIAN_POINT('',(-4.372,-4.40683631492666E-13,-1.84858989190501));
#45181=CARTESIAN_POINT('Ctrl Pts',(-4.37893064514985,-0.000718125850479884,
9.65141010809498));
#45182=CARTESIAN_POINT('Ctrl Pts',(-4.37902043646228,-0.0399142522790172,
9.65284329786977));
#45183=CARTESIAN_POINT('Ctrl Pts',(-4.36082969860212,-1.52204564057694,
9.70703992850478));
#45184=CARTESIAN_POINT('Ctrl Pts',(-2.69478237803987,-4.40306543037773,
9.81399999999999));
#45185=CARTESIAN_POINT('Ctrl Pts',(2.22377879965116,-4.65871710875468,9.97229032258064));
#45186=CARTESIAN_POINT('Ctrl Pts',(5.11810379036282,-0.67368452576514,10.1305806451613));
#45187=CARTESIAN_POINT('Ctrl Pts',(3.35357921258595,3.92458197953528,10.2888709677419));
#45188=CARTESIAN_POINT('Ctrl Pts',(-1.46360347987537,4.95042443663959,10.4471612903226));
#45189=CARTESIAN_POINT('Ctrl Pts',(-4.12415016732119,2.29334108429437,10.5680076704403));
#45190=CARTESIAN_POINT('Ctrl Pts',(-4.37307882051719,0.425051522096353,
10.6360906096977));
#45191=CARTESIAN_POINT('Ctrl Pts',(-4.36958950328423,0.00375500997191747,
10.651410108095));
#45192=CARTESIAN_POINT('Ctrl Pts',(-4.37095165486262,0.00392878392899445,
9.84858989190502));
#45193=CARTESIAN_POINT('Ctrl Pts',(-4.36138099894435,-1.0736503956833,9.88780471931308));
#45194=CARTESIAN_POINT('Ctrl Pts',(-3.41650604254828,-3.61702144425598,
9.97981608019584));
#45195=CARTESIAN_POINT('Ctrl Pts',(0.840841326532404,-5.09441123866306,
10.1246239745533));
#45196=CARTESIAN_POINT('Ctrl Pts',(4.73121909778617,-2.06775381846214,10.2830135749774));
#45197=CARTESIAN_POINT('Ctrl Pts',(4.30996593957687,2.84327867165857,10.4414031754015));
#45198=CARTESIAN_POINT('Ctrl Pts',(-0.0390238264566685,5.16318866070086,
10.5997927758256));
#45199=CARTESIAN_POINT('Ctrl Pts',(-3.7353314916358,3.11908229388608,10.7355216813268));
#45200=CARTESIAN_POINT('Ctrl Pts',(-4.36270060925329,0.829088583628261,
10.8184540533533));
#45201=CARTESIAN_POINT('Ctrl Pts',(-4.36549183168559,-0.00162636191587386,
10.848589891905));
#45202=CARTESIAN_POINT('Origin',(0.,0.,-1.84858989190501));
#45203=CARTESIAN_POINT('',(-4.3676089549007,-0.00316636266463396,8.65141010809498));
#45204=CARTESIAN_POINT('',(-4.3784939599728,-0.00146115515596901,8.84858989190502));
#45205=CARTESIAN_POINT('',(-4.372,-4.40683631492666E-13,-1.84858989190501));
#45206=CARTESIAN_POINT('Ctrl Pts',(-4.3676089549007,-0.0031663626646336,
8.65141010809498));
#45207=CARTESIAN_POINT('Ctrl Pts',(-4.37099157996906,-0.503863509155134,
8.66959598604181));
#45208=CARTESIAN_POINT('Ctrl Pts',(-4.0607005189635,-2.45318988687306,8.74054530484886));
#45209=CARTESIAN_POINT('Ctrl Pts',(-1.19412647058753,-5.02224045834365,
8.86425806451613));
#45210=CARTESIAN_POINT('Ctrl Pts',(3.56062739266322,-3.73774929868204,9.02254838709676));
#45211=CARTESIAN_POINT('Ctrl Pts',(5.07425366817473,0.949097971864315,9.18083870967742));
#45212=CARTESIAN_POINT('Ctrl Pts',(1.96894576792944,4.77201108675727,9.33912903225805));
#45213=CARTESIAN_POINT('Ctrl Pts',(-2.88428822201713,4.2558282973375,9.49598616506391));
#45214=CARTESIAN_POINT('Ctrl Pts',(-4.37571473425415,1.40310643844898,9.60007985700956));
#45215=CARTESIAN_POINT('Ctrl Pts',(-4.37893064514985,-0.000718125850479884,
9.65141010809498));
#45216=CARTESIAN_POINT('Ctrl Pts',(-4.3784939599728,-0.00146115515596968,
8.84858989190502));
#45217=CARTESIAN_POINT('Ctrl Pts',(-4.37884870232368,-0.0827753827151446,
8.85156231832348));
#45218=CARTESIAN_POINT('Ctrl Pts',(-4.34001073551865,-1.6080554399903,8.90733127821665));
#45219=CARTESIAN_POINT('Ctrl Pts',(-2.56365995117077,-4.48192901101572,
9.01589677158451));
#45220=CARTESIAN_POINT('Ctrl Pts',(2.36421564112952,-4.59026408905411,9.17428637200862));
#45221=CARTESIAN_POINT('Ctrl Pts',(5.13754605775107,-0.515422651333577,
9.33267597243274));
#45222=CARTESIAN_POINT('Ctrl Pts',(3.22895369161553,4.02913117959985,9.49106557285684));
#45223=CARTESIAN_POINT('Ctrl Pts',(-1.62223260619563,4.90187733184103,9.64945517328097));
#45224=CARTESIAN_POINT('Ctrl Pts',(-4.15999532952882,2.19738929405191,9.76862994629701));
#45225=CARTESIAN_POINT('Ctrl Pts',(-4.37426636626487,0.377138731501872,
9.83500818583837));
#45226=CARTESIAN_POINT('Ctrl Pts',(-4.37095165486262,0.00392878392899445,
9.84858989190502));
#45227=CARTESIAN_POINT('Origin',(0.,0.,-1.84858989190501));
#45228=CARTESIAN_POINT('',(-4.36783565389082,0.00326080189849165,7.65141010809498));
#45229=CARTESIAN_POINT('',(-4.36682740614764,-0.00278338701585445,7.84858989190503));
#45230=CARTESIAN_POINT('',(-4.372,-4.40683631492666E-13,-1.84858989190501));
#45231=CARTESIAN_POINT('Ctrl Pts',(-4.36783565389082,0.0032608018984915,
7.65141010809498));
#45232=CARTESIAN_POINT('Ctrl Pts',(-4.36111999858997,-0.958548857288375,
7.68634867421386));
#45233=CARTESIAN_POINT('Ctrl Pts',(-3.57508309710888,-3.38283964502905,
7.77405068119295));
#45234=CARTESIAN_POINT('Ctrl Pts',(0.424618501333285,-5.14475814567673,
7.91451612903225));
#45235=CARTESIAN_POINT('Ctrl Pts',(4.54535988400859,-2.44714952016159,8.0728064516129));
#45236=CARTESIAN_POINT('Ctrl Pts',(4.52860253637045,2.47802266268103,8.23109677419354));
#45237=CARTESIAN_POINT('Ctrl Pts',(0.389600147091602,5.14752843358518,8.38938709677419));
#45238=CARTESIAN_POINT('Ctrl Pts',(-3.58777114537366,3.36303202741965,8.52949154140801));
#45239=CARTESIAN_POINT('Ctrl Pts',(-4.36117742976588,0.948829858465871,
8.6168325451816));
#45240=CARTESIAN_POINT('Ctrl Pts',(-4.3676089549007,-0.0031663626646336,
8.65141010809498));
#45241=CARTESIAN_POINT('Ctrl Pts',(-4.36682740614764,-0.00278338701585466,
7.84858989190503));
#45242=CARTESIAN_POINT('Ctrl Pts',(-4.36998031573444,-0.540633837652302,
7.8681164508086));
#45243=CARTESIAN_POINT('Ctrl Pts',(-4.02906901036793,-2.52888541639766,
7.94043954318687));
#45244=CARTESIAN_POINT('Ctrl Pts',(-1.06391319462353,-5.05253685976928,
8.06555916903983));
#45245=CARTESIAN_POINT('Ctrl Pts',(3.65925338948522,-3.64278803069328,8.22394876946396));
#45246=CARTESIAN_POINT('Ctrl Pts',(5.04768747299395,1.08668817054443,8.38233836988805));
#45247=CARTESIAN_POINT('Ctrl Pts',(1.83608824986349,4.82584914224785,8.54072797031219));
#45248=CARTESIAN_POINT('Ctrl Pts',(-2.95709387717496,4.17950307750852,8.69614514431782));
#45249=CARTESIAN_POINT('Ctrl Pts',(-4.37254773342937,1.36153600902825,8.79876578484878));
#45250=CARTESIAN_POINT('Ctrl Pts',(-4.3784939599728,-0.00146115515596968,
8.84858989190502));
#45251=CARTESIAN_POINT('Origin',(0.,0.,-1.84858989190501));
#45252=CARTESIAN_POINT('',(-4.37899478532443,0.000538853135781114,6.65141010809498));
#45253=CARTESIAN_POINT('',(-4.36857373794226,0.00352936749739713,6.84858989190502));
#45254=CARTESIAN_POINT('',(-4.372,-4.40683631492666E-13,-1.84858989190501));
#45255=CARTESIAN_POINT('Ctrl Pts',(-4.37899478532443,0.00053885313578114,
6.65141010809498));
#45256=CARTESIAN_POINT('Ctrl Pts',(-4.37652423695377,-1.41310306479934,
6.7031013623859));
#45257=CARTESIAN_POINT('Ctrl Pts',(-2.86643925520047,-4.27424452468468,
6.80755605753705));
#45258=CARTESIAN_POINT('Ctrl Pts',(2.00137227482285,-4.75850252356265,6.96477419354837));
#45259=CARTESIAN_POINT('Ctrl Pts',(5.08059451261016,-0.914547236405604,
7.12306451612904));
#45260=CARTESIAN_POINT('Ctrl Pts',(3.53511070256229,3.76189175413264,7.28135483870967));
#45261=CARTESIAN_POINT('Ctrl Pts',(-1.22827365147281,5.01399851279189,7.43964516129032));
#45262=CARTESIAN_POINT('Ctrl Pts',(-4.06898604612617,2.43305468214084,7.56299691775209));
#45263=CARTESIAN_POINT('Ctrl Pts',(-4.37126183097366,0.493954571118568,
7.63358523335364));
#45264=CARTESIAN_POINT('Ctrl Pts',(-4.36783565389082,0.0032608018984915,
7.65141010809498));
#45265=CARTESIAN_POINT('Ctrl Pts',(-4.36857373794226,0.00352936749739713,
6.84858989190502));
#45266=CARTESIAN_POINT('Ctrl Pts',(-4.3609877808655,-0.989297031049394,
6.8846705832937));
#45267=CARTESIAN_POINT('Ctrl Pts',(-3.53400975081915,-3.4463519724339,6.97354780815709));
#45268=CARTESIAN_POINT('Ctrl Pts',(0.538586577094185,-5.13516937442138,
7.11522156649516));
#45269=CARTESIAN_POINT('Ctrl Pts',(4.60087948645563,-2.34349054961462,7.27361116691928));
#45270=CARTESIAN_POINT('Ctrl Pts',(4.47032190918109,2.58384636410851,7.43200076734339));
#45271=CARTESIAN_POINT('Ctrl Pts',(0.26589292373178,5.15648532996368,7.59039036776751));
#45272=CARTESIAN_POINT('Ctrl Pts',(-3.63264590427038,3.29210602756316,7.72925340928804));
#45273=CARTESIAN_POINT('Ctrl Pts',(-4.3614553781167,0.913623385120531,7.81531991733389));
#45274=CARTESIAN_POINT('Ctrl Pts',(-4.36682740614764,-0.00278338701585466,
7.84858989190503));
#45275=CARTESIAN_POINT('Origin',(0.,0.,-1.84858989190501));
#45276=CARTESIAN_POINT('',(-4.36931971855082,-0.00370222284602327,5.65141010809498));
#45277=CARTESIAN_POINT('',(-4.37909655387308,8.17972643269707E-5,5.84858989190502));
#45278=CARTESIAN_POINT('',(-4.372,-4.40683631492666E-13,-1.84858989190501));
#45279=CARTESIAN_POINT('Ctrl Pts',(-4.36931971855082,-0.00370222284602335,
5.65141010809498));
#45280=CARTESIAN_POINT('Ctrl Pts',(-4.37282475456675,-0.434994053437505,
5.66709060969773));
#45281=CARTESIAN_POINT('Ctrl Pts',(-4.11645084466375,-2.3134683703663,5.73553455216068));
#45282=CARTESIAN_POINT('Ctrl Pts',(-1.42988345294528,-4.96026920238937,
5.85674193548387));
#45283=CARTESIAN_POINT('Ctrl Pts',(3.38020716333018,-3.90167102433782,6.01503225806451));
#45284=CARTESIAN_POINT('Ctrl Pts',(5.11340107541181,0.708496077023162,6.17332258064516));
#45285=CARTESIAN_POINT('Ctrl Pts',(2.19202615312461,4.67374139134797,6.3316129032258));
#45286=CARTESIAN_POINT('Ctrl Pts',(-2.72468151658193,4.38462631046011,6.48990322580645));
#45287=CARTESIAN_POINT('Ctrl Pts',(-4.36552898201431,1.50209810391025,6.59650229409617));
#45288=CARTESIAN_POINT('Ctrl Pts',(-4.37904602975287,0.0298607935490157,
6.65033792152568));
#45289=CARTESIAN_POINT('Ctrl Pts',(-4.37899478532443,0.00053885313578114,
6.65141010809498));
#45290=CARTESIAN_POINT('Ctrl Pts',(-4.37909655387308,8.17972643267733E-5,
5.84858989190502));
#45291=CARTESIAN_POINT('Ctrl Pts',(-4.37869792746944,-1.43927515570558,
5.90122471577881));
#45292=CARTESIAN_POINT('Ctrl Pts',(-2.8187969284654,-4.3231521197151,6.0066560731273));
#45293=CARTESIAN_POINT('Ctrl Pts',(2.08906951604171,-4.72184588505036,6.16488396395049));
#45294=CARTESIAN_POINT('Ctrl Pts',(5.098151436811,-0.817858137064712,6.32327356437462));
#45295=CARTESIAN_POINT('Ctrl Pts',(3.46121148378334,3.83145599864432,6.48166316479871));
#45296=CARTESIAN_POINT('Ctrl Pts',(-1.32998241066,4.98910681308353,6.64005276522284));
#45297=CARTESIAN_POINT('Ctrl Pts',(-4.09382090065572,2.37211345116906,6.76236167425826));
#45298=CARTESIAN_POINT('Ctrl Pts',(-4.37208823990123,0.463496420738366,
6.831874049819));
#45299=CARTESIAN_POINT('Ctrl Pts',(-4.36857373794226,0.00352936749739713,
6.84858989190502));
#45300=CARTESIAN_POINT('Origin',(0.,0.,-1.84858989190501));
#45301=CARTESIAN_POINT('',(-4.36642690985212,0.00250163610255838,4.65141010809498));
#45302=CARTESIAN_POINT('',(-4.36880169481863,-0.00359316639133633,4.84858989190502));
#45303=CARTESIAN_POINT('',(-4.372,-4.40683631492666E-13,-1.84858989190501));
#45304=CARTESIAN_POINT('Ctrl Pts',(-4.36642690985212,0.00250163610255878,
4.65141010809498));
#45305=CARTESIAN_POINT('Ctrl Pts',(-4.36174213540044,-0.891062986338486,
4.68384329786977));
#45306=CARTESIAN_POINT('Ctrl Pts',(-3.66101665548786,-3.24505548151499,
4.76903992850477));
#45307=CARTESIAN_POINT('Ctrl Pts',(0.181272997936893,-5.15906748833169,
4.907));
#45308=CARTESIAN_POINT('Ctrl Pts',(4.4247679934035,-2.65899707670991,5.06529032258064));
#45309=CARTESIAN_POINT('Ctrl Pts',(4.64053527927078,2.26147508740778,5.22358064516129));
#45310=CARTESIAN_POINT('Ctrl Pts',(0.63216865368283,5.12339731452249,5.38187096774192));
#45311=CARTESIAN_POINT('Ctrl Pts',(-3.49756148837773,3.50013537491244,5.52448078871984));
#45312=CARTESIAN_POINT('Ctrl Pts',(-4.361030631826,1.01626315589314,5.61432716883751));
#45313=CARTESIAN_POINT('Ctrl Pts',(-4.36931971855082,-0.00370222284602335,
5.65141010809498));
#45314=CARTESIAN_POINT('Ctrl Pts',(-4.36880169481863,-0.00359316639133644,
4.84858989190502));
#45315=CARTESIAN_POINT('Ctrl Pts',(-4.37232350022417,-0.454601269873613,
4.86498231478922));
#45316=CARTESIAN_POINT('Ctrl Pts',(-4.10093982798236,-2.35407682434418,
4.93417127114812));
#45317=CARTESIAN_POINT('Ctrl Pts',(-1.36037264139205,-4.98090617072295,
5.05615676098171));
#45318=CARTESIAN_POINT('Ctrl Pts',(3.43778957362211,-3.85248528258675,5.21454636140584));
#45319=CARTESIAN_POINT('Ctrl Pts',(5.10304258525828,0.786763228710822,5.37293596182993));
#45320=CARTESIAN_POINT('Ctrl Pts',(2.11781634615703,4.70902260867037,5.53132556225406));
#45321=CARTESIAN_POINT('Ctrl Pts',(-2.79740769526454,4.33987905263503,5.68971516267816));
#45322=CARTESIAN_POINT('Ctrl Pts',(-4.37709282415761,1.45270398568835,5.79546993922849));
#45323=CARTESIAN_POINT('Ctrl Pts',(-4.37909777857019,0.00450392355468565,
5.84842818230411));
#45324=CARTESIAN_POINT('Ctrl Pts',(-4.37909655387308,8.17972643267733E-5,
5.84858989190502));
#45325=CARTESIAN_POINT('Origin',(0.,0.,-1.84858989190501));
#45326=CARTESIAN_POINT('',(-4.37822270954365,0.00173219555018226,3.65141010809498));
#45327=CARTESIAN_POINT('',(-4.36665723562798,0.00267775706545931,3.84858989190502));
#45328=CARTESIAN_POINT('',(-4.372,-4.40683631492666E-13,-1.84858989190501));
#45329=CARTESIAN_POINT('Ctrl Pts',(-4.37822270954365,0.00173219555018251,
3.65141010809498));
#45330=CARTESIAN_POINT('Ctrl Pts',(-4.37141484073147,-1.3440268941613,3.70059598604181));
#45331=CARTESIAN_POINT('Ctrl Pts',(-2.98789956101879,-4.1455315666631,3.80254530484886));
#45332=CARTESIAN_POINT('Ctrl Pts',(1.77450307237079,-4.84767739015689,3.95725806451612));
#45333=CARTESIAN_POINT('Ctrl Pts',(5.03175648528012,-1.15337068283656,4.11554838709677));
#45334=CARTESIAN_POINT('Ctrl Pts',(3.7087595738537,3.5908132325819,4.27383870967742));
#45335=CARTESIAN_POINT('Ctrl Pts',(-0.990205008382098,5.06639233464293,
4.43212903225806));
#45336=CARTESIAN_POINT('Ctrl Pts',(-4.00969822487022,2.57279053906618,4.55798616506392));
#45337=CARTESIAN_POINT('Ctrl Pts',(-4.36936348937275,0.562619011588028,
4.63107985700956));
#45338=CARTESIAN_POINT('Ctrl Pts',(-4.36642690985212,0.00250163610255878,
4.65141010809498));
#45339=CARTESIAN_POINT('Ctrl Pts',(-4.36665723562798,0.00267775706545938,
3.84858989190502));
#45340=CARTESIAN_POINT('Ctrl Pts',(-4.36155175532508,-0.904909371632279,
3.88153644727432));
#45341=CARTESIAN_POINT('Ctrl Pts',(-3.64359471136329,-3.27429676880991,
3.96727953611833));
#45342=CARTESIAN_POINT('Ctrl Pts',(0.234452652827207,-5.15801046495039,
4.10581915843705));
#45343=CARTESIAN_POINT('Ctrl Pts',(4.4544870133001,-2.61105064195526,4.26420875886115));
#45344=CARTESIAN_POINT('Ctrl Pts',(4.61508054334482,2.31539879571022,4.42259835928526));
#45345=CARTESIAN_POINT('Ctrl Pts',(0.56988195080356,5.13179058096912,4.58098795970938));
#45346=CARTESIAN_POINT('Ctrl Pts',(-3.52225462180705,3.46403365178023,4.72298513724929));
#45347=CARTESIAN_POINT('Ctrl Pts',(-4.36098050850789,0.998000618272236,
4.81218578131451));
#45348=CARTESIAN_POINT('Ctrl Pts',(-4.36880169481863,-0.00359316639133644,
4.84858989190502));
#45349=CARTESIAN_POINT('Origin',(0.,0.,-1.84858989190501));
#45350=CARTESIAN_POINT('',(-4.3712761175009,-0.0039298912494793,2.65141010809498));
#45351=CARTESIAN_POINT('',(-4.37836367713493,0.00160984593324705,2.84858989190502));
#45352=CARTESIAN_POINT('',(-4.372,-4.40683631492666E-13,-1.84858989190501));
#45353=CARTESIAN_POINT('Ctrl Pts',(-4.3712761175009,-0.00392989124947909,
2.65141010809498));
#45354=CARTESIAN_POINT('Ctrl Pts',(-4.37451696257115,-0.365899162664298,
2.66458523335364));
#45355=CARTESIAN_POINT('Ctrl Pts',(-4.16818790357475,-2.17383119834201,
2.73052379947252));
#45356=CARTESIAN_POINT('Ctrl Pts',(-1.66245191543707,-4.88723759858308,
2.84922580645161));
#45357=CARTESIAN_POINT('Ctrl Pts',(3.19224964022283,-4.05689272016998,3.00751612903226));
#45358=CARTESIAN_POINT('Ctrl Pts',(5.14114662208426,0.466314344506177,3.1658064516129));
#45359=CARTESIAN_POINT('Ctrl Pts',(2.41021871871718,4.56505016420442,3.32409677419355));
#45360=CARTESIAN_POINT('Ctrl Pts',(-2.5146557123555,4.50836375769575,3.48238709677419));
#45361=CARTESIAN_POINT('Ctrl Pts',(-4.33147098232467,1.64065849811777,3.591491541408));
#45362=CARTESIAN_POINT('Ctrl Pts',(-4.37871788376841,0.0996167512533684,
3.6478325451816));
#45363=CARTESIAN_POINT('Ctrl Pts',(-4.37822270954365,0.00173219555018251,
3.65141010809498));
#45364=CARTESIAN_POINT('Ctrl Pts',(-4.37836367713493,0.00160984593324717,
2.84858989190502));
#45365=CARTESIAN_POINT('Ctrl Pts',(-4.37193582834707,-1.35264708506912,
2.89809057975943));
#45366=CARTESIAN_POINT('Ctrl Pts',(-2.9725521843832,-4.16280399703585,3.00038780108855));
#45367=CARTESIAN_POINT('Ctrl Pts',(1.80663443860224,-4.83695274769126,3.15548155589238));
#45368=CARTESIAN_POINT('Ctrl Pts',(5.04096893490742,-1.11744005069485,3.31387115631648));
#45369=CARTESIAN_POINT('Ctrl Pts',(3.68139281034196,3.62041254264275,3.4722607567406));
#45370=CARTESIAN_POINT('Ctrl Pts',(-1.03309179131411,5.05892887272037,3.63065035716471));
#45371=CARTESIAN_POINT('Ctrl Pts',(-4.0212815682019,2.54692422938098,3.75609340221952));
#45372=CARTESIAN_POINT('Ctrl Pts',(-4.36973323768933,0.549490145536826,
3.82873991379962));
#45373=CARTESIAN_POINT('Ctrl Pts',(-4.36665723562798,0.00267775706545938,
3.84858989190502));
#45374=CARTESIAN_POINT('Origin',(0.,0.,-1.84858989190501));
#45375=CARTESIAN_POINT('',(-4.36544656918105,0.00153916655095219,1.65141010809498));
#45376=CARTESIAN_POINT('',(-4.37121340809612,-0.00394090090135357,1.84858989190502));
#45377=CARTESIAN_POINT('',(-4.372,-4.40683631492666E-13,-1.84858989190501));
#45378=CARTESIAN_POINT('Ctrl Pts',(-4.36544656918105,0.00153916655095176,
1.65141010809498));
#45379=CARTESIAN_POINT('Ctrl Pts',(-4.36281788561468,-0.823458774996837,
1.68133792152568));
#45380=CARTESIAN_POINT('Ctrl Pts',(-3.74207983653693,-3.10661615213039,
1.76402917581661));
#45381=CARTESIAN_POINT('Ctrl Pts',(-0.0624691826164238,-5.16187799225891,
1.89948387096774));
#45382=CARTESIAN_POINT('Ctrl Pts',(4.29430578210828,-2.8649130214088,2.05777419354839));
#45383=CARTESIAN_POINT('Ctrl Pts',(4.74212257914569,2.03988351823947,2.21606451612903));
#45384=CARTESIAN_POINT('Ctrl Pts',(0.873326467994359,5.08784270323556,2.37435483870968));
#45385=CARTESIAN_POINT('Ctrl Pts',(-3.40224500791429,3.63628377215307,2.51947003603166));
#45386=CARTESIAN_POINT('Ctrl Pts',(-4.36153810021927,1.08370711208091,2.61182179249343));
#45387=CARTESIAN_POINT('Ctrl Pts',(-4.3712761175009,-0.00392989124947909,
2.65141010809498));
#45388=CARTESIAN_POINT('Ctrl Pts',(-4.37121340809612,-0.00394090090135399,
1.84858989190502));
#45389=CARTESIAN_POINT('Ctrl Pts',(-4.37447604421791,-0.368207831146071,
1.86184817876984));
#45390=CARTESIAN_POINT('Ctrl Pts',(-4.16647286574876,-2.17936832407669,
1.92790299910937));
#45391=CARTESIAN_POINT('Ctrl Pts',(-1.65208468153467,-4.89189754332655,
2.04675435292359));
#45392=CARTESIAN_POINT('Ctrl Pts',(3.20433051897175,-4.04874042926377,2.20514395334771));
#45393=CARTESIAN_POINT('Ctrl Pts',(5.14059300557593,0.484092964878372,2.36353355377181));
#45394=CARTESIAN_POINT('Ctrl Pts',(2.392155064142,4.57576601695794,2.52192315419593));
#45395=CARTESIAN_POINT('Ctrl Pts',(-2.53628918908134,4.49747442552335,2.68031275462004));
#45396=CARTESIAN_POINT('Ctrl Pts',(-4.33547083524805,1.62595452236117,2.78920166718974));
#45397=CARTESIAN_POINT('Ctrl Pts',(-4.37879165497107,0.0917787298065273,
2.84529404628473));
#45398=CARTESIAN_POINT('Ctrl Pts',(-4.37836367713493,0.00160984593324717,
2.84858989190502));
#45399=CARTESIAN_POINT('Origin',(0.,0.,-1.84858989190501));
#45400=CARTESIAN_POINT('',(-4.37640441740291,0.00246357316762604,0.651410108094979));
#45401=CARTESIAN_POINT('',(-4.36535621882271,0.00145633068789036,0.848589891905021));
#45402=CARTESIAN_POINT('',(-4.372,-4.40683631492666E-13,-1.84858989190501));
#45403=CARTESIAN_POINT('Ctrl Pts',(-4.37640441740291,0.00246357316762608,
0.651410108094978));
#45404=CARTESIAN_POINT('Ctrl Pts',(-4.3669296163584,-1.27588513251927,0.698090609697727));
#45405=CARTESIAN_POINT('Ctrl Pts',(-3.10443214653608,-4.01442651751147,
0.79753455216069));
#45406=CARTESIAN_POINT('Ctrl Pts',(1.54404435335689,-4.92628156041988,0.949741935483869));
#45407=CARTESIAN_POINT('Ctrl Pts',(4.97150648183897,-1.38949747849925,1.10803225806451));
#45408=CARTESIAN_POINT('Ctrl Pts',(3.87423912778238,3.41166257284768,1.26632258064516));
#45409=CARTESIAN_POINT('Ctrl Pts',(-0.749980974679123,5.10752324154442,
1.42461290322581));
#45410=CARTESIAN_POINT('Ctrl Pts',(-3.94614385852298,2.71245661069425,1.55297541237574));
#45411=CARTESIAN_POINT('Ctrl Pts',(-4.36745231673392,0.631032051720065,
1.62857448066547));
#45412=CARTESIAN_POINT('Ctrl Pts',(-4.36544656918105,0.00153916655095176,
1.65141010809498));
#45413=CARTESIAN_POINT('Ctrl Pts',(-4.36535621882271,0.0014563306878905,
0.848589891905021));
#45414=CARTESIAN_POINT('Ctrl Pts',(-4.36284379533113,-0.820370961494963,
0.87840231125495));
#45415=CARTESIAN_POINT('Ctrl Pts',(-3.74556810328531,-3.1011139180804,0.961011264079584));
#45416=CARTESIAN_POINT('Ctrl Pts',(-0.0704529116473286,-5.16289724783097,
1.09641675037892));
#45417=CARTESIAN_POINT('Ctrl Pts',(4.29252819085395,-2.86947836000301,1.25480635080303));
#45418=CARTESIAN_POINT('Ctrl Pts',(4.74374945851672,2.03886099295457,1.41319595122714));
#45419=CARTESIAN_POINT('Ctrl Pts',(0.87187597225223,5.08919664880298,1.57158555165126));
#45420=CARTESIAN_POINT('Ctrl Pts',(-3.4039180408651,3.63453814591924,1.71671686521054));
#45421=CARTESIAN_POINT('Ctrl Pts',(-4.36148372635845,1.08235900094027,1.80905164529514));
#45422=CARTESIAN_POINT('Ctrl Pts',(-4.37121340809612,-0.00394090090135399,
1.84858989190502));
#45423=CARTESIAN_POINT('Origin',(0.,0.,19.5));
#45424=CARTESIAN_POINT('',(-4.87237116524908,0.00192128708900893,19.1338737912933));
#45425=CARTESIAN_POINT('Ctrl Pts',(-0.803308159453631,4.29756675351939,
19.628));
#45426=CARTESIAN_POINT('Ctrl Pts',(-0.673853669232168,4.32487002581643,
19.6249474412138));
#45427=CARTESIAN_POINT('Ctrl Pts',(-0.543485635434045,4.34604385579072,
19.621903094994));
#45428=CARTESIAN_POINT('Ctrl Pts',(-0.412569255997991,4.3612238307311,19.6188638308603));
#45429=CARTESIAN_POINT('Ctrl Pts',(-0.27984336996821,4.37661362101213,19.6157825584728));
#45430=CARTESIAN_POINT('Ctrl Pts',(-0.146553204834455,4.38584275860783,
19.6127065096298));
#45431=CARTESIAN_POINT('Ctrl Pts',(-0.0130667331008604,4.38900056457998,
19.6096324222416));
#45432=CARTESIAN_POINT('Ctrl Pts',(0.102479072721167,4.39173395943972,19.6069714941353));
#45433=CARTESIAN_POINT('Ctrl Pts',(0.218172435996331,4.38991749290017,19.6043120356729));
#45434=CARTESIAN_POINT('Ctrl Pts',(0.333776183320261,4.38357806344137,19.6016519311904));
#45435=CARTESIAN_POINT('Ctrl Pts',(0.379031782704649,4.38109635600062,19.6006105754768));
#45436=CARTESIAN_POINT('Ctrl Pts',(0.424273632554427,4.37792119522461,19.5995691207606));
#45437=CARTESIAN_POINT('Ctrl Pts',(0.469487373095433,4.37405300814147,19.5985274401165));
#45438=CARTESIAN_POINT('Ctrl Pts',(0.491900142232015,4.37213552060263,19.598011071696));
#45439=CARTESIAN_POINT('Ctrl Pts',(0.514298864495916,4.37004829843513,19.5974948121273));
#45440=CARTESIAN_POINT('Ctrl Pts',(0.536673783628106,4.36779258854753,19.5969788310225));
#45441=CARTESIAN_POINT('Ctrl Pts',(0.67587029099505,4.35375960205351,19.5937688633242));
#45442=CARTESIAN_POINT('Ctrl Pts',(0.814241659431173,4.33320254529649,19.5905674515573));
#45443=CARTESIAN_POINT('Ctrl Pts',(0.951373424482021,4.30622334317185,19.5873709472848));
#45444=CARTESIAN_POINT('Ctrl Pts',(1.08850518953287,4.2792441410472,19.5841744430122));
#45445=CARTESIAN_POINT('Ctrl Pts',(1.22439822554137,4.24584269855803,19.580982846234));
#45446=CARTESIAN_POINT('Ctrl Pts',(1.35863436321977,4.20606161338018,19.5777925085132));
#45447=CARTESIAN_POINT('Ctrl Pts',(1.44718365537814,4.1798198949077,19.57568799216));
#45448=CARTESIAN_POINT('Ctrl Pts',(1.53501187237287,4.15080088353343,19.573584023676));
#45449=CARTESIAN_POINT('Ctrl Pts',(1.62197697724057,4.11905814350536,19.5714795558027));
#45450=CARTESIAN_POINT('Ctrl Pts',(1.66029004733011,4.10507366288661,19.5705524181278));
#45451=CARTESIAN_POINT('Ctrl Pts',(1.69843554242665,4.09056039562537,19.5696251835263));
#45452=CARTESIAN_POINT('Ctrl Pts',(1.73640102301099,4.07552228846135,19.5686977624494));
#45453=CARTESIAN_POINT('Ctrl Pts',(1.75436952443725,4.06840497436797,19.5682588277464));
#45454=CARTESIAN_POINT('Ctrl Pts',(1.77228816141992,4.061173866115,19.5678200842298));
#45455=CARTESIAN_POINT('Ctrl Pts',(1.79015508413385,4.05383000141309,19.5673815385189));
#45456=CARTESIAN_POINT('Ctrl Pts',(1.91574464850677,4.00220875787305,19.5642989279495));
#45457=CARTESIAN_POINT('Ctrl Pts',(2.03879019285953,3.94501636210332,19.561225830935));
#45458=CARTESIAN_POINT('Ctrl Pts',(2.15887237555029,3.88249361470115,19.5581590360687));
#45459=CARTESIAN_POINT('Ctrl Pts',(2.27969637656572,3.81958462748645,19.5550732958053));
#45460=CARTESIAN_POINT('Ctrl Pts',(2.39752111769151,3.75127894449634,19.5519939357949));
#45461=CARTESIAN_POINT('Ctrl Pts',(2.51190593036526,3.67777150955579,19.5489176847461));
#45462=CARTESIAN_POINT('Ctrl Pts',(2.62522809247125,3.60494696874821,19.5458700124906));
#45463=CARTESIAN_POINT('Ctrl Pts',(2.73517470696147,3.52701649641376,19.5428253916997));
#45464=CARTESIAN_POINT('Ctrl Pts',(2.84129224832913,3.44412553804493,19.5397806414099));
#45465=CARTESIAN_POINT('Ctrl Pts',(2.91209516263097,3.38881968242346,19.5377491469835));
#45466=CARTESIAN_POINT('Ctrl Pts',(2.98119295340959,3.33130466078434,19.5357175949077));
#45467=CARTESIAN_POINT('Ctrl Pts',(3.04844206982076,3.27161381566964,19.5336850403595));
#45468=CARTESIAN_POINT('Ctrl Pts',(3.08425226424725,3.23982840519718,19.5326027038555));
#45469=CARTESIAN_POINT('Ctrl Pts',(3.1195381208217,3.20742589648737,19.5315200830935));
#45470=CARTESIAN_POINT('Ctrl Pts',(3.15427695670459,3.17441047942531,19.5304370354107));
#45471=CARTESIAN_POINT('Ctrl Pts',(3.16725486117647,3.16207641819842,19.5300324251523));
#45472=CARTESIAN_POINT('Ctrl Pts',(3.18015812731145,3.14965513440157,19.5296277011351));
#45473=CARTESIAN_POINT('Ctrl Pts',(3.19297991753168,3.13715232569191,19.5292230337074));
#45474=CARTESIAN_POINT('Ctrl Pts',(3.21028959746143,3.12027327734767,19.5286767243753));
#45475=CARTESIAN_POINT('Ctrl Pts',(3.22744427955767,3.10325207454711,19.5281307247594));
#45476=CARTESIAN_POINT('Ctrl Pts',(3.24444163127926,3.08608990264034,19.5275850170264));
#45477=CARTESIAN_POINT('Ctrl Pts',(3.33717764080849,2.99245464912803,19.5246076851246));
#45478=CARTESIAN_POINT('Ctrl Pts',(3.42523294755332,2.89462674101026,19.5216390416869));
#45479=CARTESIAN_POINT('Ctrl Pts',(3.50859096128539,2.79305369138356,19.5186761904996));
#45480=CARTESIAN_POINT('Ctrl Pts',(3.59397640033088,2.68901019215335,19.5156412771407));
#45481=CARTESIAN_POINT('Ctrl Pts',(3.67443362705331,2.58103662340854,19.5126124412155));
#45482=CARTESIAN_POINT('Ctrl Pts',(3.74990902226373,2.46957232453757,19.5095865700048));
#45483=CARTESIAN_POINT('Ctrl Pts',(3.82667993619766,2.35619476524857,19.5065087603736));
#45484=CARTESIAN_POINT('Ctrl Pts',(3.89829689144343,2.23920494837555,19.5034340181076));
#45485=CARTESIAN_POINT('Ctrl Pts',(3.96466142958627,2.11903192999767,19.5003590674328));
#45486=CARTESIAN_POINT('Ctrl Pts',(4.0309620923612,1.99897457724446,19.4972870763748));
#45487=CARTESIAN_POINT('Ctrl Pts',(4.09202070623594,1.87573937136613,19.4942148773091));
#45488=CARTESIAN_POINT('Ctrl Pts',(4.14769296331372,1.74973219296001,19.4911392039111));
#45489=CARTESIAN_POINT('Ctrl Pts',(4.15491534612853,1.73338523439156,19.4907401956463));
#45490=CARTESIAN_POINT('Ctrl Pts',(4.16204794028702,1.71698942368025,19.490341076027));
#45491=CARTESIAN_POINT('Ctrl Pts',(4.1690873140012,1.70055278577387,19.4899420115644));
#45492=CARTESIAN_POINT('Ctrl Pts',(4.2235955422653,1.57327839358026,19.4868519217777));
#45493=CARTESIAN_POINT('Ctrl Pts',(4.27240340036226,1.44383040880503,19.4837717143479));
#45494=CARTESIAN_POINT('Ctrl Pts',(4.31545919855678,1.31266698606642,19.4806981622917));
#45495=CARTESIAN_POINT('Ctrl Pts',(4.35892069590576,1.18026765801579,19.4775956492703));
#45496=CARTESIAN_POINT('Ctrl Pts',(4.39652153701043,1.04611964222381,19.4744999176358));
#45497=CARTESIAN_POINT('Ctrl Pts',(4.42816288898243,0.910666566444117,19.4714076483225));
#45498=CARTESIAN_POINT('Ctrl Pts',(4.45971763719553,0.775584231634271,19.4683238426851));
#45499=CARTESIAN_POINT('Ctrl Pts',(4.48534571134421,0.639203155572113,19.4652434804418));
#45500=CARTESIAN_POINT('Ctrl Pts',(4.50489988856683,0.501947997482608,19.4621632697058));
#45501=CARTESIAN_POINT('Ctrl Pts',(4.5234656283834,0.371630903362032,19.4592387594872));
#45502=CARTESIAN_POINT('Ctrl Pts',(4.53655584516878,0.240525160569636,19.456314385846));
#45503=CARTESIAN_POINT('Ctrl Pts',(4.5440002395032,0.108991400598333,19.453387331288));
#45504=CARTESIAN_POINT('Ctrl Pts',(4.54553145652646,0.0819365827912304,
19.4527852734757));
#45505=CARTESIAN_POINT('Ctrl Pts',(4.54682366211308,0.0548636663001908,
19.4521831022411));
#45506=CARTESIAN_POINT('Ctrl Pts',(4.54787513450369,0.0277758132908992,
19.4515807930663));
#45507=CARTESIAN_POINT('Ctrl Pts',(4.54880630338109,0.00378719894119923,
19.4510473966946));
#45508=CARTESIAN_POINT('Ctrl Pts',(4.54954867988174,-0.0202170615304457,
19.450513804788));
#45509=CARTESIAN_POINT('Ctrl Pts',(4.5501006277934,-0.0442070954676754,
19.4499806150988));
#45510=CARTESIAN_POINT('Ctrl Pts',(4.55331420062987,-0.183882814458235,
19.4468762571225));
#45511=CARTESIAN_POINT('Ctrl Pts',(4.55008558494902,-0.323251293541528,
19.443781616557));
#45512=CARTESIAN_POINT('Ctrl Pts',(4.54031186270851,-0.461877411739,19.4406934171861));
#45513=CARTESIAN_POINT('Ctrl Pts',(4.53067866021077,-0.598510460562132,
19.4376496177859));
#45514=CARTESIAN_POINT('Ctrl Pts',(4.51468731171393,-0.734423134579881,
19.4346120756979));
#45515=CARTESIAN_POINT('Ctrl Pts',(4.49218947310497,-0.869204596926774,
19.4315776539935));
#45516=CARTESIAN_POINT('Ctrl Pts',(4.48129191999887,-0.934490341445224,
19.430107834059));
#45517=CARTESIAN_POINT('Ctrl Pts',(4.46886701290829,-0.999510687886201,
19.4286387462481));
#45518=CARTESIAN_POINT('Ctrl Pts',(4.45489347098868,-1.06421861098155,19.4271700340528));
#45519=CARTESIAN_POINT('Ctrl Pts',(4.42601008140308,-1.19797025124501,19.4241341977007));
#45520=CARTESIAN_POINT('Ctrl Pts',(4.39051333916906,-1.33038812058978,19.421099966171));
#45521=CARTESIAN_POINT('Ctrl Pts',(4.34872071354063,-1.46115895479143,19.4180641910325));
#45522=CARTESIAN_POINT('Ctrl Pts',(4.32227027711835,-1.54392345173146,19.416142857398));
#45523=CARTESIAN_POINT('Ctrl Pts',(4.29329690956391,-1.62602796166861,19.4142209054574));
#45524=CARTESIAN_POINT('Ctrl Pts',(4.26187123440312,-1.70738903830258,19.4122975370436));
#45525=CARTESIAN_POINT('Ctrl Pts',(4.25321767430855,-1.72979310639049,19.4117679069221));
#45526=CARTESIAN_POINT('Ctrl Pts',(4.24437655206198,-1.75214443843245,19.4112380817814));
#45527=CARTESIAN_POINT('Ctrl Pts',(4.23535981723739,-1.7744158038722,19.4107086515302));
#45528=CARTESIAN_POINT('Ctrl Pts',(4.18439432237877,-1.90030074813356,19.4077161409069));
#45529=CARTESIAN_POINT('Ctrl Pts',(4.12776551664013,-2.02378469411099,19.4047326389142));
#45530=CARTESIAN_POINT('Ctrl Pts',(4.06584469055636,-2.14458841387499,19.4017552111055));
#45531=CARTESIAN_POINT('Ctrl Pts',(4.00036068062891,-2.2723436859638,19.3986064496223));
#45532=CARTESIAN_POINT('Ctrl Pts',(3.92895803265593,-2.39710220266129,19.3954644815049));
#45533=CARTESIAN_POINT('Ctrl Pts',(3.85201703329039,-2.51851897272141,19.392325836016));
#45534=CARTESIAN_POINT('Ctrl Pts',(3.77655716323104,-2.63759844617919,19.3892476100675));
#45535=CARTESIAN_POINT('Ctrl Pts',(3.69576939240684,-2.75346420580146,19.3861725800561));
#45536=CARTESIAN_POINT('Ctrl Pts',(3.60996439826952,-2.86576656284731,19.3830974718481));
#45537=CARTESIAN_POINT('Ctrl Pts',(3.54413699183306,-2.95192207133902,19.3807383271401));
#45538=CARTESIAN_POINT('Ctrl Pts',(3.47535563877055,-3.03597991726489,19.3783791364089));
#45539=CARTESIAN_POINT('Ctrl Pts',(3.40374469167589,-3.11776882943693,19.3760184212987));
#45540=CARTESIAN_POINT('Ctrl Pts',(3.38306291872267,-3.14139007423622,19.3753366292557));
#45541=CARTESIAN_POINT('Ctrl Pts',(3.36214505086869,-3.16482198260282,19.3746547100648));
#45542=CARTESIAN_POINT('Ctrl Pts',(3.34099389843024,-3.18806021076517,19.3739726281131));
#45543=CARTESIAN_POINT('Ctrl Pts',(3.32373515295353,-3.20702195132993,19.3734160684253));
#45544=CARTESIAN_POINT('Ctrl Pts',(3.30632108269655,-3.22585473586077,19.3728594003699));
#45545=CARTESIAN_POINT('Ctrl Pts',(3.28875317708965,-3.24455615157313,19.372302604599));
#45546=CARTESIAN_POINT('Ctrl Pts',(3.27637002727884,-3.25773828253526,19.3719101340564));
#45547=CARTESIAN_POINT('Ctrl Pts',(3.26391669904378,-3.27084847479794,19.3715177984306));
#45548=CARTESIAN_POINT('Ctrl Pts',(3.25139510554647,-3.28388487669204,19.3711256274074));
#45549=CARTESIAN_POINT('Ctrl Pts',(3.15282448543269,-3.38650809465787,19.3680384371903));
#45550=CARTESIAN_POINT('Ctrl Pts',(3.05000398947139,-3.48458548857025,19.3649607083322));
#45551=CARTESIAN_POINT('Ctrl Pts',(2.94328170324704,-3.57779502158214,19.3618892172301));
#45552=CARTESIAN_POINT('Ctrl Pts',(2.83673480189425,-3.67085137626031,19.3588227737435));
#45553=CARTESIAN_POINT('Ctrl Pts',(2.72629835158367,-3.75905650319765,19.3557625475278));
#45554=CARTESIAN_POINT('Ctrl Pts',(2.61227793614804,-3.84205888933313,19.3527053308466));
#45555=CARTESIAN_POINT('Ctrl Pts',(2.49975879118773,-3.92396840950061,19.3496883675631));
#45556=CARTESIAN_POINT('Ctrl Pts',(2.38374884571102,-4.0008118415243,19.3466743350847));
#45557=CARTESIAN_POINT('Ctrl Pts',(2.26451075890163,-4.07221233820177,19.3436601507197));
#45558=CARTESIAN_POINT('Ctrl Pts',(2.15307182587664,-4.13894265382576,19.3408431188587));
#45559=CARTESIAN_POINT('Ctrl Pts',(2.03881261846325,-4.20091883876065,19.3380259543306));
#45560=CARTESIAN_POINT('Ctrl Pts',(1.92192917555825,-4.2577952663979,19.3352061406412));
#45561=CARTESIAN_POINT('Ctrl Pts',(1.89885610409831,-4.26902280938128,19.334649502668));
#45562=CARTESIAN_POINT('Ctrl Pts',(1.87568072700257,-4.28005149894805,19.3340927614631));
#45563=CARTESIAN_POINT('Ctrl Pts',(1.85240449004643,-4.29087848232892,19.3335358976687));
#45564=CARTESIAN_POINT('Ctrl Pts',(1.83464431921192,-4.29913965765674,19.3331110009753));
#45565=CARTESIAN_POINT('Ctrl Pts',(1.81682357432143,-4.30728417370212,19.3326859893584));
#45566=CARTESIAN_POINT('Ctrl Pts',(1.79895912167073,-4.315303623104,19.3322612385723));
#45567=CARTESIAN_POINT('Ctrl Pts',(1.72163150021165,-4.35001641054753,19.3304226729781));
#45568=CARTESIAN_POINT('Ctrl Pts',(1.64342321773675,-4.38241577414544,19.3285875039126));
#45569=CARTESIAN_POINT('Ctrl Pts',(1.56440032675076,-4.41242911636972,19.3267550510791));
#45570=CARTESIAN_POINT('Ctrl Pts',(1.43711047143297,-4.46077452542352,19.3238033410982));
#45571=CARTESIAN_POINT('Ctrl Pts',(1.30770822291801,-4.50293181836922,19.3208586788369));
#45572=CARTESIAN_POINT('Ctrl Pts',(1.17662145504096,-4.53906398417229,19.3179182210069));
#45573=CARTESIAN_POINT('Ctrl Pts',(1.04250946942332,-4.57603000735673,19.3149099033514));
#45574=CARTESIAN_POINT('Ctrl Pts',(0.906633655370345,-4.60668969161992,
19.3119059864259));
#45575=CARTESIAN_POINT('Ctrl Pts',(0.769431097467203,-4.63116704578967,
19.308903425512));
#45576=CARTESIAN_POINT('Ctrl Pts',(0.630182204159468,-4.65600947242755,
19.3058560822937));
#45577=CARTESIAN_POINT('Ctrl Pts',(0.489565915681568,-4.67448381748104,
19.3028101358377));
#45578=CARTESIAN_POINT('Ctrl Pts',(0.348028745832047,-4.68666735853543,
19.2997624031501));
#45579=CARTESIAN_POINT('Ctrl Pts',(0.276401735269172,-4.69283302247179,
19.2982200522494));
#45580=CARTESIAN_POINT('Ctrl Pts',(0.204538794597775,-4.69738677129886,
19.2966772438915));
#45581=CARTESIAN_POINT('Ctrl Pts',(0.132497794988,-4.70033357743951,19.2951335655473));
#45582=CARTESIAN_POINT('Ctrl Pts',(0.112510249077041,-4.70115115941847,
19.2947052769069));
#45583=CARTESIAN_POINT('Ctrl Pts',(0.092508998863809,-4.70184502431764,
19.2942769212978));
#45584=CARTESIAN_POINT('Ctrl Pts',(0.0724952864131179,-4.70241523264229,
19.2938484899096));
#45585=CARTESIAN_POINT('Ctrl Pts',(0.0524053747538238,-4.70298761194961,
19.2934184273332));
#45586=CARTESIAN_POINT('Ctrl Pts',(0.0323102430098365,-4.70343515128597,
19.2929884454936));
#45587=CARTESIAN_POINT('Ctrl Pts',(0.0122186816347883,-4.70375813703399,
19.2925586960882));
#45588=CARTESIAN_POINT('Ctrl Pts',(-0.130279647047385,-4.70604889624492,
19.2895107213251));
#45589=CARTESIAN_POINT('Ctrl Pts',(-0.272714799094277,-4.70208198168319,
19.2864719199788));
#45590=CARTESIAN_POINT('Ctrl Pts',(-0.414633190928799,-4.69200784465072,
19.2834391901245));
#45591=CARTESIAN_POINT('Ctrl Pts',(-0.558078433367512,-4.68182532348272,
19.2803738321848));
#45592=CARTESIAN_POINT('Ctrl Pts',(-0.70099656213896,-4.66540343587715,
19.277314677082));
#45593=CARTESIAN_POINT('Ctrl Pts',(-0.842927293052888,-4.64284438111864,
19.2742585216926));
#45594=CARTESIAN_POINT('Ctrl Pts',(-0.984668741071393,-4.62031541176288,
19.2712064420796));
#45595=CARTESIAN_POINT('Ctrl Pts',(-1.12542627120009,-4.59166551790643,
19.2681573541844));
#45596=CARTESIAN_POINT('Ctrl Pts',(-1.26473685825812,-4.5569449834536,19.2651080676816));
#45597=CARTESIAN_POINT('Ctrl Pts',(-1.40219852797764,-4.52268525675062,
19.2620992510297));
#45598=CARTESIAN_POINT('Ctrl Pts',(-1.53825218997399,-4.48251476703442,
19.259090241007));
#45599=CARTESIAN_POINT('Ctrl Pts',(-1.6724364842164,-4.43643407027143,19.2560779726351));
#45600=CARTESIAN_POINT('Ctrl Pts',(-1.69577574030498,-4.42841905488856,
19.2555540357366));
#45601=CARTESIAN_POINT('Ctrl Pts',(-1.71905838453956,-4.42022512285657,
19.2550300002629));
#45602=CARTESIAN_POINT('Ctrl Pts',(-1.74228191014027,-4.41185213332152,
19.2545058500857));
#45603=CARTESIAN_POINT('Ctrl Pts',(-1.76035515482698,-4.40533602154642,
19.2540979406852));
#45604=CARTESIAN_POINT('Ctrl Pts',(-1.77838477372036,-4.39871426481839,
19.2536901381687));
#45605=CARTESIAN_POINT('Ctrl Pts',(-1.79636551936284,-4.3919886694264,19.2532825296376));
#45606=CARTESIAN_POINT('Ctrl Pts',(-1.93187451941972,-4.34130230054732,
19.2502106534458));
#45607=CARTESIAN_POINT('Ctrl Pts',(-2.06468449537211,-4.28469503542289,
19.2471480732848));
#45608=CARTESIAN_POINT('Ctrl Pts',(-2.19433977491624,-4.22226508755719,
19.2440916139197));
#45609=CARTESIAN_POINT('Ctrl Pts',(-2.32196725551768,-4.1608115394395,19.2410829573521));
#45610=CARTESIAN_POINT('Ctrl Pts',(-2.44653872111971,-4.09371577322205,
19.23808023162));
#45611=CARTESIAN_POINT('Ctrl Pts',(-2.56760656005401,-4.02102358517923,
19.235080408152));
#45612=CARTESIAN_POINT('Ctrl Pts',(-2.68526160349352,-3.95038052574101,
19.2321651470591));
#45613=CARTESIAN_POINT('Ctrl Pts',(-2.79960837675168,-3.87445182317372,
19.229252626912));
#45614=CARTESIAN_POINT('Ctrl Pts',(-2.91021369160128,-3.79323796763903,
19.2263400681055));
#45615=CARTESIAN_POINT('Ctrl Pts',(-2.98399388261748,-3.73906359290253,
19.2243972216394));
#45616=CARTESIAN_POINT('Ctrl Pts',(-3.05610871619606,-3.68253657740801,
19.2224543579711));
#45617=CARTESIAN_POINT('Ctrl Pts',(-3.12651483591522,-3.62376762555295,
19.2205106520618));
#45618=CARTESIAN_POINT('Ctrl Pts',(-3.16741234664924,-3.58962991353437,
19.2193815920652));
#45619=CARTESIAN_POINT('Ctrl Pts',(-3.20773318569702,-3.55473559432281,
19.2182522478782));
#45620=CARTESIAN_POINT('Ctrl Pts',(-3.24746784403176,-3.51910539807467,
19.217122457792));
#45621=CARTESIAN_POINT('Ctrl Pts',(-3.26700401396051,-3.50158725150764,
19.2165669787208));
#45622=CARTESIAN_POINT('Ctrl Pts',(-3.28639847163628,-3.48389120743249,
19.21601139186));
#45623=CARTESIAN_POINT('Ctrl Pts',(-3.30565001708697,-3.46601967389373,
19.2154556779901));
#45624=CARTESIAN_POINT('Ctrl Pts',(-3.31923733798883,-3.45340633530117,
19.2150634672609));
#45625=CARTESIAN_POINT('Ctrl Pts',(-3.33275239972697,-3.44070650564925,
19.2146712232022));
#45626=CARTESIAN_POINT('Ctrl Pts',(-3.34618584616149,-3.42792978435657,
19.2142792032619));
#45627=CARTESIAN_POINT('Ctrl Pts',(-3.44713342315095,-3.33191726347047,
19.2113333126973));
#45628=CARTESIAN_POINT('Ctrl Pts',(-3.54361479719668,-3.23143681477532,
19.2083960349772));
#45629=CARTESIAN_POINT('Ctrl Pts',(-3.63553433126932,-3.126940879262,19.2054645714511));
#45630=CARTESIAN_POINT('Ctrl Pts',(-3.73049026986206,-3.01899309932707,
19.2024362720435));
#45631=CARTESIAN_POINT('Ctrl Pts',(-3.82057851236323,-2.90675969406161,
19.1994141772984));
#45632=CARTESIAN_POINT('Ctrl Pts',(-3.90566064499467,-2.79069444962541,
19.1963952019566));
#45633=CARTESIAN_POINT('Ctrl Pts',(-3.99147592842286,-2.67362907362455,
19.1933502121733));
#45634=CARTESIAN_POINT('Ctrl Pts',(-4.07219888206677,-2.55266483623709,
19.1903083957846));
#45635=CARTESIAN_POINT('Ctrl Pts',(-4.14764752468129,-2.42823151976782,
19.1872665870857));
#45636=CARTESIAN_POINT('Ctrl Pts',(-4.20306739838779,-2.33683055555379,
19.1850322638681));
#45637=CARTESIAN_POINT('Ctrl Pts',(-4.25564073821494,-2.24355706942676,
19.1827979447995));
#45638=CARTESIAN_POINT('Ctrl Pts',(-4.30527982057198,-2.14857260904585,
19.1805623752584));
#45639=CARTESIAN_POINT('Ctrl Pts',(-4.32699691910319,-2.10701690762921,
19.1795843135842));
#45640=CARTESIAN_POINT('Ctrl Pts',(-4.3481522027174,-2.06513363702578,19.1786060125617));
#45641=CARTESIAN_POINT('Ctrl Pts',(-4.36873745807105,-2.02293601505909,
19.1776273671286));
#45642=CARTESIAN_POINT('Ctrl Pts',(-4.38086243818899,-1.99808107308335,
19.1770509323837));
#45643=CARTESIAN_POINT('Ctrl Pts',(-4.39278964467502,-1.97311706816874,
19.1764743781503));
#45644=CARTESIAN_POINT('Ctrl Pts',(-4.40451730909724,-1.9480466787424,19.175897682959));
#45645=CARTESIAN_POINT('Ctrl Pts',(-4.4127985002692,-1.93034386255322,19.1754904643556));
#45646=CARTESIAN_POINT('Ctrl Pts',(-4.42097601800018,-1.91259691029446,
19.1750833804788));
#45647=CARTESIAN_POINT('Ctrl Pts',(-4.42904852534276,-1.89480918199437,
19.1746764755087));
#45648=CARTESIAN_POINT('Ctrl Pts',(-4.48950921559979,-1.76158436280397,
19.1716288777402));
#45649=CARTESIAN_POINT('Ctrl Pts',(-4.54410184606152,-1.62603381239176,
19.1685903704127));
#45650=CARTESIAN_POINT('Ctrl Pts',(-4.59268280744846,-1.48860776987399,
19.1655578531078));
#45651=CARTESIAN_POINT('Ctrl Pts',(-4.64144650306992,-1.35066480793007,
19.1625139291796));
#45652=CARTESIAN_POINT('Ctrl Pts',(-4.68415360775462,-1.21083146528599,
19.1594760404209));
#45653=CARTESIAN_POINT('Ctrl Pts',(-4.72061445405524,-1.06953622768658,
19.1564410512956));
#45654=CARTESIAN_POINT('Ctrl Pts',(-4.75671346962216,-0.929643178041525,
19.1534361808442));
#45655=CARTESIAN_POINT('Ctrl Pts',(-4.78668986944038,-0.78831633896503,
19.1504341527609));
#45656=CARTESIAN_POINT('Ctrl Pts',(-4.81031125214298,-0.645956691618861,
19.1474319239356));
#45657=CARTESIAN_POINT('Ctrl Pts',(-4.82807965738957,-0.538871347096197,
19.1451735964244));
#45658=CARTESIAN_POINT('Ctrl Pts',(-4.84225125518576,-0.431201234879474,
19.1429151553273));
#45659=CARTESIAN_POINT('Ctrl Pts',(-4.85270728658022,-0.32311529964396,
19.1406553054137));
#45660=CARTESIAN_POINT('Ctrl Pts',(-4.85885127437678,-0.259603758599947,
19.1393274124716));
#45661=CARTESIAN_POINT('Ctrl Pts',(-4.86371203457958,-0.195948633814534,
19.1379990330984));
#45662=CARTESIAN_POINT('Ctrl Pts',(-4.86726251019289,-0.132184380886881,
19.136669904511));
#45663=CARTESIAN_POINT('Ctrl Pts',(-4.86838059639054,-0.112104273637358,
19.1362513464105));
#45664=CARTESIAN_POINT('Ctrl Pts',(-4.86936819801155,-0.0920224658990377,
19.1358329041084));
#45665=CARTESIAN_POINT('Ctrl Pts',(-4.87022464687506,-0.0719445408679467,
19.1354146627671));
#45666=CARTESIAN_POINT('Ctrl Pts',(-4.87127693233824,-0.0472755739962392,
19.1349007858712));
#45667=CARTESIAN_POINT('Ctrl Pts',(-4.87213135174695,-0.0226102934020704,
19.134387167001));
#45668=CARTESIAN_POINT('Ctrl Pts',(-4.8727870952798,0.00204924970852941,
19.1338737912933));
#45669=CARTESIAN_POINT('',(0.446113671359645,4.91412736825422,19.058));
#45670=CARTESIAN_POINT('Ctrl Pts',(0.44649414690178,4.91265885279919,19.058));
#45671=CARTESIAN_POINT('Ctrl Pts',(0.299727560449543,4.91447193481392,19.0691244126311));
#45672=CARTESIAN_POINT('Ctrl Pts',(0.153167317909177,4.91005959431981,19.0802626720314));
#45673=CARTESIAN_POINT('Ctrl Pts',(0.00725046426545532,4.89944030839442,
19.0914270753353));
#45674=CARTESIAN_POINT('Ctrl Pts',(-0.137909608980915,4.88887609813179,
19.10253357579));
#45675=CARTESIAN_POINT('Ctrl Pts',(-0.282433758712205,4.87216902002991,
19.1136659496671));
#45676=CARTESIAN_POINT('Ctrl Pts',(-0.425882683147369,4.84928678485378,
19.1248363037588));
#45677=CARTESIAN_POINT('Ctrl Pts',(-0.565675808016648,4.82698770403557,
19.1357219810862));
#45678=CARTESIAN_POINT('Ctrl Pts',(-0.704448457143253,4.79882393308609,
19.1466437274425));
#45679=CARTESIAN_POINT('Ctrl Pts',(-0.841774914873059,4.76472078486696,
19.1576127473831));
#45680=CARTESIAN_POINT('Ctrl Pts',(-0.940805834192305,4.74012781002693,
19.1655228919155));
#45681=CARTESIAN_POINT('Ctrl Pts',(-1.0390843184423,4.71244522520194,19.1734576204009));
#45682=CARTESIAN_POINT('Ctrl Pts',(-1.13644149966956,4.68163105513636,19.181421134727));
#45683=CARTESIAN_POINT('Ctrl Pts',(-1.16730557623662,4.6718623776514,19.1839457201022));
#45684=CARTESIAN_POINT('Ctrl Pts',(-1.198076992637,4.66177888532038,19.1864731984846));
#45685=CARTESIAN_POINT('Ctrl Pts',(-1.22875016771071,4.65137899873876,19.1890037037495));
#45686=CARTESIAN_POINT('Ctrl Pts',(-1.24841289336978,4.644712257645,19.190625858309));
#45687=CARTESIAN_POINT('Ctrl Pts',(-1.26802854233492,4.6379177328912,19.1922487049096));
#45688=CARTESIAN_POINT('Ctrl Pts',(-1.28758810772402,4.63099805128267,19.1938716419773));
#45689=CARTESIAN_POINT('Ctrl Pts',(-1.41973360557623,4.58424830235176,19.204836293928));
#45690=CARTESIAN_POINT('Ctrl Pts',(-1.54943066798541,4.53175252800649,19.2158141351685));
#45691=CARTESIAN_POINT('Ctrl Pts',(-1.67628513679076,4.47348474855613,19.2268170475339));
#45692=CARTESIAN_POINT('Ctrl Pts',(-1.77854477370016,4.42651405823497,19.2356866903145));
#45693=CARTESIAN_POINT('Ctrl Pts',(-1.87895707987582,4.37579165399884,19.2445726249588));
#45694=CARTESIAN_POINT('Ctrl Pts',(-1.97730366067652,4.32128226154577,19.2534810756009));
#45695=CARTESIAN_POINT('Ctrl Pts',(-2.10058309475894,4.25295363233385,19.2646479991967));
#45696=CARTESIAN_POINT('Ctrl Pts',(-2.22061803115919,4.17867506623871,19.275850302475));
#45697=CARTESIAN_POINT('Ctrl Pts',(-2.3371003873209,4.09882401061829,19.2871002449437));
#45698=CARTESIAN_POINT('Ctrl Pts',(-2.45349352336119,4.01903411722977,19.2983415704744));
#45699=CARTESIAN_POINT('Ctrl Pts',(-2.56634003134295,3.93367951832198,19.3096304622446));
#45700=CARTESIAN_POINT('Ctrl Pts',(-2.67529062823455,3.84310647943015,19.3209791516131));
#45701=CARTESIAN_POINT('Ctrl Pts',(-2.71693531724479,3.80848632915125,19.3253170134781));
#45702=CARTESIAN_POINT('Ctrl Pts',(-2.75801032451888,3.77310349110297,19.3296636119694));
#45703=CARTESIAN_POINT('Ctrl Pts',(-2.79849428295858,3.73697648238141,19.3340196301562));
#45704=CARTESIAN_POINT('Ctrl Pts',(-2.81294818526249,3.72407813264686,19.335574850143));
#45705=CARTESIAN_POINT('Ctrl Pts',(-2.82732736116309,3.71108427106867,19.3371313434063));
#45706=CARTESIAN_POINT('Ctrl Pts',(-2.84161861583708,3.69800711896962,19.3386877998622));
#45707=CARTESIAN_POINT('Ctrl Pts',(-2.94391515755751,3.60440110145739,19.34982888694));
#45708=CARTESIAN_POINT('Ctrl Pts',(-3.04186033803071,3.50639786607989,19.3609841912936));
#45709=CARTESIAN_POINT('Ctrl Pts',(-3.13519298587128,3.40438402939327,19.3721662582028));
#45710=CARTESIAN_POINT('Ctrl Pts',(-3.22998005288867,3.30078049302696,19.3835225772406));
#45711=CARTESIAN_POINT('Ctrl Pts',(-3.32001032606879,3.19303967930977,19.3949064994243));
#45712=CARTESIAN_POINT('Ctrl Pts',(-3.4049668301135,3.08153340439932,19.4063311657064));
#45713=CARTESIAN_POINT('Ctrl Pts',(-3.48992333415822,2.97002712948888,19.4177558319884));
#45714=CARTESIAN_POINT('Ctrl Pts',(-3.56980658085615,2.85475460919877,19.4292212423689));
#45715=CARTESIAN_POINT('Ctrl Pts',(-3.64424819284547,2.73606613269444,19.4407405378004));
#45716=CARTESIAN_POINT('Ctrl Pts',(-3.69362849951562,2.65733498741996,19.4483817793834));
#45717=CARTESIAN_POINT('Ctrl Pts',(-3.74061319511361,2.57710031760525,19.4560467316635));
#45718=CARTESIAN_POINT('Ctrl Pts',(-3.78513614038734,2.49546231597417,19.463739230308));
#45719=CARTESIAN_POINT('Ctrl Pts',(-3.80567440292713,2.4578030214146,19.4672877501953));
#45720=CARTESIAN_POINT('Ctrl Pts',(-3.82568866999261,2.41984508871949,19.470842131787));
#45721=CARTESIAN_POINT('Ctrl Pts',(-3.84517166765662,2.38159830576804,19.4744027515965));
#45722=CARTESIAN_POINT('Ctrl Pts',(-3.85722034167954,2.35794573298872,19.4766047098446));
#45723=CARTESIAN_POINT('Ctrl Pts',(-3.86906582550741,2.33418269113951,19.4788090538567));
#45724=CARTESIAN_POINT('Ctrl Pts',(-3.88070630194933,2.310311496771,19.4810158726822));
#45725=CARTESIAN_POINT('Ctrl Pts',(-3.8885082527386,2.29431198982011,19.4824949781091));
#45726=CARTESIAN_POINT('Ctrl Pts',(-3.8962165975453,2.27826690602767,19.4839749160027));
#45727=CARTESIAN_POINT('Ctrl Pts',(-3.90382674774023,2.26218599112426,19.4854548878754));
#45728=CARTESIAN_POINT('Ctrl Pts',(-3.96414789534232,2.13472211503535,19.4971857472531));
#45729=CARTESIAN_POINT('Ctrl Pts',(-4.01838481417725,2.00484470453858,19.5089339279855));
#45730=CARTESIAN_POINT('Ctrl Pts',(-4.06640211675339,1.87293521419554,19.5207141703003));
#45731=CARTESIAN_POINT('Ctrl Pts',(-4.11224826252183,1.74699016109889,19.5319617555951));
#45732=CARTESIAN_POINT('Ctrl Pts',(-4.15242432683241,1.61919178653392,19.5432385686204));
#45733=CARTESIAN_POINT('Ctrl Pts',(-4.18676153681696,1.4898597689249,19.554557439162));
#45734=CARTESIAN_POINT('Ctrl Pts',(-4.2207524598163,1.36183205048544,19.5657621601394));
#45735=CARTESIAN_POINT('Ctrl Pts',(-4.24902179998014,1.23230080216518,19.5770080946197));
#45736=CARTESIAN_POINT('Ctrl Pts',(-4.27135507448881,1.1015746586975,19.588307688129));
#45737=CARTESIAN_POINT('Ctrl Pts',(-4.29323252438759,0.973516650317833,
19.5993766556815));
#45738=CARTESIAN_POINT('Ctrl Pts',(-4.30941374767392,0.844311453337346,
19.6104971142425));
#45739=CARTESIAN_POINT('Ctrl Pts',(-4.31964759244882,0.714256825545012,
19.621680762742));
#45740=CARTESIAN_POINT('Ctrl Pts',(-4.32157304106312,0.689787673591424,
19.6237849123534));
#45741=CARTESIAN_POINT('Ctrl Pts',(-4.32328781702124,0.665288489028016,
19.6258912988008));
#45742=CARTESIAN_POINT('Ctrl Pts',(-4.32479004603219,0.640761311051878,
19.628));
#45743=CARTESIAN_POINT('',(-3.60367707498796,3.37571982724537,19.058));
#45744=CARTESIAN_POINT('Origin',(0.,0.,19.058));
#45745=CARTESIAN_POINT('Ctrl Pts',(-4.8727870952798,0.00204924970852941,
19.1338737912933));
#45746=CARTESIAN_POINT('Ctrl Pts',(-4.87617886814195,0.129598459003725,
19.1312184028586));
#45747=CARTESIAN_POINT('Ctrl Pts',(-4.87425769241846,0.256993603559053,
19.1285695196845));
#45748=CARTESIAN_POINT('Ctrl Pts',(-4.86689403436298,0.383955746440246,
19.1259250851319));
#45749=CARTESIAN_POINT('Ctrl Pts',(-4.85865401760772,0.526027822131655,
19.1229659329201));
#45750=CARTESIAN_POINT('Ctrl Pts',(-4.84360044272571,0.667558209996482,
19.1200123512114));
#45751=CARTESIAN_POINT('Ctrl Pts',(-4.82205180462592,0.808202442374607,
19.117061458221));
#45752=CARTESIAN_POINT('Ctrl Pts',(-4.80012826355871,0.951293601552751,
19.1140592256271));
#45753=CARTESIAN_POINT('Ctrl Pts',(-4.77148144982624,1.09346818380839,19.1110597761218));
#45754=CARTESIAN_POINT('Ctrl Pts',(-4.73639180273002,1.23435901743,19.1080600748768));
#45755=CARTESIAN_POINT('Ctrl Pts',(-4.71189105823817,1.33273362650888,19.1059655849107));
#45756=CARTESIAN_POINT('Ctrl Pts',(-4.68424808585656,1.43048229055225,19.1038709722142));
#45757=CARTESIAN_POINT('Ctrl Pts',(-4.6535439006576,1.52747603119476,19.1017752037047));
#45758=CARTESIAN_POINT('Ctrl Pts',(-4.64011081963306,1.56991079272586,19.1008583049818));
#45759=CARTESIAN_POINT('Ctrl Pts',(-4.62609165763282,1.61220100164168,19.099941185029));
#45760=CARTESIAN_POINT('Ctrl Pts',(-4.61149254035212,1.65433555918283,19.0990237573359));
#45761=CARTESIAN_POINT('Ctrl Pts',(-4.60425406248102,1.6752265525563,19.098568881885));
#45762=CARTESIAN_POINT('Ctrl Pts',(-4.59687300609065,1.69607927843875,19.0981139307812));
#45763=CARTESIAN_POINT('Ctrl Pts',(-4.58935008303519,1.71689236429986,19.0976588934799));
#45764=CARTESIAN_POINT('Ctrl Pts',(-4.58288926961042,1.73476699408821,19.0972680997573));
#45765=CARTESIAN_POINT('Ctrl Pts',(-4.57632388063936,1.75261206193917,19.0968772491973));
#45766=CARTESIAN_POINT('Ctrl Pts',(-4.56965942251531,1.77041363655401,19.0964866227106));
#45767=CARTESIAN_POINT('Ctrl Pts',(-4.51879838731399,1.90626962008207,19.0935054849917));
#45768=CARTESIAN_POINT('Ctrl Pts',(-4.4621015938381,2.03978869153619,19.090533120728));
#45769=CARTESIAN_POINT('Ctrl Pts',(-4.39988991481362,2.17062521779186,19.0875666304161));
#45770=CARTESIAN_POINT('Ctrl Pts',(-4.33631291127845,2.304333139242,19.0845350362203));
#45771=CARTESIAN_POINT('Ctrl Pts',(-4.26697605411688,2.4352402172723,19.08150957663));
#45772=CARTESIAN_POINT('Ctrl Pts',(-4.19216902199247,2.5629660482269,19.0784871570202));
#45773=CARTESIAN_POINT('Ctrl Pts',(-4.11721282278043,2.69094656767373,19.0754587106304));
#45774=CARTESIAN_POINT('Ctrl Pts',(-4.03676418963347,2.81573387820879,19.0724333163567));
#45775=CARTESIAN_POINT('Ctrl Pts',(-3.95106744680097,2.93692273562437,19.0694078610249));
#45776=CARTESIAN_POINT('Ctrl Pts',(-3.86644065662709,3.05659850939287,19.0664201795206));
#45777=CARTESIAN_POINT('Ctrl Pts',(-3.77669549591118,3.17276577294219,19.0634324384734));
#45778=CARTESIAN_POINT('Ctrl Pts',(-3.68202832948565,3.28500209019142,19.0604416398662));
#45779=CARTESIAN_POINT('Ctrl Pts',(-3.65627454507218,3.31553548447098,19.0596280063176));
#45780=CARTESIAN_POINT('Ctrl Pts',(-3.63015628737134,3.34577773744076,19.0588141464826));
#45781=CARTESIAN_POINT('Ctrl Pts',(-3.60367707498796,3.37571982724537,19.058));
#45782=CARTESIAN_POINT('',(-4.,-4.89858719658941E-16,20.));
#45783=CARTESIAN_POINT('',(-4.5,-5.51091059616309E-16,19.5));
#45784=CARTESIAN_POINT('Origin',(0.,0.,20.));
#45785=CARTESIAN_POINT('Ctrl Pts',(2.86929757049748,-4.02374147429196,-0.329089653438089));
#45786=CARTESIAN_POINT('Ctrl Pts',(3.53627793941073,-3.54812315628632,-0.302707933007981));
#45787=CARTESIAN_POINT('Ctrl Pts',(4.61815699384527,-2.26074102389229,-0.249944492147766));
#45788=CARTESIAN_POINT('Ctrl Pts',(5.34305681190694,1.0543831002385,-0.144417610427336));
#45789=CARTESIAN_POINT('Ctrl Pts',(2.97075510791326,5.02204979956487,-0.0125090082767979));
#45790=CARTESIAN_POINT('Ctrl Pts',(-2.60167993603097,5.22655530852652,0.145781314303847));
#45791=CARTESIAN_POINT('Ctrl Pts',(-5.79544439621568,0.666623916928201,
0.304071636884492));
#45792=CARTESIAN_POINT('Ctrl Pts',(-3.71916882578288,-4.49661457488776,
0.462361959465137));
#45793=CARTESIAN_POINT('Ctrl Pts',(1.74534931250902,-5.56854608224957,0.620652282045782));
#45794=CARTESIAN_POINT('Ctrl Pts',(5.61966720797076,-1.57065337116734,0.778942604626428));
#45795=CARTESIAN_POINT('Ctrl Pts',(4.37934349714106,3.85645847095449,0.937232927207072));
#45796=CARTESIAN_POINT('Ctrl Pts',(-0.84775983002377,5.77341716827827,1.09552324978772));
#45797=CARTESIAN_POINT('Ctrl Pts',(-5.30296447800194,2.43487893547456,1.25381357236836));
#45798=CARTESIAN_POINT('Ctrl Pts',(-4.93115623773879,-3.11998211803485,
1.41210389494901));
#45799=CARTESIAN_POINT('Ctrl Pts',(-0.0706136094443395,-5.83485842583339,
1.57039421752965));
#45800=CARTESIAN_POINT('Ctrl Pts',(4.85417638956518,-3.23842638421833,1.7286845401103));
#45801=CARTESIAN_POINT('Ctrl Pts',(5.36037735273058,2.3058335652194,1.88697486269095));
#45802=CARTESIAN_POINT('Ctrl Pts',(0.98718650613642,5.75117077753662,2.04526518527159));
#45803=CARTESIAN_POINT('Ctrl Pts',(-4.28460500301765,3.96139458246299,2.20355550785224));
#45804=CARTESIAN_POINT('Ctrl Pts',(-5.65625702821141,-1.43431356080714,
2.36184583043288));
#45805=CARTESIAN_POINT('Ctrl Pts',(-1.87919427403712,-5.52441175942303,
2.52013615301353));
#45806=CARTESIAN_POINT('Ctrl Pts',(3.60843955214569,-4.58581057252521,2.67842647559417));
#45807=CARTESIAN_POINT('Ctrl Pts',(5.81142420090129,0.527110130500736,2.83671679817481));
#45808=CARTESIAN_POINT('Ctrl Pts',(2.72445125981257,5.16021910144056,2.99500712075546));
#45809=CARTESIAN_POINT('Ctrl Pts',(-2.84250423844022,5.09614219820049,3.15329744333611));
#45810=CARTESIAN_POINT('Ctrl Pts',(-5.82201720884499,0.393206705834578,
3.31158776591675));
#45811=CARTESIAN_POINT('Ctrl Pts',(-3.50193025017819,-4.66765255027645,
3.4698780884974));
#45812=CARTESIAN_POINT('Ctrl Pts',(2.00585411337058,-5.47969388429905,3.62816841107804));
#45813=CARTESIAN_POINT('Ctrl Pts',(5.68777231250098,-1.30374151751568,3.78645873365868));
#45814=CARTESIAN_POINT('Ctrl Pts',(4.19228952744401,4.05896591843996,3.94474905623933));
#45815=CARTESIAN_POINT('Ctrl Pts',(-1.11930309959379,5.72692381468561,4.10303937881998));
#45816=CARTESIAN_POINT('Ctrl Pts',(-5.41202917540188,2.18184234468851,4.26132970140061));
#45817=CARTESIAN_POINT('Ctrl Pts',(-4.77835461070898,-3.34930187121133,
4.41962002398127));
#45818=CARTESIAN_POINT('Ctrl Pts',(0.204906485773977,-5.83168150213524,
4.57791034656191));
#45819=CARTESIAN_POINT('Ctrl Pts',(5.00164762657821,-3.00566412467992,4.73620066914256));
#45820=CARTESIAN_POINT('Ctrl Pts',(5.24554559701654,2.55631516056015,4.8944909917232));
#45821=CARTESIAN_POINT('Ctrl Pts',(0.714587714204218,5.79136082533626,5.05278131430385));
#45822=CARTESIAN_POINT('Ctrl Pts',(-4.46683698218372,3.75471213080312,5.21107163688449));
#45823=CARTESIAN_POINT('Ctrl Pts',(-5.58223988624457,-1.69973340938259,
5.36936195946513));
#45824=CARTESIAN_POINT('Ctrl Pts',(-1.61630467165047,-5.60696486692776,
5.52765228204579));
#45825=CARTESIAN_POINT('Ctrl Pts',(3.82090205882377,-4.41035183034713,5.68594260462642));
#45826=CARTESIAN_POINT('Ctrl Pts',(5.78006132540833,0.800866334091529,5.84423292720708));
#45827=CARTESIAN_POINT('Ctrl Pts',(2.47781181352747,5.28308095975332,6.00252324978771));
#45828=CARTESIAN_POINT('Ctrl Pts',(-3.07991218091209,4.95627246713037,6.16081357236837));
#45829=CARTESIAN_POINT('Ctrl Pts',(-5.83408858766023,0.117924390593317,
6.319103894949));
#45830=CARTESIAN_POINT('Ctrl Pts',(-3.27767689138409,-4.82776656501236,
6.47739421752966));
#45831=CARTESIAN_POINT('Ctrl Pts',(2.26230141403803,-5.37889283427418,6.63568454011029));
#45832=CARTESIAN_POINT('Ctrl Pts',(5.7429776032295,-1.03378143694346,6.79397486269095));
#45833=CARTESIAN_POINT('Ctrl Pts',(3.99600116469878,4.25234882180315,6.95226518527158));
#45834=CARTESIAN_POINT('Ctrl Pts',(-1.38840996925396,5.66769914231875,7.11055550785224));
#45835=CARTESIAN_POINT('Ctrl Pts',(-5.50899499668582,1.92392046016856,7.26884583043288));
#45836=CARTESIAN_POINT('Ctrl Pts',(-4.61491443420867,-3.57114275484712,
7.42713615301353));
#45837=CARTESIAN_POINT('Ctrl Pts',(0.47997818700567,-5.81550657729517,7.58542647559416));
#45838=CARTESIAN_POINT('Ctrl Pts',(5.13796169871233,-2.76619691871885,7.74371679817482));
#45839=CARTESIAN_POINT('Ctrl Pts',(5.1190196099595,2.80109515072493,7.90200712075546));
#45840=CARTESIAN_POINT('Ctrl Pts',(0.440394310825021,5.81863804180648,8.06029744333611));
#45841=CARTESIAN_POINT('Ctrl Pts',(-4.63910813519642,3.53965697780435,8.21858776591675));
#45842=CARTESIAN_POINT('Ctrl Pts',(-5.49577575427904,-1.96136296213705,
8.3768780884974));
#45843=CARTESIAN_POINT('Ctrl Pts',(-1.34981084575569,-5.67701563246438,
8.53516841107803));
#45844=CARTESIAN_POINT('Ctrl Pts',(4.02484459618971,-4.22505879096223,8.69345873365869));
#45845=CARTESIAN_POINT('Ctrl Pts',(5.73581007047566,1.07283672848883,8.85174905623933));
#45846=CARTESIAN_POINT('Ctrl Pts',(2.22564729760008,5.39416257794014,9.01003937881998));
#45847=CARTESIAN_POINT('Ctrl Pts',(-3.31045249741171,4.80535119142661,9.16832970140062));
#45848=CARTESIAN_POINT('Ctrl Pts',(-5.83315107572507,-0.157620868961595,
9.32662002398126));
#45849=CARTESIAN_POINT('Ctrl Pts',(-3.04611493876333,-4.97711558941596,
9.48491034656191));
#45850=CARTESIAN_POINT('Ctrl Pts',(2.51370421497615,-5.26609788459876,9.64320066914256));
#45851=CARTESIAN_POINT('Ctrl Pts',(5.78537715735888,-0.761516222857186,
9.8014909917232));
#45852=CARTESIAN_POINT('Ctrl Pts',(3.79080248595607,4.43624980394858,9.95978131430386));
#45853=CARTESIAN_POINT('Ctrl Pts',(-1.6544209509478,5.59583658871751,10.1180716368845));
#45854=CARTESIAN_POINT('Ctrl Pts',(-5.59367681682763,1.66170860244797,10.2763619594652));
#45855=CARTESIAN_POINT('Ctrl Pts',(-4.44118388437089,-3.78502067573863,
10.4346522820458));
#45856=CARTESIAN_POINT('Ctrl Pts',(0.753979628983335,-5.78636418916428,
10.5929426046264));
#45857=CARTESIAN_POINT('Ctrl Pts',(5.26281910261167,-2.52056162466824,10.7512329272071));
#45858=CARTESIAN_POINT('Ctrl Pts',(4.98107919185876,3.03962923643596,10.9095232497877));
#45859=CARTESIAN_POINT('Ctrl Pts',(0.165218912680596,5.83294081244249,11.0678135723684));
#45860=CARTESIAN_POINT('Ctrl Pts',(-4.80103496763896,3.31670906925412,11.226103894949));
#45861=CARTESIAN_POINT('Ctrl Pts',(-5.3970570974028,-2.21861905200931,11.3843942175297));
#45862=CARTESIAN_POINT('Ctrl Pts',(-1.08030720079852,-5.73440774295545,
11.5426845401103));
#45863=CARTESIAN_POINT('Ctrl Pts',(4.219812502755,-4.03034468155729,11.7009748626909));
#45864=CARTESIAN_POINT('Ctrl Pts',(5.67876906018774,1.34241490293389,11.8592651852716));
#45865=CARTESIAN_POINT('Ctrl Pts',(1.96852001545618,5.49321624909424,12.0175555078522));
#45866=CARTESIAN_POINT('Ctrl Pts',(-3.53361114034896,4.64371490504813,12.1758458304329));
#45867=CARTESIAN_POINT('Ctrl Pts',(-5.81920675667964,-0.432814664237157,
12.3341361530135));
#45868=CARTESIAN_POINT('Ctrl Pts',(-2.80776073459116,-5.11536660151085,
12.4924264755942));
#45869=CARTESIAN_POINT('Ctrl Pts',(2.75950193807008,-5.14156054757227,12.6507167981748));
#45870=CARTESIAN_POINT('Ctrl Pts',(5.81487643104491,-0.487552973782061,
12.8090071207555));
#45871=CARTESIAN_POINT('Ctrl Pts',(3.57715104538901,4.61025880065714,12.9672974433361));
#45872=CARTESIAN_POINT('Ctrl Pts',(-1.91674289151962,5.51149639375472,13.1255877659167));
#45873=CARTESIAN_POINT('Ctrl Pts',(-5.66588581148519,1.39579145354196,13.2838780884974));
#45874=CARTESIAN_POINT('Ctrl Pts',(-4.25755034704318,-3.99045872713326,
13.442168411078));
#45875=CARTESIAN_POINT('Ctrl Pts',(1.02629984112814,-5.74431931969763,13.6004587336587));
#45876=CARTESIAN_POINT('Ctrl Pts',(5.37594143021732,-2.26930596206795,13.7587490562393));
#45877=CARTESIAN_POINT('Ctrl Pts',(4.8320319233711,3.27138553246996,13.91703937882));
#45878=CARTESIAN_POINT('Ctrl Pts',(-0.110324891911251,5.8342372448088,14.0753297014006));
#45879=CARTESIAN_POINT('Ctrl Pts',(-4.95225641377798,3.0863655361992,14.2336200239813));
#45880=CARTESIAN_POINT('Ctrl Pts',(-5.28630403923151,-2.47092804732617,
14.3919103465619));
#45881=CARTESIAN_POINT('Ctrl Pts',(-0.808394678245584,-5.77901322496909,
14.5502006691425));
#45882=CARTESIAN_POINT('Ctrl Pts',(4.40537103766032,-3.82664367730009,14.7084909917232));
#45883=CARTESIAN_POINT('Ctrl Pts',(5.60906548477092,1.60899975000773,14.8667813143038));
#45884=CARTESIAN_POINT('Ctrl Pts',(1.70700331210297,5.58002110223998,15.0250716368845));
#45885=CARTESIAN_POINT('Ctrl Pts',(-3.74889050980069,4.47172402646598,15.1833619594651));
#45886=CARTESIAN_POINT('Ctrl Pts',(-5.7922867217461,-0.707043367010812,
15.3416522820458));
#45887=CARTESIAN_POINT('Ctrl Pts',(-2.56314576668009,-5.24221132595445,
15.4999426046264));
#45888=CARTESIAN_POINT('Ctrl Pts',(2.99914650864464,-5.00555852161226,15.658232927207));
#45889=CARTESIAN_POINT('Ctrl Pts',(5.83140963307135,-0.2125025674033,15.8165232497877));
#45890=CARTESIAN_POINT('Ctrl Pts',(3.35552327049972,4.77398779042229,15.9748135723683));
#45891=CARTESIAN_POINT('Ctrl Pts',(-2.17479091272675,5.41486664825819,16.133103894949));
#45892=CARTESIAN_POINT('Ctrl Pts',(-5.72546087416986,1.12676190338666,16.2913942175296));
#45893=CARTESIAN_POINT('Ctrl Pts',(-4.06442347000951,-4.18699871789581,
16.4496845401103));
#45894=CARTESIAN_POINT('Ctrl Pts',(1.29633194620277,-5.68946591914921,16.6079748626909));
#45895=CARTESIAN_POINT('Ctrl Pts',(5.47707578180272,-2.01298980380955,16.7662651852716));
#45896=CARTESIAN_POINT('Ctrl Pts',(4.67221141036031,3.49584654228241,16.9245555078522));
#45897=CARTESIAN_POINT('Ctrl Pts',(-0.385625099973721,5.82252583304098,
17.0828458304329));
#45898=CARTESIAN_POINT('Ctrl Pts',(-5.09243067800049,2.84913735309004,17.2411361530135));
#45899=CARTESIAN_POINT('Ctrl Pts',(-5.163772332666,-2.71772228672297,17.3994264755942));
#45900=CARTESIAN_POINT('Ctrl Pts',(-0.534662778757779,-5.81074229086598,
17.5577167981748));
#45901=CARTESIAN_POINT('Ctrl Pts',(4.58107430334251,-3.61439149963352,17.7160071207555));
#45902=CARTESIAN_POINT('Ctrl Pts',(5.52691620363093,1.87196148635973,17.8742974433361));
#45903=CARTESIAN_POINT('Ctrl Pts',(1.44156288337564,5.6544511543935,18.0325877659168));
#45904=CARTESIAN_POINT('Ctrl Pts',(-3.95558608138272,4.2896328856293,18.1908780884974));
#45905=CARTESIAN_POINT('Ctrl Pts',(-5.75288016701676,-0.979448557484372,
18.349168411078));
#45906=CARTESIAN_POINT('Ctrl Pts',(-2.31199479018177,-5.35783906812632,
18.5074587336587));
#45907=CARTESIAN_POINT('Ctrl Pts',(3.23053211221357,-4.8574916848313,18.6657490562393));
#45908=CARTESIAN_POINT('Ctrl Pts',(5.83796734686214,0.0612873527283092,
18.82403937882));
#45909=CARTESIAN_POINT('Ctrl Pts',(3.12041701848007,4.9304530959418,18.9823297014006));
#45910=CARTESIAN_POINT('Ctrl Pts',(-1.49215234175522,5.23769617354117,19.1142383035512));
#45911=CARTESIAN_POINT('Ctrl Pts',(-4.11442054260868,3.08380732139205,19.2197651852716));
#45912=CARTESIAN_POINT('Ctrl Pts',(-4.76857407193705,1.53464683800148,19.2725286261318));
#45913=CARTESIAN_POINT('Ctrl Pts',(-4.8886350428845,0.724300640260437,19.2989103465619));
#45914=CARTESIAN_POINT('Ctrl Pts',(2.75898463274061,-3.86904481704479,-0.21939310229206));
#45915=CARTESIAN_POINT('Ctrl Pts',(3.40032229220555,-3.4117121081895,-0.193011381861952));
#45916=CARTESIAN_POINT('Ctrl Pts',(4.44060745341011,-2.17382463487172,-0.140247941001737));
#45917=CARTESIAN_POINT('Ctrl Pts',(5.13763779242852,1.01384631572915,-0.0347210592813072));
#45918=CARTESIAN_POINT('Ctrl Pts',(2.85654153638278,4.82897220710893,0.0971875428692309));
#45919=CARTESIAN_POINT('Ctrl Pts',(-2.50165581870078,5.02561530273532,0.255477865449875));
#45920=CARTESIAN_POINT('Ctrl Pts',(-5.57263289575413,0.640994911623377,
0.413768188030522));
#45921=CARTESIAN_POINT('Ctrl Pts',(-3.5761817604452,-4.32373785104547,0.572058510611166));
#45922=CARTESIAN_POINT('Ctrl Pts',(1.67824765945831,-5.35445790830635,0.730348833191812));
#45923=CARTESIAN_POINT('Ctrl Pts',(5.4036136325935,-1.51026807361131,0.888639155772457));
#45924=CARTESIAN_POINT('Ctrl Pts',(4.2109753740215,3.70819317158555,1.0469294783531));
#45925=CARTESIAN_POINT('Ctrl Pts',(-0.815166878242221,5.55145252603366,
1.20521980093375));
#45926=CARTESIAN_POINT('Ctrl Pts',(-5.09908684732198,2.3412676449565,1.36351012351439));
#45927=CARTESIAN_POINT('Ctrl Pts',(-4.74157313673304,-3.0000313688591,1.52180044609504));
#45928=CARTESIAN_POINT('Ctrl Pts',(-0.0678988005016982,-5.6105316146419,
1.68009076867568));
#45929=CARTESIAN_POINT('Ctrl Pts',(4.66755285374621,-3.11392192994849,1.83838109125633));
#45930=CARTESIAN_POINT('Ctrl Pts',(5.15429242820228,2.21718354955942,1.99667141383697));
#45931=CARTESIAN_POINT('Ctrl Pts',(0.94923316008907,5.53006141943627,2.15496173641762));
#45932=CARTESIAN_POINT('Ctrl Pts',(-4.11987919351274,3.8090949121538,2.31325205899827));
#45933=CARTESIAN_POINT('Ctrl Pts',(-5.43879672158246,-1.37916997995865,
2.47154238157891));
#45934=CARTESIAN_POINT('Ctrl Pts',(-1.80694682117044,-5.31202037247638,
2.62983270415955));
#45935=CARTESIAN_POINT('Ctrl Pts',(3.46970958150474,-4.40950462174014,2.7881230267402));
#45936=CARTESIAN_POINT('Ctrl Pts',(5.58799834129561,0.506844868502552,2.94641334932084));
#45937=CARTESIAN_POINT('Ctrl Pts',(2.61970707944744,4.96182945569518,3.10470367190149));
#45938=CARTESIAN_POINT('Ctrl Pts',(-2.73322139641198,4.90021605136558,3.26299399448213));
#45939=CARTESIAN_POINT('Ctrl Pts',(-5.59818409073885,0.378089491324522,
3.42128431706278));
#45940=CARTESIAN_POINT('Ctrl Pts',(-3.3672951333158,-4.48820010500075,3.57957463964342));
#45941=CARTESIAN_POINT('Ctrl Pts',(1.92873709970399,-5.269021719585,3.73786496222407));
#45942=CARTESIAN_POINT('Ctrl Pts',(5.46910037009403,-1.25361790595597,3.89615528480471));
#45943=CARTESIAN_POINT('Ctrl Pts',(4.03111287624724,3.90291502315395,4.05444560738536));
#45944=CARTESIAN_POINT('Ctrl Pts',(-1.07627040252322,5.50674665467138,4.21273592996601));
#45945=CARTESIAN_POINT('Ctrl Pts',(-5.20395844627879,2.09795929218125,4.37102625254665));
#45946=CARTESIAN_POINT('Ctrl Pts',(-4.5946461169747,-3.22053470093006,4.5293165751273));
#45947=CARTESIAN_POINT('Ctrl Pts',(0.197028656494944,-5.60747683086738,
4.68760689770794));
#45948=CARTESIAN_POINT('Ctrl Pts',(4.80935441551997,-2.89010844202325,4.84589722028858));
#45949=CARTESIAN_POINT('Ctrl Pts',(5.04387549110129,2.45803513617603,5.00418754286923));
#45950=CARTESIAN_POINT('Ctrl Pts',(0.687114694030425,5.56870632173167,5.16247786544987));
#45951=CARTESIAN_POINT('Ctrl Pts',(-4.29510508687517,3.61035856850998,5.32076818803052));
#45952=CARTESIAN_POINT('Ctrl Pts',(-5.3676252406787,-1.63438550412508,5.47905851061116));
#45953=CARTESIAN_POINT('Ctrl Pts',(-1.55416426541541,-5.39139964541496,
5.63734883319181));
#45954=CARTESIAN_POINT('Ctrl Pts',(3.67400376032591,-4.24079156167736,5.79563915577246));
#45955=CARTESIAN_POINT('Ctrl Pts',(5.55784124207616,0.770076248402076,5.95392947835309));
#45956=CARTESIAN_POINT('Ctrl Pts',(2.38254992672651,5.07996777028487,6.11221980093375));
#45957=CARTESIAN_POINT('Ctrl Pts',(-2.9615019594687,4.76572374824029,6.27051012351439));
#45958=CARTESIAN_POINT('Ctrl Pts',(-5.60979137364659,0.113390672622288,
6.42880044609503));
#45959=CARTESIAN_POINT('Ctrl Pts',(-3.15166341316413,-4.64215838060276,
6.58709076867568));
#45960=CARTESIAN_POINT('Ctrl Pts',(2.17532503429963,-5.17209606403701,6.74538109125632));
#45961=CARTESIAN_POINT('Ctrl Pts',(5.52218323968972,-0.994036703430842,
6.90367141383697));
#45962=CARTESIAN_POINT('Ctrl Pts',(3.84237101065328,4.08886313257964,7.06196173641762));
#45963=CARTESIAN_POINT('Ctrl Pts',(-1.33503119666024,5.44979893247647,7.22025205899827));
#45964=CARTESIAN_POINT('Ctrl Pts',(-5.29719632218758,1.84995346554449,7.3785423815789));
#45965=CARTESIAN_POINT('Ctrl Pts',(-4.43748955713467,-3.43384669587891,
7.53683270415955));
#45966=CARTESIAN_POINT('Ctrl Pts',(0.461524958448211,-5.59192376675569,
7.6951230267402));
#45967=CARTESIAN_POINT('Ctrl Pts',(4.94042776047775,-2.65984778586643,7.85341334932084));
#45968=CARTESIAN_POINT('Ctrl Pts',(4.92221391876315,2.69340432137696,8.01170367190149));
#45969=CARTESIAN_POINT('Ctrl Pts',(0.42346292291388,5.59493483906605,8.16999399448214));
#45970=CARTESIAN_POINT('Ctrl Pts',(-4.46075310774047,3.40357142017932,8.32828431706278));
#45971=CARTESIAN_POINT('Ctrl Pts',(-5.28448530642128,-1.88595645408243,
8.48657463964342));
#45972=CARTESIAN_POINT('Ctrl Pts',(-1.29791605403297,-5.4587572410908,8.64486496222408));
#45973=CARTESIAN_POINT('Ctrl Pts',(3.87010552834755,-4.0626222935355,8.8031552848047));
#45974=CARTESIAN_POINT('Ctrl Pts',(5.51529126970868,1.03159047628066,8.96144560738537));
#45975=CARTESIAN_POINT('Ctrl Pts',(2.1400801210432,5.18677874754585,9.11973592996599));
#45976=CARTESIAN_POINT('Ctrl Pts',(-3.18317892911787,4.62060478787114,9.27802625254666));
#45977=CARTESIAN_POINT('Ctrl Pts',(-5.60888990527024,-0.151560981243543,
9.43631657512728));
#45978=CARTESIAN_POINT('Ctrl Pts',(-2.92900408518884,-4.78576553640322,
9.59460689770795));
#45979=CARTESIAN_POINT('Ctrl Pts',(2.41706240986782,-5.06363762598407,9.75289722028857));
#45980=CARTESIAN_POINT('Ctrl Pts',(5.56295270169353,-0.732238990493172,
9.91118754286925));
#45981=CARTESIAN_POINT('Ctrl Pts',(3.6450613948327,4.26569386247748,10.0694778654499));
#45982=CARTESIAN_POINT('Ctrl Pts',(-1.59081512725699,5.38069920469153,10.2277681880305));
#45983=CARTESIAN_POINT('Ctrl Pts',(-5.37862246733407,1.5978225979022,10.3860585106112));
#45984=CARTESIAN_POINT('Ctrl Pts',(-4.27043824737563,-3.63950187193647,
10.5443488331918));
#45985=CARTESIAN_POINT('Ctrl Pts',(0.724992148306133,-5.56390178610049,
10.7026391557725));
#45986=CARTESIAN_POINT('Ctrl Pts',(5.0604848999617,-2.42365617977001,10.8609294783531));
#45987=CARTESIAN_POINT('Ctrl Pts',(4.78957675429235,2.92276773199996,11.0192198009338));
#45988=CARTESIAN_POINT('Ctrl Pts',(0.158866910776627,5.60868772576421,11.1775101235144));
#45989=CARTESIAN_POINT('Ctrl Pts',(-4.61645450550797,3.18919496096631,11.335800446095));
#45990=CARTESIAN_POINT('Ctrl Pts',(-5.18956198439054,-2.13332208319472,
11.4940907686757));
#45991=CARTESIAN_POINT('Ctrl Pts',(-1.03877373901142,-5.51394285603487,
11.6523810912563));
#45992=CARTESIAN_POINT('Ctrl Pts',(4.05757770398459,-3.87539415757996,11.810671413837));
#45993=CARTESIAN_POINT('Ctrl Pts',(5.46044325657874,1.29080445543139,11.9689617364176));
#45994=CARTESIAN_POINT('Ctrl Pts',(1.89283834752078,5.28202420390446,12.1272520589983));
#45995=CARTESIAN_POINT('Ctrl Pts',(-3.39775802082929,4.4651827658415,12.2855423815789));
#45996=CARTESIAN_POINT('Ctrl Pts',(-5.59548168914238,-0.416174683216324,
12.4438327041595));
#45997=CARTESIAN_POINT('Ctrl Pts',(-2.69981364038388,-4.91870135377977,
12.6021230267402));
#45998=CARTESIAN_POINT('Ctrl Pts',(2.65341020026489,-4.94388824809053,12.7604133493208));
#45999=CARTESIAN_POINT('Ctrl Pts',(5.59131784709134,-0.468808525174477,
12.9187036719015));
#46000=CARTESIAN_POINT('Ctrl Pts',(3.43962399184309,4.43301291394634,13.0769939944821));
#46001=CARTESIAN_POINT('Ctrl Pts',(-1.84305184550816,5.29960155061157,13.2352843170628));
#46002=CARTESIAN_POINT('Ctrl Pts',(-5.44805531691171,1.34212889260043,13.3935746396434));
#46003=CARTESIAN_POINT('Ctrl Pts',(-4.0938646801192,-3.8370416574944,13.5518649622241));
#46004=CARTESIAN_POINT('Ctrl Pts',(0.986842744848443,-5.52347337256235,
13.7101552848047));
#46005=CARTESIAN_POINT('Ctrl Pts',(5.1692581295817,-2.18206028566305,13.8684456073854));
#46006=CARTESIAN_POINT('Ctrl Pts',(4.64625975310793,3.1456139316668,14.026735929966));
#46007=CARTESIAN_POINT('Ctrl Pts',(-0.106083344063608,5.60993431552639,
14.1850262525467));
#46008=CARTESIAN_POINT('Ctrl Pts',(-4.76186209596784,2.96770720923078,14.3433165751273));
#46009=CARTESIAN_POINT('Ctrl Pts',(-5.08306693533551,-2.37593081361676,
14.5016068977079));
#46010=CARTESIAN_POINT('Ctrl Pts',(-0.777315158037826,-5.55683343687841,
14.6598972202886));
#46011=CARTESIAN_POINT('Ctrl Pts',(4.23600226041317,-3.67952463669161,14.8181875428692));
#46012=CARTESIAN_POINT('Ctrl Pts',(5.39341950296062,1.54714018859507,14.9764778654499));
#46013=CARTESIAN_POINT('Ctrl Pts',(1.64137590835962,5.3654917599847,15.1347681880305));
#46014=CARTESIAN_POINT('Ctrl Pts',(-3.60476076539315,4.29980424398346,15.2930585106112));
#46015=CARTESIAN_POINT('Ctrl Pts',(-5.56959662115286,-0.679860396607744,
15.4513488331918));
#46016=CARTESIAN_POINT('Ctrl Pts',(-2.46460313299549,-5.04066940933542,
15.6096391557725));
#46017=CARTESIAN_POINT('Ctrl Pts',(2.88384140208001,-4.81311495238798,15.7679294783531));
#46018=CARTESIAN_POINT('Ctrl Pts',(5.60721541407427,-0.204332699372805,
15.9262198009337));
#46019=CARTESIAN_POINT('Ctrl Pts',(3.22651691246755,4.59044718334415,16.0845101235144));
#46020=CARTESIAN_POINT('Ctrl Pts',(-2.09117895938438,5.20668682972943,16.242800446095));
#46021=CARTESIAN_POINT('Ctrl Pts',(-5.50533995832764,1.08344244534466,16.4010907686757));
#46022=CARTESIAN_POINT('Ctrl Pts',(-3.90816275384159,-4.02602547702165,
16.5593810912563));
#46023=CARTESIAN_POINT('Ctrl Pts',(1.24649320282389,-5.47072886438628,16.717671413837));
#46024=CARTESIAN_POINT('Ctrl Pts',(5.26650427258732,-1.9355984515789,16.8759617364176));
#46025=CARTESIAN_POINT('Ctrl Pts',(4.49258369527158,3.36144531949132,17.0342520589983));
#46026=CARTESIAN_POINT('Ctrl Pts',(-0.370799367680139,5.59867316038258,
17.1925423815789));
#46027=CARTESIAN_POINT('Ctrl Pts',(-4.89664722417207,2.73959949451312,17.3508327041595));
#46028=CARTESIAN_POINT('Ctrl Pts',(-4.96524607948782,-2.61323680827755,
17.5091230267402));
#46029=CARTESIAN_POINT('Ctrl Pts',(-0.51410714784639,-5.58734264795531,
17.6674133493208));
#46030=CARTESIAN_POINT('Ctrl Pts',(4.40495044303595,-3.47543270057839,17.8257036719015));
#46031=CARTESIAN_POINT('Ctrl Pts',(5.31442853088914,1.79999210505495,17.9839939944821));
#46032=CARTESIAN_POINT('Ctrl Pts',(1.38614059526527,5.43706027634114,18.1422843170628));
#46033=CARTESIAN_POINT('Ctrl Pts',(-3.80350972455094,4.12471377428376,18.3005746396434));
#46034=CARTESIAN_POINT('Ctrl Pts',(-5.53170508977411,-0.941792704404255,
18.4588649622241));
#46035=CARTESIAN_POINT('Ctrl Pts',(-2.22310790023142,-5.15185173042014,
18.6171552848047));
#46036=CARTESIAN_POINT('Ctrl Pts',(3.1063311609144,-4.67074068925906,18.7754456073854));
#46037=CARTESIAN_POINT('Ctrl Pts',(5.61352101017582,0.0589311008023047,
18.933735929966));
#46038=CARTESIAN_POINT('Ctrl Pts',(3.00044954913339,4.74089702790683,19.0920262525466));
#46039=CARTESIAN_POINT('Ctrl Pts',(-1.43478509267926,5.03632784635119,19.2239348546972));
#46040=CARTESIAN_POINT('Ctrl Pts',(-3.95623764032305,2.96524734748178,19.3294617364176));
#46041=CARTESIAN_POINT('Ctrl Pts',(-4.58524160053518,1.47564584665783,19.3822251772778));
#46042=CARTESIAN_POINT('Ctrl Pts',(-4.70068671060039,0.696454197190917,
19.4086068977079));
#46043=CARTESIAN_POINT('Ctrl Pts',(2.64867169498374,-3.71434815979762,-0.109696551146031));
#46044=CARTESIAN_POINT('Ctrl Pts',(3.26436664500038,-3.27530106009269,-0.0833148307159233));
#46045=CARTESIAN_POINT('Ctrl Pts',(4.26305791297495,-2.08690824585116,-0.0305513898557082));
#46046=CARTESIAN_POINT('Ctrl Pts',(4.93221877295011,0.973309531219794,0.0749754918647217));
#46047=CARTESIAN_POINT('Ctrl Pts',(2.74232796485231,4.63589461465298,0.20688409401526));
#46048=CARTESIAN_POINT('Ctrl Pts',(-2.40163170137059,4.82467529694413,0.365174416595904));
#46049=CARTESIAN_POINT('Ctrl Pts',(-5.34982139529258,0.615365906318545,
0.52346473917655));
#46050=CARTESIAN_POINT('Ctrl Pts',(-3.43319469510752,-4.15086112720317,
0.681755061757195));
#46051=CARTESIAN_POINT('Ctrl Pts',(1.6111460064076,-5.14036973436311,0.84004538433784));
#46052=CARTESIAN_POINT('Ctrl Pts',(5.18756005721624,-1.44988277605528,0.998335706918485));
#46053=CARTESIAN_POINT('Ctrl Pts',(4.04260725090194,3.55992787221662,1.15662602949913));
#46054=CARTESIAN_POINT('Ctrl Pts',(-0.782573926460673,5.32948788378904,
1.31491635207978));
#46055=CARTESIAN_POINT('Ctrl Pts',(-4.89520921664203,2.24765635443844,1.47320667466042));
#46056=CARTESIAN_POINT('Ctrl Pts',(-4.55199003572729,-2.88008061968337,
1.63149699724107));
#46057=CARTESIAN_POINT('Ctrl Pts',(-0.065183991559061,-5.3862048034504,
1.78978731982171));
#46058=CARTESIAN_POINT('Ctrl Pts',(4.48092931792725,-2.98941747567865,1.94807764240236));
#46059=CARTESIAN_POINT('Ctrl Pts',(4.94820750367398,2.12853353389945,2.106367964983));
#46060=CARTESIAN_POINT('Ctrl Pts',(0.911279814041717,5.30895206133591,2.26465828756365));
#46061=CARTESIAN_POINT('Ctrl Pts',(-3.95515338400782,3.6567952418446,2.42294861014429));
#46062=CARTESIAN_POINT('Ctrl Pts',(-5.22133641495353,-1.32402639911015,
2.58123893272494));
#46063=CARTESIAN_POINT('Ctrl Pts',(-1.73469936830376,-5.09962898552972,
2.73952925530558));
#46064=CARTESIAN_POINT('Ctrl Pts',(3.33097961086378,-4.23319867095506,2.89781957788623));
#46065=CARTESIAN_POINT('Ctrl Pts',(5.36457248168994,0.486579606504366,3.05610990046687));
#46066=CARTESIAN_POINT('Ctrl Pts',(2.51496289908231,4.7634398099498,3.21440022304752));
#46067=CARTESIAN_POINT('Ctrl Pts',(-2.62393855438374,4.70428990453067,3.37269054562815));
#46068=CARTESIAN_POINT('Ctrl Pts',(-5.37435097263271,0.362972276814471,
3.53098086820881));
#46069=CARTESIAN_POINT('Ctrl Pts',(-3.23266001645341,-4.30874765972506,
3.68927119078945));
#46070=CARTESIAN_POINT('Ctrl Pts',(1.85162008603739,-5.05834955487095,3.8475615133701));
#46071=CARTESIAN_POINT('Ctrl Pts',(5.25042842768707,-1.20349429439626,4.00585183595074));
#46072=CARTESIAN_POINT('Ctrl Pts',(3.86993622505047,3.74686412786792,4.16414215853139));
#46073=CARTESIAN_POINT('Ctrl Pts',(-1.03323770545266,5.28656949465716,4.32243248111203));
#46074=CARTESIAN_POINT('Ctrl Pts',(-4.9958877171557,2.01407623967397,4.48072280369268));
#46075=CARTESIAN_POINT('Ctrl Pts',(-4.41093762324043,-3.09176753064878,
4.63901312627333));
#46076=CARTESIAN_POINT('Ctrl Pts',(0.18915082721592,-5.38327215959954,4.79730344885396));
#46077=CARTESIAN_POINT('Ctrl Pts',(4.61706120446174,-2.77455275936658,4.95559377143462));
#46078=CARTESIAN_POINT('Ctrl Pts',(4.84220538518603,2.3597551117919,5.11388409401526));
#46079=CARTESIAN_POINT('Ctrl Pts',(0.65964167385663,5.34605181812708,5.2721744165959));
#46080=CARTESIAN_POINT('Ctrl Pts',(-4.12337319156663,3.46600500621685,5.43046473917655));
#46081=CARTESIAN_POINT('Ctrl Pts',(-5.15301059511283,-1.56903759886758,
5.58875506175719));
#46082=CARTESIAN_POINT('Ctrl Pts',(-1.49202385918035,-5.17583442390216,
5.74704538433784));
#46083=CARTESIAN_POINT('Ctrl Pts',(3.52710546182805,-4.07123129300759,5.90533570691848));
#46084=CARTESIAN_POINT('Ctrl Pts',(5.33562115874398,0.739286162712621,6.06362602949913));
#46085=CARTESIAN_POINT('Ctrl Pts',(2.28728803992556,4.87685458081641,6.22191635207978));
#46086=CARTESIAN_POINT('Ctrl Pts',(-2.84309173802532,4.5751750293502,6.38020667466042));
#46087=CARTESIAN_POINT('Ctrl Pts',(-5.38549415963294,0.108856954651256,
6.53849699724107));
#46088=CARTESIAN_POINT('Ctrl Pts',(-3.02564993494416,-4.45655019619314,
6.6967873198217));
#46089=CARTESIAN_POINT('Ctrl Pts',(2.08834865456124,-4.96529929379983,6.85507764240235));
#46090=CARTESIAN_POINT('Ctrl Pts',(5.30138887614994,-0.954291969918219,
7.013367964983));
#46091=CARTESIAN_POINT('Ctrl Pts',(3.68874085660779,3.92537744335614,7.17165828756364));
#46092=CARTESIAN_POINT('Ctrl Pts',(-1.28165242406652,5.23189872263419,7.32994861014429));
#46093=CARTESIAN_POINT('Ctrl Pts',(-5.08539764768935,1.77598647092042,7.48823893272493));
#46094=CARTESIAN_POINT('Ctrl Pts',(-4.26006468006067,-3.2965506369107,7.64652925530558));
#46095=CARTESIAN_POINT('Ctrl Pts',(0.443071729890745,-5.36834095621621,
7.80481957788623));
#46096=CARTESIAN_POINT('Ctrl Pts',(4.74289382224317,-2.55349865301401,7.96310990046686));
#46097=CARTESIAN_POINT('Ctrl Pts',(4.7254082275668,2.58571349202899,8.12140022304752));
#46098=CARTESIAN_POINT('Ctrl Pts',(0.406531535002743,5.37123163632562,8.27969054562816));
#46099=CARTESIAN_POINT('Ctrl Pts',(-4.28239808028453,3.26748586255429,8.43798086820882));
#46100=CARTESIAN_POINT('Ctrl Pts',(-5.07319485856352,-1.81054994602781,
8.59627119078944));
#46101=CARTESIAN_POINT('Ctrl Pts',(-1.24602126231025,-5.24049884971722,
8.7545615133701));
#46102=CARTESIAN_POINT('Ctrl Pts',(3.71536646050538,-3.90018579610877,8.91285183595074));
#46103=CARTESIAN_POINT('Ctrl Pts',(5.29477246894171,0.99034422407249,9.07114215853139));
#46104=CARTESIAN_POINT('Ctrl Pts',(2.05451294448632,4.97939491715156,9.22943248111203));
#46105=CARTESIAN_POINT('Ctrl Pts',(-3.05590536082404,4.43585838431568,9.38772280369268));
#46106=CARTESIAN_POINT('Ctrl Pts',(-5.38462873481541,-0.145501093525492,
9.54601312627332));
#46107=CARTESIAN_POINT('Ctrl Pts',(-2.81189323161436,-4.59441548339048,
9.70430344885398));
#46108=CARTESIAN_POINT('Ctrl Pts',(2.32042060475949,-4.86117736736937,9.8625937714346));
#46109=CARTESIAN_POINT('Ctrl Pts',(5.34052824602817,-0.702961758129157,
10.0208840940153));
#46110=CARTESIAN_POINT('Ctrl Pts',(3.49932030370932,4.09513792100639,10.1791744165959));
#46111=CARTESIAN_POINT('Ctrl Pts',(-1.52720930356618,5.16556182066556,10.3374647391766));
#46112=CARTESIAN_POINT('Ctrl Pts',(-5.16356811784049,1.53393659335643,10.4957550617572));
#46113=CARTESIAN_POINT('Ctrl Pts',(-4.09969261038038,-3.49398306813431,
10.6540453843378));
#46114=CARTESIAN_POINT('Ctrl Pts',(0.69600466762893,-5.34143938303671,10.8123357069185));
#46115=CARTESIAN_POINT('Ctrl Pts',(4.85815069731172,-2.32675073487178,10.9706260294991));
#46116=CARTESIAN_POINT('Ctrl Pts',(4.59807431672593,2.80590622756395,11.1289163520798));
#46117=CARTESIAN_POINT('Ctrl Pts',(0.152514908872657,5.38443463908592,11.2872066746604));
#46118=CARTESIAN_POINT('Ctrl Pts',(-4.43187404337698,3.0616808526785,11.4454969972411));
#46119=CARTESIAN_POINT('Ctrl Pts',(-4.98206687137828,-2.04802511438014,
11.6037873198217));
#46120=CARTESIAN_POINT('Ctrl Pts',(-0.997240277224328,-5.29347796911429,
11.7620776424023));
#46121=CARTESIAN_POINT('Ctrl Pts',(3.89534290521418,-3.72044363360263,11.920367964983));
#46122=CARTESIAN_POINT('Ctrl Pts',(5.24211745296974,1.2391940079289,12.0786582875636));
#46123=CARTESIAN_POINT('Ctrl Pts',(1.81715667958537,5.07083215871469,12.2369486101443));
#46124=CARTESIAN_POINT('Ctrl Pts',(-3.26190490130962,4.28665062663486,12.3952389327249));
#46125=CARTESIAN_POINT('Ctrl Pts',(-5.37175662160512,-0.399534702195488,
12.5535292553056));
#46126=CARTESIAN_POINT('Ctrl Pts',(-2.59186654617659,-4.72203610604869,
12.7118195778862));
#46127=CARTESIAN_POINT('Ctrl Pts',(2.5473184624597,-4.74621594860878,12.8701099004669));
#46128=CARTESIAN_POINT('Ctrl Pts',(5.36775926313778,-0.450064076566892,
13.0284002230475));
#46129=CARTESIAN_POINT('Ctrl Pts',(3.30209693829715,4.25576702723554,13.1866905456282));
#46130=CARTESIAN_POINT('Ctrl Pts',(-1.76936079949669,5.08770670746843,13.3449808682088));
#46131=CARTESIAN_POINT('Ctrl Pts',(-5.23022482233823,1.28846633165889,13.5032711907894));
#46132=CARTESIAN_POINT('Ctrl Pts',(-3.93017901319522,-3.68362458785553,
13.6615615133701));
#46133=CARTESIAN_POINT('Ctrl Pts',(0.947385648568746,-5.30262742542707,
13.8198518359507));
#46134=CARTESIAN_POINT('Ctrl Pts',(4.96257482894607,-2.09481460925815,13.9781421585314));
#46135=CARTESIAN_POINT('Ctrl Pts',(4.46048758284477,3.01984233086364,14.136432481112));
#46136=CARTESIAN_POINT('Ctrl Pts',(-0.101841796215968,5.38563138624398,
14.2947228036927));
#46137=CARTESIAN_POINT('Ctrl Pts',(-4.57146777815769,2.84904888226236,14.4530131262733));
#46138=CARTESIAN_POINT('Ctrl Pts',(-4.87982983143951,-2.28093357990735,
14.611303448854));
#46139=CARTESIAN_POINT('Ctrl Pts',(-0.746235637830062,-5.33465364878775,
14.7695937714346));
#46140=CARTESIAN_POINT('Ctrl Pts',(4.06663348316603,-3.53240559608313,14.9278840940153));
#46141=CARTESIAN_POINT('Ctrl Pts',(5.17777352115031,1.48528062718241,15.0861744165959));
#46142=CARTESIAN_POINT('Ctrl Pts',(1.57574850461626,5.15096241772943,15.2444647391765));
#46143=CARTESIAN_POINT('Ctrl Pts',(-3.46063102098561,4.12788446150094,15.4027550617572));
#46144=CARTESIAN_POINT('Ctrl Pts',(-5.34690652055963,-0.652677426204677,
15.5610453843378));
#46145=CARTESIAN_POINT('Ctrl Pts',(-2.36606049931089,-4.83912749271637,
15.7193357069185));
#46146=CARTESIAN_POINT('Ctrl Pts',(2.76853629551539,-4.62067138316371,15.8776260294991));
#46147=CARTESIAN_POINT('Ctrl Pts',(5.3830211950772,-0.196162831342301,16.0359163520798));
#46148=CARTESIAN_POINT('Ctrl Pts',(3.09751055443537,4.406906576266,16.1942066746604));
#46149=CARTESIAN_POINT('Ctrl Pts',(-2.00756700604201,4.99850701120068,16.3524969972411));
#46150=CARTESIAN_POINT('Ctrl Pts',(-5.28521904248542,1.04012298730266,16.5107873198217));
#46151=CARTESIAN_POINT('Ctrl Pts',(-3.75190203767367,-3.86505223614748,
16.6690776424023));
#46152=CARTESIAN_POINT('Ctrl Pts',(1.19665445944501,-5.25199180962336,16.827367964983));
#46153=CARTESIAN_POINT('Ctrl Pts',(5.05593276337192,-1.85820709934824,16.9856582875636));
#46154=CARTESIAN_POINT('Ctrl Pts',(4.31295598018285,3.22704409670023,17.1439486101443));
#46155=CARTESIAN_POINT('Ctrl Pts',(-0.355973635386551,5.37482048772419,
17.3022389327249));
#46156=CARTESIAN_POINT('Ctrl Pts',(-4.70086377034365,2.63006163593618,17.4605292553056));
#46157=CARTESIAN_POINT('Ctrl Pts',(-4.76671982630963,-2.50875132983212,
17.6188195778862));
#46158=CARTESIAN_POINT('Ctrl Pts',(-0.493551516935001,-5.36394300504465,
17.7771099004669));
#46159=CARTESIAN_POINT('Ctrl Pts',(4.22882658272939,-3.33647390152326,17.9354002230475));
#46160=CARTESIAN_POINT('Ctrl Pts',(5.10194085814736,1.72802272375016,18.0936905456282));
#46161=CARTESIAN_POINT('Ctrl Pts',(1.3307183071549,5.21966939828879,18.2519808682088));
#46162=CARTESIAN_POINT('Ctrl Pts',(-3.65143336771916,3.95979466293823,18.4102711907895));
#46163=CARTESIAN_POINT('Ctrl Pts',(-5.31053001253145,-0.904136851324141,
18.5685615133701));
#46164=CARTESIAN_POINT('Ctrl Pts',(-2.13422101028107,-4.94586439271395,
18.7268518359507));
#46165=CARTESIAN_POINT('Ctrl Pts',(2.98213020961523,-4.48398969368682,18.8851421585314));
#46166=CARTESIAN_POINT('Ctrl Pts',(5.3890746734895,0.056574848876316,19.043432481112));
#46167=CARTESIAN_POINT('Ctrl Pts',(2.88048207978671,4.55134095987183,19.2017228036927));
#46168=CARTESIAN_POINT('Ctrl Pts',(-1.3774178436033,4.83495951916122,19.3336314058432));
#46169=CARTESIAN_POINT('Ctrl Pts',(-3.79805473803742,2.8466873735715,19.4391582875636));
#46170=CARTESIAN_POINT('Ctrl Pts',(-4.40190912913332,1.41664485531417,19.4919217284239));
#46171=CARTESIAN_POINT('Ctrl Pts',(-4.51273837831629,0.668607754121397,
19.518303448854));
#46172=CARTESIAN_POINT('Ctrl Pts',(2.53835875722687,-3.55965150255045,-1.94289029309402E-15));
#46173=CARTESIAN_POINT('Ctrl Pts',(3.1284109977952,-3.13889001199587,0.0263817204301056));
#46174=CARTESIAN_POINT('Ctrl Pts',(4.08550837253979,-1.9999918568306,0.0791451612903207));
#46175=CARTESIAN_POINT('Ctrl Pts',(4.72679975347169,0.932772746710439,0.184672043010751));
#46176=CARTESIAN_POINT('Ctrl Pts',(2.62811439332184,4.44281702219704,0.316580645161289));
#46177=CARTESIAN_POINT('Ctrl Pts',(-2.3016075840404,4.62373529115294,0.474870967741933));
#46178=CARTESIAN_POINT('Ctrl Pts',(-5.12700989483103,0.589736901013719,
0.633161290322578));
#46179=CARTESIAN_POINT('Ctrl Pts',(-3.29020762976984,-3.97798440336088,
0.791451612903224));
#46180=CARTESIAN_POINT('Ctrl Pts',(1.54404435335689,-4.92628156041988,0.949741935483869));
#46181=CARTESIAN_POINT('Ctrl Pts',(4.97150648183897,-1.38949747849925,1.10803225806451));
#46182=CARTESIAN_POINT('Ctrl Pts',(3.87423912778238,3.41166257284768,1.26632258064516));
#46183=CARTESIAN_POINT('Ctrl Pts',(-0.749980974679123,5.10752324154442,
1.42461290322581));
#46184=CARTESIAN_POINT('Ctrl Pts',(-4.69133158596208,2.15404506392038,1.58290322580645));
#46185=CARTESIAN_POINT('Ctrl Pts',(-4.36240693472153,-2.76012987050762,
1.7411935483871));
#46186=CARTESIAN_POINT('Ctrl Pts',(-0.0624691826164238,-5.16187799225891,
1.89948387096774));
#46187=CARTESIAN_POINT('Ctrl Pts',(4.29430578210828,-2.8649130214088,2.05777419354839));
#46188=CARTESIAN_POINT('Ctrl Pts',(4.74212257914569,2.03988351823947,2.21606451612903));
#46189=CARTESIAN_POINT('Ctrl Pts',(0.873326467994359,5.08784270323556,2.37435483870968));
#46190=CARTESIAN_POINT('Ctrl Pts',(-3.7904275745029,3.50449557153541,2.53264516129032));
#46191=CARTESIAN_POINT('Ctrl Pts',(-5.00387610832461,-1.26888281826166,
2.69093548387097));
#46192=CARTESIAN_POINT('Ctrl Pts',(-1.66245191543707,-4.88723759858308,
2.84922580645161));
#46193=CARTESIAN_POINT('Ctrl Pts',(3.19224964022283,-4.05689272016998,3.00751612903226));
#46194=CARTESIAN_POINT('Ctrl Pts',(5.14114662208426,0.466314344506177,3.1658064516129));
#46195=CARTESIAN_POINT('Ctrl Pts',(2.41021871871718,4.56505016420442,3.32409677419355));
#46196=CARTESIAN_POINT('Ctrl Pts',(-2.5146557123555,4.50836375769575,3.48238709677419));
#46197=CARTESIAN_POINT('Ctrl Pts',(-5.15051785452657,0.347855062304423,
3.64067741935484));
#46198=CARTESIAN_POINT('Ctrl Pts',(-3.09802489959102,-4.12929521444937,
3.79896774193548));
#46199=CARTESIAN_POINT('Ctrl Pts',(1.77450307237079,-4.84767739015689,3.95725806451612));
#46200=CARTESIAN_POINT('Ctrl Pts',(5.03175648528012,-1.15337068283656,4.11554838709677));
#46201=CARTESIAN_POINT('Ctrl Pts',(3.7087595738537,3.5908132325819,4.27383870967742));
#46202=CARTESIAN_POINT('Ctrl Pts',(-0.990205008382098,5.06639233464293,
4.43212903225806));
#46203=CARTESIAN_POINT('Ctrl Pts',(-4.7878169880326,1.93019318716672,4.59041935483871));
#46204=CARTESIAN_POINT('Ctrl Pts',(-4.22722912950617,-2.96300036036751,
4.74870967741935));
#46205=CARTESIAN_POINT('Ctrl Pts',(0.181272997936893,-5.15906748833169,
4.907));
#46206=CARTESIAN_POINT('Ctrl Pts',(4.4247679934035,-2.65899707670991,5.06529032258064));
#46207=CARTESIAN_POINT('Ctrl Pts',(4.64053527927078,2.26147508740778,5.22358064516129));
#46208=CARTESIAN_POINT('Ctrl Pts',(0.63216865368283,5.12339731452249,5.38187096774192));
#46209=CARTESIAN_POINT('Ctrl Pts',(-3.95164129625807,3.32165144392371,5.54016129032259));
#46210=CARTESIAN_POINT('Ctrl Pts',(-4.93839594954698,-1.50368969361007,
5.69845161290321));
#46211=CARTESIAN_POINT('Ctrl Pts',(-1.42988345294528,-4.96026920238937,
5.85674193548387));
#46212=CARTESIAN_POINT('Ctrl Pts',(3.38020716333018,-3.90167102433782,6.01503225806451));
#46213=CARTESIAN_POINT('Ctrl Pts',(5.11340107541181,0.708496077023162,6.17332258064516));
#46214=CARTESIAN_POINT('Ctrl Pts',(2.19202615312461,4.67374139134797,6.3316129032258));
#46215=CARTESIAN_POINT('Ctrl Pts',(-2.72468151658193,4.38462631046011,6.48990322580645));
#46216=CARTESIAN_POINT('Ctrl Pts',(-5.16119694561929,0.104323236680228,
6.64819354838708));
#46217=CARTESIAN_POINT('Ctrl Pts',(-2.8996364567242,-4.27094201178353,6.80648387096775));
#46218=CARTESIAN_POINT('Ctrl Pts',(2.00137227482285,-4.75850252356265,6.96477419354837));
#46219=CARTESIAN_POINT('Ctrl Pts',(5.08059451261016,-0.914547236405604,
7.12306451612904));
#46220=CARTESIAN_POINT('Ctrl Pts',(3.53511070256229,3.76189175413264,7.28135483870967));
#46221=CARTESIAN_POINT('Ctrl Pts',(-1.22827365147281,5.01399851279189,7.43964516129032));
#46222=CARTESIAN_POINT('Ctrl Pts',(-4.87359897319111,1.70201947629637,7.59793548387097));
#46223=CARTESIAN_POINT('Ctrl Pts',(-4.08263980298667,-3.1592545779425,7.75622580645161));
#46224=CARTESIAN_POINT('Ctrl Pts',(0.424618501333285,-5.14475814567673,
7.91451612903225));
#46225=CARTESIAN_POINT('Ctrl Pts',(4.54535988400859,-2.44714952016159,8.0728064516129));
#46226=CARTESIAN_POINT('Ctrl Pts',(4.52860253637045,2.47802266268103,8.23109677419354));
#46227=CARTESIAN_POINT('Ctrl Pts',(0.389600147091602,5.14752843358518,8.38938709677419));
#46228=CARTESIAN_POINT('Ctrl Pts',(-4.10404305282859,3.13140030492926,8.54767741935484));
#46229=CARTESIAN_POINT('Ctrl Pts',(-4.86190441070575,-1.73514343797319,
8.70596774193548));
#46230=CARTESIAN_POINT('Ctrl Pts',(-1.19412647058753,-5.02224045834365,
8.86425806451613));
#46231=CARTESIAN_POINT('Ctrl Pts',(3.56062739266322,-3.73774929868204,9.02254838709676));
#46232=CARTESIAN_POINT('Ctrl Pts',(5.07425366817473,0.949097971864315,9.18083870967742));
#46233=CARTESIAN_POINT('Ctrl Pts',(1.96894576792944,4.77201108675727,9.33912903225805));
#46234=CARTESIAN_POINT('Ctrl Pts',(-2.9286317925302,4.25111198076021,9.4974193548387));
#46235=CARTESIAN_POINT('Ctrl Pts',(-5.16036756436058,-0.139441205807441,
9.65570967741936));
#46236=CARTESIAN_POINT('Ctrl Pts',(-2.69478237803987,-4.40306543037773,
9.81399999999999));
#46237=CARTESIAN_POINT('Ctrl Pts',(2.22377879965116,-4.65871710875468,9.97229032258064));
#46238=CARTESIAN_POINT('Ctrl Pts',(5.11810379036282,-0.67368452576514,10.1305806451613));
#46239=CARTESIAN_POINT('Ctrl Pts',(3.35357921258595,3.92458197953528,10.2888709677419));
#46240=CARTESIAN_POINT('Ctrl Pts',(-1.46360347987537,4.95042443663959,10.4471612903226));
#46241=CARTESIAN_POINT('Ctrl Pts',(-4.94851376834693,1.47005058881065,10.6054516129032));
#46242=CARTESIAN_POINT('Ctrl Pts',(-3.92894697338513,-3.34846426433215,
10.7637419354839));
#46243=CARTESIAN_POINT('Ctrl Pts',(0.667017186951725,-5.11897697997292,
10.9220322580645));
#46244=CARTESIAN_POINT('Ctrl Pts',(4.65581649466175,-2.22984528997355,11.0803225806452));
#46245=CARTESIAN_POINT('Ctrl Pts',(4.40657187915952,2.68904472312794,11.2386129032258));
#46246=CARTESIAN_POINT('Ctrl Pts',(0.14616290696869,5.16018155240764,11.3969032258064));
#46247=CARTESIAN_POINT('Ctrl Pts',(-4.24729358124599,2.93416674439068,11.5551935483871));
#46248=CARTESIAN_POINT('Ctrl Pts',(-4.77457175836603,-1.96272814556555,
11.7134838709677));
#46249=CARTESIAN_POINT('Ctrl Pts',(-0.955706815437237,-5.07301308219371,
11.8717741935484));
#46250=CARTESIAN_POINT('Ctrl Pts',(3.73310810644377,-3.5654931096253,12.030064516129));
#46251=CARTESIAN_POINT('Ctrl Pts',(5.02379164936073,1.1875835604264,12.1883548387097));
#46252=CARTESIAN_POINT('Ctrl Pts',(1.74147501164997,4.85964011352491,12.3466451612903));
#46253=CARTESIAN_POINT('Ctrl Pts',(-3.12605178178994,4.10811848742822,12.504935483871));
#46254=CARTESIAN_POINT('Ctrl Pts',(-5.14803155406786,-0.382894721174656,
12.6632258064516));
#46255=CARTESIAN_POINT('Ctrl Pts',(-2.4839194519693,-4.5253708583176,12.8215161290323));
#46256=CARTESIAN_POINT('Ctrl Pts',(2.44122672465452,-4.54854364912704,12.9798064516129));
#46257=CARTESIAN_POINT('Ctrl Pts',(5.14420067918421,-0.431319627959304,
13.1380967741936));
#46258=CARTESIAN_POINT('Ctrl Pts',(3.16456988475122,4.07852114052473,13.2963870967742));
#46259=CARTESIAN_POINT('Ctrl Pts',(-1.69566975348524,4.87581186432528,13.4546774193548));
#46260=CARTESIAN_POINT('Ctrl Pts',(-5.01239432776474,1.23480377071736,13.6129677419355));
#46261=CARTESIAN_POINT('Ctrl Pts',(-3.76649334627126,-3.53020751821668,
13.7712580645161));
#46262=CARTESIAN_POINT('Ctrl Pts',(0.907928552289056,-5.08178147829179,
13.9295483870968));
#46263=CARTESIAN_POINT('Ctrl Pts',(4.75589152831045,-2.00756893285326,14.0878387096774));
#46264=CARTESIAN_POINT('Ctrl Pts',(4.2747154125816,2.89407073006048,14.2461290322581));
#46265=CARTESIAN_POINT('Ctrl Pts',(-0.0976002483683332,5.16132845696157,
14.4044193548387));
#46266=CARTESIAN_POINT('Ctrl Pts',(-4.38107346034753,2.73039055529394,14.5627096774194));
#46267=CARTESIAN_POINT('Ctrl Pts',(-4.67659272754351,-2.18593634619795,
14.721));
#46268=CARTESIAN_POINT('Ctrl Pts',(-0.715156117622299,-5.11247386069707,
14.8792903225806));
#46269=CARTESIAN_POINT('Ctrl Pts',(3.89726470591888,-3.38528655547465,15.0375806451613));
#46270=CARTESIAN_POINT('Ctrl Pts',(4.96212753934002,1.42342106576975,15.1958709677419));
#46271=CARTESIAN_POINT('Ctrl Pts',(1.5101211008729,4.93643307547415,15.3541612903226));
#46272=CARTESIAN_POINT('Ctrl Pts',(-3.31650127657807,3.95596467901843,15.5124516129032));
#46273=CARTESIAN_POINT('Ctrl Pts',(-5.1242164199664,-0.62549445580161,15.6707419354839));
#46274=CARTESIAN_POINT('Ctrl Pts',(-2.26751786562628,-4.63758557609733,
15.8290322580645));
#46275=CARTESIAN_POINT('Ctrl Pts',(2.65323118895075,-4.42822781393943,15.9873225806452));
#46276=CARTESIAN_POINT('Ctrl Pts',(5.15882697608013,-0.187992963311806,
16.1456129032258));
#46277=CARTESIAN_POINT('Ctrl Pts',(2.96850419640318,4.22336596918787,16.3039032258064));
#46278=CARTESIAN_POINT('Ctrl Pts',(-1.92395505269964,4.79032719267193,16.4621935483871));
#46279=CARTESIAN_POINT('Ctrl Pts',(-5.06509812664321,0.99680352926066,16.6204838709677));
#46280=CARTESIAN_POINT('Ctrl Pts',(-3.59564132150574,-3.70407899527331,
16.7787741935484));
#46281=CARTESIAN_POINT('Ctrl Pts',(1.14681571606612,-5.03325475486043,16.937064516129));
#46282=CARTESIAN_POINT('Ctrl Pts',(4.84536125415653,-1.78081574711759,17.0953548387097));
#46283=CARTESIAN_POINT('Ctrl Pts',(4.13332826509411,3.09264287390914,17.2536451612903));
#46284=CARTESIAN_POINT('Ctrl Pts',(-0.341147903092961,5.15096781506579,
17.411935483871));
#46285=CARTESIAN_POINT('Ctrl Pts',(-4.50508031651524,2.52052377735926,17.5702258064516));
#46286=CARTESIAN_POINT('Ctrl Pts',(-4.56819357313145,-2.40426585138671,
17.7285161290323));
#46287=CARTESIAN_POINT('Ctrl Pts',(-0.472995886023615,-5.14054336213398,
17.8868064516129));
#46288=CARTESIAN_POINT('Ctrl Pts',(4.05270272242283,-3.19751510246813,18.0450967741935));
#46289=CARTESIAN_POINT('Ctrl Pts',(4.88945318540557,1.65605334244537,18.2033870967742));
#46290=CARTESIAN_POINT('Ctrl Pts',(1.27529601904452,5.00227852023644,18.3616774193548));
#46291=CARTESIAN_POINT('Ctrl Pts',(-3.49935701088739,3.79487555159269,18.5199677419355));
#46292=CARTESIAN_POINT('Ctrl Pts',(-5.0893549352888,-0.866480998244023,
18.6782580645161));
#46293=CARTESIAN_POINT('Ctrl Pts',(-2.04533412033072,-4.73987705500777,
18.8365483870968));
#46294=CARTESIAN_POINT('Ctrl Pts',(2.85792925831606,-4.29723869811459,18.9948387096774));
#46295=CARTESIAN_POINT('Ctrl Pts',(5.16462833680317,0.0542185969503185,
19.1531290322581));
#46296=CARTESIAN_POINT('Ctrl Pts',(2.76051461044002,4.36178489183685,19.3114193548387));
#46297=CARTESIAN_POINT('Ctrl Pts',(-1.32005059452733,4.63359119197125,19.4433279569892));
#46298=CARTESIAN_POINT('Ctrl Pts',(-3.63987183575178,2.72812739966123,19.5488548387097));
#46299=CARTESIAN_POINT('Ctrl Pts',(-4.21857665773145,1.35764386397051,19.6016182795699));
#46300=CARTESIAN_POINT('Ctrl Pts',(-4.32479004603219,0.640761311051878,
19.628));
#46301=CARTESIAN_POINT('',(2.53835875722687,-3.55965150255045,0.));
#46302=CARTESIAN_POINT('Ctrl Pts',(2.53835875722687,-3.55965150255045,-1.94289029309402E-15));
#46303=CARTESIAN_POINT('Ctrl Pts',(3.1284109977952,-3.13889001199587,0.0263817204301056));
#46304=CARTESIAN_POINT('Ctrl Pts',(4.08550837253979,-1.9999918568306,0.0791451612903207));
#46305=CARTESIAN_POINT('Ctrl Pts',(4.72679975347169,0.932772746710439,0.184672043010751));
#46306=CARTESIAN_POINT('Ctrl Pts',(2.62811439332184,4.44281702219704,0.316580645161289));
#46307=CARTESIAN_POINT('Ctrl Pts',(-2.3016075840404,4.62373529115294,0.474870967741933));
#46308=CARTESIAN_POINT('Ctrl Pts',(-4.29378651801925,1.77938049543143,0.58648078871983));
#46309=CARTESIAN_POINT('Ctrl Pts',(-4.37763907935493,0.169045277724475,
0.645327168837512));
#46310=CARTESIAN_POINT('Ctrl Pts',(-4.37640441740291,0.00246357316762608,
0.651410108094978));
#46311=CARTESIAN_POINT('Ctrl Pts',(2.17571852337094,4.44456444733847,4.16333634234434E-17));
#46312=CARTESIAN_POINT('Ctrl Pts',(2.288553758881,4.38223977042994,4.80899030934479E-17));
#46313=CARTESIAN_POINT('Ctrl Pts',(2.39856816217823,4.31535914976362,1.26999648448827E-16));
#46314=CARTESIAN_POINT('Ctrl Pts',(2.50544378309707,4.24391302988421,1.37043154602168E-16));
#46315=CARTESIAN_POINT('Ctrl Pts',(2.62554044419194,4.16362867343386,1.45788230031228E-16));
#46316=CARTESIAN_POINT('Ctrl Pts',(2.7416747038151,4.07757963945051,2.86902645733316E-16));
#46317=CARTESIAN_POINT('Ctrl Pts',(2.85366454038282,3.98618686426695,3.64291929955129E-16));
#46318=CARTESIAN_POINT('Ctrl Pts',(2.9232629976869,3.92938888726778,4.12387140724083E-16));
#46319=CARTESIAN_POINT('Ctrl Pts',(2.99126006746036,3.87052620415169,6.62527936102846E-16));
#46320=CARTESIAN_POINT('Ctrl Pts',(3.05760444128136,3.80969336998723,7.21644966006352E-16));
#46321=CARTESIAN_POINT('Ctrl Pts',(3.09753791324214,3.7730773596537,7.57228213237312E-16));
#46322=CARTESIAN_POINT('Ctrl Pts',(3.13687250045182,3.73574748028041,-2.48343235400226E-16));
#46323=CARTESIAN_POINT('Ctrl Pts',(3.17559590361344,3.69772367591327,-3.60822483003176E-16));
#46324=CARTESIAN_POINT('Ctrl Pts',(3.19355313598542,3.68009086900739,-4.12982567637309E-16));
#46325=CARTESIAN_POINT('Ctrl Pts',(3.21137384475144,3.66231375739153,2.85386760819859E-16));
#46326=CARTESIAN_POINT('Ctrl Pts',(3.22905135321198,3.64440041383412,2.77555756156289E-16));
#46327=CARTESIAN_POINT('Ctrl Pts',(3.33032953777236,3.54177108012739,2.32690274271181E-16));
#46328=CARTESIAN_POINT('Ctrl Pts',(3.42697009782031,3.4346145361773,1.17947475774344E-16));
#46329=CARTESIAN_POINT('Ctrl Pts',(3.51879473621821,3.32334962039163,1.38777878078145E-16));
#46330=CARTESIAN_POINT('Ctrl Pts',(3.60865605635445,3.21446367875555,1.59162901995989E-16));
#46331=CARTESIAN_POINT('Ctrl Pts',(3.69390536375717,3.10164237133953,1.64416256607793E-16));
#46332=CARTESIAN_POINT('Ctrl Pts',(3.77433601631748,2.9852523894932,1.52655665885959E-16));
#46333=CARTESIAN_POINT('Ctrl Pts',(3.80952442681261,2.93433177243543,1.47510407445157E-16));
#46334=CARTESIAN_POINT('Ctrl Pts',(3.84378998451378,2.88272782098782,-1.03604202083645E-16));
#46335=CARTESIAN_POINT('Ctrl Pts',(3.87711279910771,2.83047021492504,-1.52655665885959E-16));
#46336=CARTESIAN_POINT('Ctrl Pts',(3.90167945166607,2.79194422402902,-1.88817985407716E-16));
#46337=CARTESIAN_POINT('Ctrl Pts',(3.92573367987553,2.75306295204808,1.37038491228682E-16));
#46338=CARTESIAN_POINT('Ctrl Pts',(3.94926693181774,2.71383814709955,1.2490009027033E-16));
#46339=CARTESIAN_POINT('Ctrl Pts',(3.95979885299727,2.69628372856808,1.19467747878689E-16));
#46340=CARTESIAN_POINT('Ctrl Pts',(3.97022193097802,2.67866796640904,3.81603872600368E-16));
#46341=CARTESIAN_POINT('Ctrl Pts',(3.98053410416003,2.66099477842828,3.7470027081099E-16));
#46342=CARTESIAN_POINT('Ctrl Pts',(4.05311436653015,2.53660541859884,3.26110587499023E-16));
#46343=CARTESIAN_POINT('Ctrl Pts',(4.12023044721824,2.40933003202768,5.80264781591426E-16));
#46344=CARTESIAN_POINT('Ctrl Pts',(4.1817056161975,2.27957303631144,5.41233724504764E-16));
#46345=CARTESIAN_POINT('Ctrl Pts',(4.24306352883745,2.15006353613803,5.02277114368784E-16));
#46346=CARTESIAN_POINT('Ctrl Pts',(4.29880233786649,2.01808110524174,-2.01806554237873E-16));
#46347=CARTESIAN_POINT('Ctrl Pts',(4.34869895497134,1.88400727320529,-2.08166817117217E-16));
#46348=CARTESIAN_POINT('Ctrl Pts',(4.3987130094648,1.74961788308838,-2.14542049601851E-16));
#46349=CARTESIAN_POINT('Ctrl Pts',(4.44285769397013,1.61312648052743,2.07700331834603E-16));
#46350=CARTESIAN_POINT('Ctrl Pts',(4.48085566800584,1.47490808725521,2.22044604925031E-16));
#46351=CARTESIAN_POINT('Ctrl Pts',(4.50935414853263,1.37124429230104,2.32802809742852E-16));
#46352=CARTESIAN_POINT('Ctrl Pts',(4.53439405643066,1.26660880723853,3.27090126933202E-16));
#46353=CARTESIAN_POINT('Ctrl Pts',(4.55583718119808,1.16116031586893,3.33066907387547E-16));
#46354=CARTESIAN_POINT('Ctrl Pts',(4.5647459632839,1.1173505800641,3.35550026579367E-16));
#46355=CARTESIAN_POINT('Ctrl Pts',(4.57303368750873,1.073400536371,3.93488937669688E-16));
#46356=CARTESIAN_POINT('Ctrl Pts',(4.58068946156208,1.02932171064127,4.16333634234434E-16));
#46357=CARTESIAN_POINT('Ctrl Pts',(4.58528213032192,1.00287899635937,4.3003807790138E-16));
#46358=CARTESIAN_POINT('Ctrl Pts',(4.58964820129846,0.976383975558462,1.1911498064296E-16));
#46359=CARTESIAN_POINT('Ctrl Pts',(4.59378028021791,0.949872636571533,1.38777878078145E-16));
#46360=CARTESIAN_POINT('Ctrl Pts',(4.61514939077547,0.812768833647209,2.40464858739661E-16));
#46361=CARTESIAN_POINT('Ctrl Pts',(4.63029132458926,0.675091193156248,-6.4053354410212E-17));
#46362=CARTESIAN_POINT('Ctrl Pts',(4.63900152451931,0.537186451104229,-1.38777878078145E-16));
#46363=CARTESIAN_POINT('Ctrl Pts',(4.64607280433788,0.42523000611001,-1.99442159083017E-16));
#46364=CARTESIAN_POINT('Ctrl Pts',(4.64890419840177,0.313123505052828,4.93108554065338E-16));
#46365=CARTESIAN_POINT('Ctrl Pts',(4.64736094433393,0.20105139156818,4.71844785465692E-16));
#46366=CARTESIAN_POINT('Ctrl Pts',(4.64544832051237,0.0621554064876461,
4.17736069944506E-16));
#46367=CARTESIAN_POINT('Ctrl Pts',(4.63681759992347,-0.0766885915146454,
3.72153370275118E-16));
#46368=CARTESIAN_POINT('Ctrl Pts',(4.62166663169142,-0.215038242011895,
4.16333634234434E-16));
#46369=CARTESIAN_POINT('Ctrl Pts',(4.60648817669052,-0.353638885370275,
4.605940496854E-16));
#46370=CARTESIAN_POINT('Ctrl Pts',(4.58476541728463,-0.491744202092864,
1.3585326957315E-16));
#46371=CARTESIAN_POINT('Ctrl Pts',(4.55664910490708,-0.628889846984247,
2.22044604925031E-16));
#46372=CARTESIAN_POINT('Ctrl Pts',(4.54627797904168,-0.679478086507271,
2.53837578891091E-16));
#46373=CARTESIAN_POINT('Ctrl Pts',(4.53503649423606,-0.729935498537829,
-4.17628381648536E-17));
#46374=CARTESIAN_POINT('Ctrl Pts',(4.52293072203927,-0.780237766000663,
-5.55111512312578E-17));
#46375=CARTESIAN_POINT('Ctrl Pts',(4.51852089045776,-0.798561630358381,
-6.05193195799785E-17));
#46376=CARTESIAN_POINT('Ctrl Pts',(4.51399616118864,-0.816865466942453,
-2.76721061431502E-16));
#46377=CARTESIAN_POINT('Ctrl Pts',(4.50936083932464,-0.835132869996713,
-2.77555756156289E-16));
#46378=CARTESIAN_POINT('Ctrl Pts',(4.47555258032973,-0.968368298245966,
-2.83643699187054E-16));
#46379=CARTESIAN_POINT('Ctrl Pts',(4.43581935723855,-1.09986196998026,4.56182438062644E-17));
#46380=CARTESIAN_POINT('Ctrl Pts',(4.39038959840621,-1.229200829575,5.55111512312578E-17));
#46381=CARTESIAN_POINT('Ctrl Pts',(4.34480983538931,-1.35896675219327,6.54367239740816E-17));
#46382=CARTESIAN_POINT('Ctrl Pts',(4.29349546516567,-1.48656440482432,-4.64120495657098E-16));
#46383=CARTESIAN_POINT('Ctrl Pts',(4.23662839209755,-1.61155805192221,-3.05311331771918E-16));
#46384=CARTESIAN_POINT('Ctrl Pts',(4.17976131902944,-1.7365516990201,-1.46502167886738E-16));
#46385=CARTESIAN_POINT('Ctrl Pts',(4.11734114389621,-1.85894212089202,1.98375931461375E-16));
#46386=CARTESIAN_POINT('Ctrl Pts',(4.04950702451708,-1.97826322671605,2.22044604925031E-16));
#46387=CARTESIAN_POINT('Ctrl Pts',(4.0039219578893,-2.05844795689127,2.37950141352824E-16));
#46388=CARTESIAN_POINT('Ctrl Pts',(3.95589106826036,-2.13724588577774,1.34209299017938E-16));
#46389=CARTESIAN_POINT('Ctrl Pts',(3.90547300064698,-2.21455451296583,1.66533453693773E-16));
#46390=CARTESIAN_POINT('Ctrl Pts',(3.88226355505238,-2.25014275467462,1.81413550152313E-16));
#46391=CARTESIAN_POINT('Ctrl Pts',(3.85854814303777,-2.28541527809141,-1.96535868138964E-16));
#46392=CARTESIAN_POINT('Ctrl Pts',(3.8343320388377,-2.32036145673223,-2.22044604925031E-16));
#46393=CARTESIAN_POINT('Ctrl Pts',(3.81846869581275,-2.34325379377416,-2.38754718097135E-16));
#46394=CARTESIAN_POINT('Ctrl Pts',(3.80239048915502,-2.36600608076709,-1.28420314193019E-17));
#46395=CARTESIAN_POINT('Ctrl Pts',(3.78609884210449,-2.38861523157554,0.));
#46396=CARTESIAN_POINT('Ctrl Pts',(3.77490538198125,-2.40414924279059,8.82334156561408E-18));
#46397=CARTESIAN_POINT('Ctrl Pts',(3.76361599384939,-2.41960894071961,1.65364095173029E-16));
#46398=CARTESIAN_POINT('Ctrl Pts',(3.7522346949218,-2.43498912758705,1.66533453693773E-16));
#46399=CARTESIAN_POINT('Ctrl Pts',(3.66941253061457,-2.54691135824948,1.75042922090602E-16));
#46400=CARTESIAN_POINT('Ctrl Pts',(3.58167249725696,-2.65470179052059,3.28026165867355E-16));
#46401=CARTESIAN_POINT('Ctrl Pts',(3.48928766288614,-2.75807107487432,2.22044604925031E-16));
#46402=CARTESIAN_POINT('Ctrl Pts',(3.39991887248819,-2.85806571111424,1.19522973854221E-16));
#46403=CARTESIAN_POINT('Ctrl Pts',(3.30620285470906,-2.9539234934181,-1.0442180859248E-16));
#46404=CARTESIAN_POINT('Ctrl Pts',(3.20834980062004,-3.04534562649001,-1.66533453693773E-16));
#46405=CARTESIAN_POINT('Ctrl Pts',(3.11144260907094,-3.13588405928502,-2.28044718163707E-16));
#46406=CARTESIAN_POINT('Ctrl Pts',(3.01047744826623,-3.22207261031851,3.41219002678743E-16));
#46407=CARTESIAN_POINT('Ctrl Pts',(2.90563068007557,-3.30357847782834,3.33066907387547E-16));
#46408=CARTESIAN_POINT('Ctrl Pts',(2.80291415997029,-3.38342833131688,3.25080444148589E-16));
#46409=CARTESIAN_POINT('Ctrl Pts',(2.69647166403099,-3.45878415557578,1.92670969748543E-16));
#46410=CARTESIAN_POINT('Ctrl Pts',(2.58644978075874,-3.52928668450907,1.66533453693773E-16));
#46411=CARTESIAN_POINT('Ctrl Pts',(2.57049460076127,-3.53951083724989,1.62743037088118E-16));
#46412=CARTESIAN_POINT('Ctrl Pts',(2.5544641189252,-3.54963283815124,3.31276988434876E-16));
#46413=CARTESIAN_POINT('Ctrl Pts',(2.53835875722692,-3.55965150255041,3.33066907387547E-16));
#46414=CARTESIAN_POINT('Ctrl Pts',(0.446494146901359,4.91265885279923,19.058));
#46415=CARTESIAN_POINT('Ctrl Pts',(1.22846295052447,4.84360722676543,19.0327765671335));
#46416=CARTESIAN_POINT('Ctrl Pts',(1.9933030120195,4.59769822736177,19.0075531342671));
#46417=CARTESIAN_POINT('Ctrl Pts',(2.65082820116331,4.18037408759279,18.9823297014006));
#46418=CARTESIAN_POINT('Ctrl Pts',(4.02626712794074,3.307397848204,18.9295662605404));
#46419=CARTESIAN_POINT('Ctrl Pts',(4.93211723740144,1.68434260046616,18.8768028196802));
#46420=CARTESIAN_POINT('Ctrl Pts',(4.95046975302369,0.05301847033729,18.82403937882));
#46421=CARTESIAN_POINT('Ctrl Pts',(4.96882226864594,-1.57830565979157,18.7712759379598));
#46422=CARTESIAN_POINT('Ctrl Pts',(4.09967719042974,-3.21789867231146,18.7185124970995));
#46423=CARTESIAN_POINT('Ctrl Pts',(2.74135016758908,-4.12108640912056,18.6657490562393));
#46424=CARTESIAN_POINT('Ctrl Pts',(1.38302314474846,-5.02427414592964,18.6129856153791));
#46425=CARTESIAN_POINT('Ctrl Pts',(-0.464485822716606,-5.19105660702797,
18.5602221745189));
#46426=CARTESIAN_POINT('Ctrl Pts',(-1.9617212025883,-4.54471608580352,18.5074587336587));
#46427=CARTESIAN_POINT('Ctrl Pts',(-3.45895658246008,-3.89837556457903,
18.4546952927985));
#46428=CARTESIAN_POINT('Ctrl Pts',(-4.60591837473846,-2.43891206103166,
18.4019318519383));
#46429=CARTESIAN_POINT('Ctrl Pts',(-4.87985025660527,-0.831000068739,18.349168411078));
#46430=CARTESIAN_POINT('Ctrl Pts',(-4.92631242249651,-0.558278714746532,
18.340219092271));
#46431=CARTESIAN_POINT('Ctrl Pts',(-4.94765902855038,-0.28128675460715,
18.3312697734639));
#46432=CARTESIAN_POINT('Ctrl Pts',(-4.94522242777803,-0.0039236424385497,
18.3223204546569));
#46433=CARTESIAN_POINT('Origin',(0.,0.,-1.84858989190501));
#46434=CARTESIAN_POINT('',(-2.53835875722683,-3.55965150255047,0.));
#46435=CARTESIAN_POINT('Ctrl Pts',(-2.54467524200888,-3.56229978442276,
-3.12521276218947E-15));
#46436=CARTESIAN_POINT('Ctrl Pts',(-1.45608504857279,-4.32913804450291,
0.0486930492780809));
#46437=CARTESIAN_POINT('Ctrl Pts',(1.60942354292801,-4.84594693373762,0.150182632030869));
#46438=CARTESIAN_POINT('Ctrl Pts',(4.96501177239675,-1.41203703483287,0.304468748258361));
#46439=CARTESIAN_POINT('Ctrl Pts',(3.88934922870828,3.39617009289883,0.462858348682473));
#46440=CARTESIAN_POINT('Ctrl Pts',(-0.732920742143878,5.1113964007393,0.621247949106584));
#46441=CARTESIAN_POINT('Ctrl Pts',(-3.9420462167219,2.72159457156631,0.749825130180767));
#46442=CARTESIAN_POINT('Ctrl Pts',(-4.36729319104836,0.635050406119092,
0.825605777780246));
#46443=CARTESIAN_POINT('Ctrl Pts',(-4.36535621882271,0.0014563306878905,
0.848589891905021));
#46444=CARTESIAN_POINT('Origin',(0.,0.,0.));
#46445=CARTESIAN_POINT('Ctrl Pts',(-1.91898364244012,3.92834389788461,-0.329089653438086));
#46446=CARTESIAN_POINT('Ctrl Pts',(-2.57055919540632,3.61005128897394,-0.302691386700734));
#46447=CARTESIAN_POINT('Ctrl Pts',(-3.7023655534584,2.64307614504004,-0.24989485322603));
#46448=CARTESIAN_POINT('Ctrl Pts',(-4.81630944128875,-0.146849281373132,
-0.144301786276623));
#46449=CARTESIAN_POINT('Ctrl Pts',(-3.3181593418561,-3.95557434013013,-0.0123104525898624));
#46450=CARTESIAN_POINT('Ctrl Pts',(1.52017634683108,-4.93727721897207,0.146079147834249));
#46451=CARTESIAN_POINT('Ctrl Pts',(4.96501177239675,-1.41203703483287,0.304468748258361));
#46452=CARTESIAN_POINT('Ctrl Pts',(3.88934922870828,3.39617009289883,0.462858348682473));
#46453=CARTESIAN_POINT('Ctrl Pts',(-0.732920742143878,5.1113964007393,0.621247949106584));
#46454=CARTESIAN_POINT('Ctrl Pts',(-4.68612688169979,2.16748556327014,0.779637549530696));
#46455=CARTESIAN_POINT('Ctrl Pts',(-4.36939265644683,-2.75114092476471,
0.938027149954809));
#46456=CARTESIAN_POINT('Ctrl Pts',(-0.0704529116473286,-5.16289724783097,
1.09641675037892));
#46457=CARTESIAN_POINT('Ctrl Pts',(4.29252819085395,-2.86947836000301,1.25480635080303));
#46458=CARTESIAN_POINT('Ctrl Pts',(4.74374945851672,2.03886099295457,1.41319595122714));
#46459=CARTESIAN_POINT('Ctrl Pts',(0.87187597225223,5.08919664880298,1.57158555165126));
#46460=CARTESIAN_POINT('Ctrl Pts',(-3.79452777359949,3.50164966549009,1.72997515207536));
#46461=CARTESIAN_POINT('Ctrl Pts',(-5.00293367927747,-1.2769919878773,1.88836475249948));
#46462=CARTESIAN_POINT('Ctrl Pts',(-1.65208468153467,-4.89189754332655,
2.04675435292359));
#46463=CARTESIAN_POINT('Ctrl Pts',(3.20433051897175,-4.04874042926377,2.20514395334771));
#46464=CARTESIAN_POINT('Ctrl Pts',(5.14059300557593,0.484092964878372,2.36353355377181));
#46465=CARTESIAN_POINT('Ctrl Pts',(2.392155064142,4.57576601695794,2.52192315419593));
#46466=CARTESIAN_POINT('Ctrl Pts',(-2.53628918908134,4.49747442552335,2.68031275462004));
#46467=CARTESIAN_POINT('Ctrl Pts',(-5.15337531200808,0.320567159775624,
2.83870235504415));
#46468=CARTESIAN_POINT('Ctrl Pts',(-3.07411308423917,-4.14847788693502,
2.99709195546826));
#46469=CARTESIAN_POINT('Ctrl Pts',(1.80663443860224,-4.83695274769126,3.15548155589238));
#46470=CARTESIAN_POINT('Ctrl Pts',(5.04096893490742,-1.11744005069485,3.31387115631648));
#46471=CARTESIAN_POINT('Ctrl Pts',(3.68139281034196,3.62041254264275,3.4722607567406));
#46472=CARTESIAN_POINT('Ctrl Pts',(-1.03309179131411,5.05892887272037,3.63065035716471));
#46473=CARTESIAN_POINT('Ctrl Pts',(-4.80610435287845,1.88716744466989,3.78903995758882));
#46474=CARTESIAN_POINT('Ctrl Pts',(-4.19924192609147,-3.00439798462519,
3.94742955801293));
#46475=CARTESIAN_POINT('Ctrl Pts',(0.234452652827207,-5.15801046495039,
4.10581915843705));
#46476=CARTESIAN_POINT('Ctrl Pts',(4.4544870133001,-2.61105064195526,4.26420875886115));
#46477=CARTESIAN_POINT('Ctrl Pts',(4.61508054334482,2.31539879571022,4.42259835928526));
#46478=CARTESIAN_POINT('Ctrl Pts',(0.56988195080356,5.13179058096912,4.58098795970938));
#46479=CARTESIAN_POINT('Ctrl Pts',(-3.99465861152192,3.27150463588748,4.73937756013348));
#46480=CARTESIAN_POINT('Ctrl Pts',(-4.91880686345887,-1.5701525546756,4.89776716055761));
#46481=CARTESIAN_POINT('Ctrl Pts',(-1.36037264139205,-4.98090617072295,
5.05615676098171));
#46482=CARTESIAN_POINT('Ctrl Pts',(3.43778957362211,-3.85248528258675,5.21454636140584));
#46483=CARTESIAN_POINT('Ctrl Pts',(5.10304258525828,0.786763228710822,5.37293596182993));
#46484=CARTESIAN_POINT('Ctrl Pts',(2.11781634615703,4.70902260867037,5.53132556225406));
#46485=CARTESIAN_POINT('Ctrl Pts',(-2.79740769526454,4.33987905263503,5.68971516267816));
#46486=CARTESIAN_POINT('Ctrl Pts',(-5.16331214443354,0.0157386201644824,
5.84810476310228));
#46487=CARTESIAN_POINT('Ctrl Pts',(-2.82381278957536,-4.32274465293194,
6.00649436352639));
#46488=CARTESIAN_POINT('Ctrl Pts',(2.08906951604171,-4.72184588505036,6.16488396395049));
#46489=CARTESIAN_POINT('Ctrl Pts',(5.098151436811,-0.817858137064712,6.32327356437462));
#46490=CARTESIAN_POINT('Ctrl Pts',(3.46121148378334,3.83145599864432,6.48166316479871));
#46491=CARTESIAN_POINT('Ctrl Pts',(-1.32998241066,4.98910681308353,6.64005276522284));
#46492=CARTESIAN_POINT('Ctrl Pts',(-4.90914338527368,1.60010975493711,6.79844236564693));
#46493=CARTESIAN_POINT('Ctrl Pts',(-4.01452835847177,-3.24709132363831,
6.95683196607106));
#46494=CARTESIAN_POINT('Ctrl Pts',(0.538586577094185,-5.13516937442138,
7.11522156649516));
#46495=CARTESIAN_POINT('Ctrl Pts',(4.60087948645563,-2.34349054961462,7.27361116691928));
#46496=CARTESIAN_POINT('Ctrl Pts',(4.47032190918109,2.58384636410851,7.43200076734339));
#46497=CARTESIAN_POINT('Ctrl Pts',(0.26589292373178,5.15648532996368,7.59039036776751));
#46498=CARTESIAN_POINT('Ctrl Pts',(-4.18084827136001,3.02994187021587,7.74877996819161));
#46499=CARTESIAN_POINT('Ctrl Pts',(-4.81751972636668,-1.85783306329961,
7.90716956861574));
#46500=CARTESIAN_POINT('Ctrl Pts',(-1.06391319462353,-5.05253685976928,
8.06555916903983));
#46501=CARTESIAN_POINT('Ctrl Pts',(3.65925338948522,-3.64278803069328,8.22394876946396));
#46502=CARTESIAN_POINT('Ctrl Pts',(5.04768747299395,1.08668817054443,8.38233836988805));
#46503=CARTESIAN_POINT('Ctrl Pts',(1.83608824986349,4.82584914224785,8.54072797031219));
#46504=CARTESIAN_POINT('Ctrl Pts',(-3.04876573566835,4.1671414055724,8.69911757073628));
#46505=CARTESIAN_POINT('Ctrl Pts',(-5.15523377649819,-0.289144798800594,
8.8575071711604));
#46506=CARTESIAN_POINT('Ctrl Pts',(-2.56365995117077,-4.48192901101572,
9.01589677158451));
#46507=CARTESIAN_POINT('Ctrl Pts',(2.36421564112952,-4.59026408905411,9.17428637200862));
#46508=CARTESIAN_POINT('Ctrl Pts',(5.13754605775107,-0.515422651333577,
9.33267597243274));
#46509=CARTESIAN_POINT('Ctrl Pts',(3.22895369161553,4.02913117959985,9.49106557285684));
#46510=CARTESIAN_POINT('Ctrl Pts',(-1.62223260619563,4.90187733184103,9.64945517328097));
#46511=CARTESIAN_POINT('Ctrl Pts',(-4.99505399739544,1.30746914614654,9.80784477370506));
#46512=CARTESIAN_POINT('Ctrl Pts',(-3.81580775774175,-3.47845528374006,
9.96623437412919));
#46513=CARTESIAN_POINT('Ctrl Pts',(0.840841326532404,-5.09441123866306,
10.1246239745533));
#46514=CARTESIAN_POINT('Ctrl Pts',(4.73121909778617,-2.06775381846214,10.2830135749774));
#46515=CARTESIAN_POINT('Ctrl Pts',(4.30996593957687,2.84327867165857,10.4414031754015));
#46516=CARTESIAN_POINT('Ctrl Pts',(-0.0390238264566685,5.16318866070086,
10.5997927758256));
#46517=CARTESIAN_POINT('Ctrl Pts',(-4.35245059410458,2.77780737829316,10.7581823762498));
#46518=CARTESIAN_POINT('Ctrl Pts',(-4.69942385101101,-2.13903143351615,
10.9165719766738));
#46519=CARTESIAN_POINT('Ctrl Pts',(-0.763741663751577,-5.10653881568242,
11.074961577098));
#46520=CARTESIAN_POINT('Ctrl Pts',(3.86794975738412,-3.42038077988013,11.2333511775221));
#46521=CARTESIAN_POINT('Ctrl Pts',(4.97472054752429,1.38282156443299,11.3917407779462));
#46522=CARTESIAN_POINT('Ctrl Pts',(1.54795388466898,4.92583787552529,11.5501303783703));
#46523=CARTESIAN_POINT('Ctrl Pts',(-3.28948637173101,3.97986424582764,11.7085199787944));
#46524=CARTESIAN_POINT('Ctrl Pts',(-5.12916835710966,-0.593019366839089,
11.8669095792185));
#46525=CARTESIAN_POINT('Ctrl Pts',(-2.29456228398659,-4.62547553554524,
12.0252991796426));
#46526=CARTESIAN_POINT('Ctrl Pts',(2.63111281568934,-4.44266646915302,12.1836887800668));
#46527=CARTESIAN_POINT('Ctrl Pts',(5.15901534120123,-0.211188811899807,
12.3420783804909));
#46528=CARTESIAN_POINT('Ctrl Pts',(2.98542980392062,4.2127483773522,12.500467980915));
#46529=CARTESIAN_POINT('Ctrl Pts',(-1.90882269345658,4.79754478144462,12.6588575813391));
#46530=CARTESIAN_POINT('Ctrl Pts',(-5.0635364390099,1.01026666570772,12.8172471817632));
#46531=CARTESIAN_POINT('Ctrl Pts',(-3.60377347746801,-3.6976826159257,12.9756367821873));
#46532=CARTESIAN_POINT('Ctrl Pts',(1.14016230868481,-5.03587826648703,13.1340263826114));
#46533=CARTESIAN_POINT('Ctrl Pts',(4.84505108113381,-1.78480251743019,13.2924159830355));
#46534=CARTESIAN_POINT('Ctrl Pts',(4.13457213027864,3.09279053680373,13.4508055834596));
#46535=CARTESIAN_POINT('Ctrl Pts',(-0.343804419177731,5.15187718471428,
13.6091951838838));
#46536=CARTESIAN_POINT('Ctrl Pts',(-4.50886684456297,2.51598087890574,13.7675847843078));
#46537=CARTESIAN_POINT('Ctrl Pts',(-4.56493128400683,-2.41276654015816,
13.925974384732));
#46538=CARTESIAN_POINT('Ctrl Pts',(-0.460905372910369,-5.14272362102755,
14.0843639851561));
#46539=CARTESIAN_POINT('Ctrl Pts',(4.06315051784514,-3.18603952805496,14.2427535855802));
#46540=CARTESIAN_POINT('Ctrl Pts',(4.88439639669049,1.67413017563193,14.4011431860043));
#46541=CARTESIAN_POINT('Ctrl Pts',(1.25441857601452,5.00863993928383,14.5595327864284));
#46542=CARTESIAN_POINT('Ctrl Pts',(-3.51872970857736,3.7787009993846,14.7179223868525));
#46543=CARTESIAN_POINT('Ctrl Pts',(-5.08520683073047,-0.894824839523584,
14.8763119872766));
#46544=CARTESIAN_POINT('Ctrl Pts',(-2.01745869282129,-4.75288338056742,
15.0347015877008));
#46545=CARTESIAN_POINT('Ctrl Pts',(2.88882981271105,-4.27956800578602,15.1930911881249));
#46546=CARTESIAN_POINT('Ctrl Pts',(5.16248437889336,0.0937818828261288,
15.351480788549));
#46547=CARTESIAN_POINT('Ctrl Pts',(2.73148949656154,4.38166693681219,15.5098703889731));
#46548=CARTESIAN_POINT('Ctrl Pts',(-2.18875273549729,4.67647318514471,15.6682599893972));
#46549=CARTESIAN_POINT('Ctrl Pts',(-5.11435176830703,0.709539282194621,
15.8266495898213));
#46550=CARTESIAN_POINT('Ctrl Pts',(-3.37916532475269,-3.90400842437456,
15.9850391902454));
#46551=CARTESIAN_POINT('Ctrl Pts',(1.43550516966593,-4.9597746708902,16.1434287906695));
#46552=CARTESIAN_POINT('Ctrl Pts',(4.94197826197569,-1.49562391370258,16.3018183910937));
#46553=CARTESIAN_POINT('Ctrl Pts',(3.94475245484231,3.3315114408263,16.4602079915177));
#46554=CARTESIAN_POINT('Ctrl Pts',(-0.647385467154988,5.12259027405121,
16.6185975919419));
#46555=CARTESIAN_POINT('Ctrl Pts',(-4.64955123813058,2.24537608806315,16.776987192366));
#46556=CARTESIAN_POINT('Ctrl Pts',(-4.41451134820182,-2.67808364399215,
16.9353767927901));
#46557=CARTESIAN_POINT('Ctrl Pts',(-0.156460816144074,-5.16096436253732,
17.0937663932142));
#46558=CARTESIAN_POINT('Ctrl Pts',(4.24417435465306,-2.94058317628852,17.2521559936383));
#46559=CARTESIAN_POINT('Ctrl Pts',(4.7770306357801,1.95960002071087,17.4105455940624));
#46560=CARTESIAN_POINT('Ctrl Pts',(0.956505601666415,5.07396180892462,17.5689351944865));
#46561=CARTESIAN_POINT('Ctrl Pts',(-3.73569419127765,3.5643623764192,17.7273247949107));
#46562=CARTESIAN_POINT('Ctrl Pts',(-5.02350584303606,-1.19352508090609,
17.8857143953348));
#46563=CARTESIAN_POINT('Ctrl Pts',(-1.7333097832156,-4.86367572142824,18.0441039957589));
#46564=CARTESIAN_POINT('Ctrl Pts',(3.13645552043595,-4.10159948955856,18.202493596183));
#46565=CARTESIAN_POINT('Ctrl Pts',(5.14796384574126,0.398543369117654,18.3608831966071));
#46566=CARTESIAN_POINT('Ctrl Pts',(2.46797524199195,4.53507188733415,18.5192727970312));
#46567=CARTESIAN_POINT('Ctrl Pts',(-2.46096278237594,4.53951629179981,18.6776623974553));
#46568=CARTESIAN_POINT('Ctrl Pts',(-5.14748183280556,0.405511410062441,
18.8360519978794));
#46569=CARTESIAN_POINT('Ctrl Pts',(-3.14246278706502,-4.0951334678725,18.9944415983036));
#46570=CARTESIAN_POINT('Ctrl Pts',(1.72525842040716,-4.86940713488401,19.1528311987277));
#46571=CARTESIAN_POINT('Ctrl Pts',(5.02276837180745,-1.19521866677756,19.3112207991518));
#46572=CARTESIAN_POINT('Ctrl Pts',(3.95306672650205,2.75529758855723,19.4432121328385));
#46573=CARTESIAN_POINT('Ctrl Pts',(1.3947178009747,4.32991044428859,19.548805199788));
#46574=CARTESIAN_POINT('Ctrl Pts',(-0.0904913830656236,4.43080762341373,
19.6016017332627));
#46575=CARTESIAN_POINT('Ctrl Pts',(-0.803308159453631,4.29756675351939,
19.628));
#46576=CARTESIAN_POINT('Ctrl Pts',(-2.00237954638878,4.09906332620074,-0.219393102292058));
#46577=CARTESIAN_POINT('Ctrl Pts',(-2.6822715117666,3.76693823886074,-0.192994835554706));
#46578=CARTESIAN_POINT('Ctrl Pts',(-3.86326433094171,2.75793992993429,-0.140198302080001));
#46579=CARTESIAN_POINT('Ctrl Pts',(-5.02561840602911,-0.153231111990883,
-0.0346052351305939));
#46580=CARTESIAN_POINT('Ctrl Pts',(-3.46236114308042,-4.12747715912022,
0.0973860985561662));
#46581=CARTESIAN_POINT('Ctrl Pts',(1.58624073518831,-5.15184324632905,0.255775698980278));
#46582=CARTESIAN_POINT('Ctrl Pts',(5.18078309827857,-1.47340186480046,0.414165299404389));
#46583=CARTESIAN_POINT('Ctrl Pts',(4.0583740122066,3.54376211431939,0.572554899828502));
#46584=CARTESIAN_POINT('Ctrl Pts',(-0.764772284002811,5.33352936417491,
0.730944500252612));
#46585=CARTESIAN_POINT('Ctrl Pts',(-4.88977832440859,2.26168095600148,0.889334100676726));
#46586=CARTESIAN_POINT('Ctrl Pts',(-4.55927934554221,-2.87070102899737,
1.04772370110084));
#46587=CARTESIAN_POINT('Ctrl Pts',(-0.0735146804517841,-5.38726835420972,
1.20611330152495));
#46588=CARTESIAN_POINT('Ctrl Pts',(4.47907447545189,-2.9941812164533,1.36450290194906));
#46589=CARTESIAN_POINT('Ctrl Pts',(4.94990508457304,2.12746657133089,1.52289250237317));
#46590=CARTESIAN_POINT('Ctrl Pts',(0.909766282116828,5.31036484717274,1.68128210279728));
#46591=CARTESIAN_POINT('Ctrl Pts',(-3.95943177107978,3.65382565735724,1.8396717032214));
#46592=CARTESIAN_POINT('Ctrl Pts',(-5.2203530294748,-1.33248798003114,1.99806130364551));
#46593=CARTESIAN_POINT('Ctrl Pts',(-1.72388159129946,-5.10449144388282,
2.15645090406962));
#46594=CARTESIAN_POINT('Ctrl Pts',(3.34358550492888,-4.22469209476243,2.31484050449373));
#46595=CARTESIAN_POINT('Ctrl Pts',(5.36399480590974,0.505130856764646,2.47323010491784));
#46596=CARTESIAN_POINT('Ctrl Pts',(2.49611422749678,4.77462135621273,2.63161970534196));
#46597=CARTESIAN_POINT('Ctrl Pts',(-2.64651218677699,4.69292733971583,2.79000930576607));
#46598=CARTESIAN_POINT('Ctrl Pts',(-5.37733261056287,0.334498486481351,
2.94839890619018));
#46599=CARTESIAN_POINT('Ctrl Pts',(-3.20770903254784,-4.32876397991708,
3.10678850661429));
#46600=CARTESIAN_POINT('Ctrl Pts',(1.88514782911787,-5.04715883690933,3.2651781070384));
#46601=CARTESIAN_POINT('Ctrl Pts',(5.26004123537227,-1.16600217549634,3.42356770746252));
#46602=CARTESIAN_POINT('Ctrl Pts',(3.84138014656453,3.77774977574021,3.58195730788662));
#46603=CARTESIAN_POINT('Ctrl Pts',(-1.07798827812784,5.27878168283402,3.74034690831074));
#46604=CARTESIAN_POINT('Ctrl Pts',(-5.01496982109594,1.96918066847761,3.89873650873484));
#46605=CARTESIAN_POINT('Ctrl Pts',(-4.38173414154377,-3.1349642282388,4.05712610915897));
#46606=CARTESIAN_POINT('Ctrl Pts',(0.244641583302294,-5.38216919970349,
4.21551570958307));
#46607=CARTESIAN_POINT('Ctrl Pts',(4.64807176456428,-2.72452265064043,4.37390531000719));
#46608=CARTESIAN_POINT('Ctrl Pts',(4.81564442789093,2.41602225663996,4.53229491043129));
#46609=CARTESIAN_POINT('Ctrl Pts',(0.594648092306935,5.35480984226466,4.69068451085541));
#46610=CARTESIAN_POINT('Ctrl Pts',(-4.16825996929618,3.41367889956971,4.84907411127951));
#46611=CARTESIAN_POINT('Ctrl Pts',(-5.13257019924506,-1.63838882763724,
5.00746371170364));
#46612=CARTESIAN_POINT('Ctrl Pts',(-1.41949222095851,-5.19736824127129,
5.16585331212774));
#46613=CARTESIAN_POINT('Ctrl Pts',(3.58719030989569,-4.01990801902123,5.32424291255186));
#46614=CARTESIAN_POINT('Ctrl Pts',(5.32481250547765,0.820954677351021,5.48263251297596));
#46615=CARTESIAN_POINT('Ctrl Pts',(2.2098531956012,4.91366906238659,5.64102211340008));
#46616=CARTESIAN_POINT('Ctrl Pts',(-2.9189784779956,4.52848312857297,5.79941171382418));
#46617=CARTESIAN_POINT('Ctrl Pts',(-5.38770128154296,0.0164225949658002,
5.9578013142483));
#46618=CARTESIAN_POINT('Ctrl Pts',(-2.9465310947033,-4.51060409576292,6.11619091467242));
#46619=CARTESIAN_POINT('Ctrl Pts',(2.17985707506455,-4.92704961747478,6.27458051509652));
#46620=CARTESIAN_POINT('Ctrl Pts',(5.3197087956843,-0.853400919782555,6.43297011552065));
#46621=CARTESIAN_POINT('Ctrl Pts',(3.61163009812893,3.99796483664578,6.59135971594474));
#46622=CARTESIAN_POINT('Ctrl Pts',(-1.38778128029068,5.20592527019374,6.74974931636887));
#46623=CARTESIAN_POINT('Ctrl Pts',(-5.12248676203533,1.6696479190355,6.90813891679296));
#46624=CARTESIAN_POINT('Ctrl Pts',(-4.18899322308973,-3.38820462452834,
7.0665285172171));
#46625=CARTESIAN_POINT('Ctrl Pts',(0.561992672622043,-5.35833547257784,
7.22491811764118));
#46626=CARTESIAN_POINT('Ctrl Pts',(4.80082621619637,-2.44533483242041,7.38330771806533));
#46627=CARTESIAN_POINT('Ctrl Pts',(4.66459481923242,2.69613611918183,7.5416973184894));
#46628=CARTESIAN_POINT('Ctrl Pts',(0.27744819717852,5.38057778483401,7.70008691891355));
#46629=CARTESIAN_POINT('Ctrl Pts',(-4.36254112853255,3.16161820949792,7.85847651933763));
#46630=CARTESIAN_POINT('Ctrl Pts',(-5.02688128812553,-1.93857146266532,
8.01686611976177));
#46631=CARTESIAN_POINT('Ctrl Pts',(-1.11014912943107,-5.27211188340975,
8.17525572018585));
#46632=CARTESIAN_POINT('Ctrl Pts',(3.81827858253237,-3.80109766606194,8.33364532061));
#46633=CARTESIAN_POINT('Ctrl Pts',(5.26705175018262,1.13391386871537,8.49203492103408));
#46634=CARTESIAN_POINT('Ctrl Pts',(1.91588165504971,5.03557268685605,8.65042452145821));
#46635=CARTESIAN_POINT('Ctrl Pts',(-3.18126012948741,4.34823858468009,8.80881412188231));
#46636=CARTESIAN_POINT('Ctrl Pts',(-5.37927184089313,-0.301710560871043,
8.96720372230643));
#46637=CARTESIAN_POINT('Ctrl Pts',(-2.67507243761234,-4.67670634681008,
9.12559332273054));
#46638=CARTESIAN_POINT('Ctrl Pts',(2.46696060266074,-4.78974949091146,9.28398292315464));
#46639=CARTESIAN_POINT('Ctrl Pts',(5.36081544269451,-0.537822080371423,
9.44237252357877));
#46640=CARTESIAN_POINT('Ctrl Pts',(3.36927876055584,4.20423065904265,9.60076212400287));
#46641=CARTESIAN_POINT('Ctrl Pts',(-1.69273219338161,5.11490493775362,9.75915172442699));
#46642=CARTESIAN_POINT('Ctrl Pts',(-5.21213090945059,1.36428962596537,9.91754132485109));
#46643=CARTESIAN_POINT('Ctrl Pts',(-3.98163654867748,-3.62962328554942,
10.0759309252752));
#46644=CARTESIAN_POINT('Ctrl Pts',(0.877382921235304,-5.31580605461594,
10.2343205256993));
#46645=CARTESIAN_POINT('Ctrl Pts',(4.93683017477137,-2.15761503198178,10.3927101261234));
#46646=CARTESIAN_POINT('Ctrl Pts',(4.49727004033617,2.96684293232075,10.5510997265475));
#46647=CARTESIAN_POINT('Ctrl Pts',(-0.0407197384023858,5.38757243140836,
10.7094893269717));
#46648=CARTESIAN_POINT('Ctrl Pts',(-4.54160100876145,2.89852636316868,10.8678789273958));
#46649=CARTESIAN_POINT('Ctrl Pts',(-4.90365315835139,-2.23199025610718,
11.0262685278199));
#46650=CARTESIAN_POINT('Ctrl Pts',(-0.796932632670351,-5.32846067638225,
11.184658128244));
#46651=CARTESIAN_POINT('Ctrl Pts',(4.03604455470867,-3.56902495832874,11.3430477286681));
#46652=CARTESIAN_POINT('Ctrl Pts',(5.19091380096199,1.44291673763568,11.5014373290922));
#46653=CARTESIAN_POINT('Ctrl Pts',(1.6152254395837,5.13990676764554,11.6598269295163));
#46654=CARTESIAN_POINT('Ctrl Pts',(-3.43244209236889,4.15282266456216,11.8182165299404));
#46655=CARTESIAN_POINT('Ctrl Pts',(-5.3520736608267,-0.618791022762998,
11.9766061303646));
#46656=CARTESIAN_POINT('Ctrl Pts',(-2.39428022405006,-4.82649116952364,
12.1349957307887));
#46657=CARTESIAN_POINT('Ctrl Pts',(2.7454566937728,-4.63573751881888,12.2933853312128));
#46658=CARTESIAN_POINT('Ctrl Pts',(5.38321774623971,-0.22036673373445,12.4517749316369));
#46659=CARTESIAN_POINT('Ctrl Pts',(3.11517172129139,4.39582756118039,12.610164532061));
#46660=CARTESIAN_POINT('Ctrl Pts',(-1.99177701910997,5.00603826462726,12.7685541324851));
#46661=CARTESIAN_POINT('Ctrl Pts',(-5.28358948645086,1.05417120973438,12.9269437329092));
#46662=CARTESIAN_POINT('Ctrl Pts',(-3.76038760389046,-3.85837788057022,
13.0853333333334));
#46663=CARTESIAN_POINT('Ctrl Pts',(1.18971190581428,-5.25472933479274,13.2437229337574));
#46664=CARTESIAN_POINT('Ctrl Pts',(5.05560911073477,-1.862367128206,13.4021125341816));
#46665=CARTESIAN_POINT('Ctrl Pts',(4.3142539017226,3.22719817678374,13.5605021346057));
#46666=CARTESIAN_POINT('Ctrl Pts',(-0.358745599334103,5.37576937709664,
13.7188917350298));
#46667=CARTESIAN_POINT('Ctrl Pts',(-4.70481485473382,2.6253213105142,13.8772813354539));
#46668=CARTESIAN_POINT('Ctrl Pts',(-4.76331576341244,-2.51762144469383,
14.035670935878));
#46669=CARTESIAN_POINT('Ctrl Pts',(-0.480935569811807,-5.36621801443908,
14.1940605363021));
#46670=CARTESIAN_POINT('Ctrl Pts',(4.23972842232605,-3.32449961733459,14.3524501367262));
#46671=CARTESIAN_POINT('Ctrl Pts',(5.09666430962992,1.74688514666806,14.5108397371504));
#46672=CARTESIAN_POINT('Ctrl Pts',(1.30893356445067,5.22630727424813,14.6692293375744));
#46673=CARTESIAN_POINT('Ctrl Pts',(-3.67164797130143,3.94291719103216,14.8276189379986));
#46674=CARTESIAN_POINT('Ctrl Pts',(-5.30620163810439,-0.933712469786478,
14.9860085384227));
#46675=CARTESIAN_POINT('Ctrl Pts',(-2.10513416208848,-4.95943595200104,
15.1443981388468));
#46676=CARTESIAN_POINT('Ctrl Pts',(3.01437365178127,-4.46555106184718,15.3027877392709));
#46677=CARTESIAN_POINT('Ctrl Pts',(5.38683754266046,0.0978574907256861,
15.461177339695));
#46678=CARTESIAN_POINT('Ctrl Pts',(2.85019558172777,4.57208704614299,15.6195669401191));
#46679=CARTESIAN_POINT('Ctrl Pts',(-2.28387236489903,4.87970509392274,15.7779565405432));
#46680=CARTESIAN_POINT('Ctrl Pts',(-5.33661316720418,0.740374703881965,
15.9363461409674));
#46681=CARTESIAN_POINT('Ctrl Pts',(-3.5260183466427,-4.07367027264334,16.0947357413914));
#46682=CARTESIAN_POINT('Ctrl Pts',(1.49788988655441,-5.17531840086943,16.2531253418156));
#46683=CARTESIAN_POINT('Ctrl Pts',(5.15674858900573,-1.56062129330084,16.4115149422397));
#46684=CARTESIAN_POINT('Ctrl Pts',(4.11618497232175,3.47629350252734,16.5699045426638));
#46685=CARTESIAN_POINT('Ctrl Pts',(-0.675519785260975,5.34520970499122,
16.7282941430879));
#46686=CARTESIAN_POINT('Ctrl Pts',(-4.85161316293496,2.34295647615374,16.886683743512));
#46687=CARTESIAN_POINT('Ctrl Pts',(-4.60635882216303,-2.79446879777952,
17.0450733439361));
#46688=CARTESIAN_POINT('Ctrl Pts',(-0.16326034841019,-5.385251468869,17.2034629443603));
#46689=CARTESIAN_POINT('Ctrl Pts',(4.42861926027611,-3.06837613225715,17.3618525447843));
#46690=CARTESIAN_POINT('Ctrl Pts',(4.98463260760038,2.04476104631356,17.5202421452085));
#46691=CARTESIAN_POINT('Ctrl Pts',(0.998073777402168,5.29446792596388,17.6786317456326));
#46692=CARTESIAN_POINT('Ctrl Pts',(-3.89804137708339,3.71926376057284,17.8370213460567));
#46693=CARTESIAN_POINT('Ctrl Pts',(-5.24181922596764,-1.24539373721259,
17.9954109464808));
#46694=CARTESIAN_POINT('Ctrl Pts',(-1.8086366036207,-5.07504314756533,18.1538005469049));
#46695=CARTESIAN_POINT('Ctrl Pts',(3.27276076949422,-4.27984832373426,18.312190147329));
#46696=CARTESIAN_POINT('Ctrl Pts',(5.37168597078491,0.415863414893554,18.4705797477531));
#46697=CARTESIAN_POINT('Ctrl Pts',(2.57522942679949,4.73215872598774,18.6289693481773));
#46698=CARTESIAN_POINT('Ctrl Pts',(-2.56791221710864,4.73679627703356,18.7873589486013));
#46699=CARTESIAN_POINT('Ctrl Pts',(-5.371183010352,0.423134275550087,18.9457485490255));
#46700=CARTESIAN_POINT('Ctrl Pts',(-3.27902910214792,-4.27310129927592,
19.1041381494496));
#46701=CARTESIAN_POINT('Ctrl Pts',(1.80023534169657,-5.08102363891602,19.2625277498737));
#46702=CARTESIAN_POINT('Ctrl Pts',(5.24104970544042,-1.24716092356801,19.4209173502978));
#46703=CARTESIAN_POINT('Ctrl Pts',(4.12486056868766,2.87503833462901,19.5529086839846));
#46704=CARTESIAN_POINT('Ctrl Pts',(1.45532996524397,4.51808130074211,19.658501750934));
#46705=CARTESIAN_POINT('Ctrl Pts',(-0.0944239912043199,4.62336330695642,
19.7112982844087));
#46706=CARTESIAN_POINT('Ctrl Pts',(-0.838218623839749,4.48433200584526,
19.737696551146));
#46707=CARTESIAN_POINT('Ctrl Pts',(-2.08577545033744,4.26978275451687,-0.109696551146029));
#46708=CARTESIAN_POINT('Ctrl Pts',(-2.79398382812688,3.92382518874754,-0.0832982844086765));
#46709=CARTESIAN_POINT('Ctrl Pts',(-4.02416310842503,2.87280371482855,-0.0305017509339729));
#46710=CARTESIAN_POINT('Ctrl Pts',(-5.23492737076948,-0.159612942608633,
0.0750913160154349));
#46711=CARTESIAN_POINT('Ctrl Pts',(-3.60656294430474,-4.29937997811031,
0.207082649702195));
#46712=CARTESIAN_POINT('Ctrl Pts',(1.65230512354554,-5.36640927368603,0.365472250126306));
#46713=CARTESIAN_POINT('Ctrl Pts',(5.39655442416041,-1.53476669476806,0.523861850550419));
#46714=CARTESIAN_POINT('Ctrl Pts',(4.22739879570491,3.69135413573996,0.68225145097453));
#46715=CARTESIAN_POINT('Ctrl Pts',(-0.796623825861737,5.55566232761052,
0.840641051398642));
#46716=CARTESIAN_POINT('Ctrl Pts',(-5.09342976711741,2.35587634873282,0.999030651822753));
#46717=CARTESIAN_POINT('Ctrl Pts',(-4.74916603463757,-2.99026113323004,
1.15742025224687));
#46718=CARTESIAN_POINT('Ctrl Pts',(-0.0765764492562429,-5.61163946058846,
1.31580985267098));
#46719=CARTESIAN_POINT('Ctrl Pts',(4.66562076004983,-3.11888407290359,1.47419945309509));
#46720=CARTESIAN_POINT('Ctrl Pts',(5.15606071062936,2.21607214970721,1.6325890535192));
#46721=CARTESIAN_POINT('Ctrl Pts',(0.947656591981422,5.53153304554248,1.79097865394331));
#46722=CARTESIAN_POINT('Ctrl Pts',(-4.12433576856007,3.80600164922439,1.94936825436742));
#46723=CARTESIAN_POINT('Ctrl Pts',(-5.43777237967215,-1.38798397218498,
2.10775785479154));
#46724=CARTESIAN_POINT('Ctrl Pts',(-1.79567850106425,-5.31708534443909,
2.26614745521565));
#46725=CARTESIAN_POINT('Ctrl Pts',(3.482840490886,-4.4006437602611,2.42453705563976));
#46726=CARTESIAN_POINT('Ctrl Pts',(5.58739660624356,0.526168748650917,2.58292665606387));
#46727=CARTESIAN_POINT('Ctrl Pts',(2.60007339085155,4.97347669546753,2.74131625648798));
#46728=CARTESIAN_POINT('Ctrl Pts',(-2.75673518447264,4.88838025390829,2.8997058569121));
#46729=CARTESIAN_POINT('Ctrl Pts',(-5.60128990911765,0.348429813187091,
3.05809545733621));
#46730=CARTESIAN_POINT('Ctrl Pts',(-3.34130498085651,-4.50905007289915,
3.21648505776032));
#46731=CARTESIAN_POINT('Ctrl Pts',(1.9636612196335,-5.25736492612739,3.37487465818443));
#46732=CARTESIAN_POINT('Ctrl Pts',(5.47911353583714,-1.21456430029784,3.53326425860854));
#46733=CARTESIAN_POINT('Ctrl Pts',(4.00136748278709,3.93508700883766,3.69165385903265));
#46734=CARTESIAN_POINT('Ctrl Pts',(-1.12288476494156,5.49863449294768,3.85004345945677));
#46735=CARTESIAN_POINT('Ctrl Pts',(-5.22383528931343,2.05119389228533,4.00843305988088));
#46736=CARTESIAN_POINT('Ctrl Pts',(-4.56422635699607,-3.26553047185241,
4.16682266030499));
#46737=CARTESIAN_POINT('Ctrl Pts',(0.254830513777376,-5.6063279344566,4.3252122607291));
#46738=CARTESIAN_POINT('Ctrl Pts',(4.84165651582845,-2.8379946593256,4.48360186115322));
#46739=CARTESIAN_POINT('Ctrl Pts',(5.01620831243703,2.51664571756971,4.64199146157732));
#46740=CARTESIAN_POINT('Ctrl Pts',(0.619414233810315,5.57782910356021,4.80038106200144));
#46741=CARTESIAN_POINT('Ctrl Pts',(-4.34186132707045,3.55585316325194,4.95877066242554));
#46742=CARTESIAN_POINT('Ctrl Pts',(-5.34633353503125,-1.70662510059887,
5.11716026284966));
#46743=CARTESIAN_POINT('Ctrl Pts',(-1.47861180052498,-5.41383031181963,
5.27554986327377));
#46744=CARTESIAN_POINT('Ctrl Pts',(3.73659104616929,-4.18733075545571,5.43393946369789));
#46745=CARTESIAN_POINT('Ctrl Pts',(5.54658242569702,0.855146125991221,5.59232906412199));
#46746=CARTESIAN_POINT('Ctrl Pts',(2.30189004504538,5.11831551610282,5.75071866454611));
#46747=CARTESIAN_POINT('Ctrl Pts',(-3.04054926072666,4.71708720451092,5.90910826497022));
#46748=CARTESIAN_POINT('Ctrl Pts',(-5.61209041865238,0.0171065697671163,
6.06749786539433));
#46749=CARTESIAN_POINT('Ctrl Pts',(-3.06924939983126,-4.69846353859389,
6.22588746581845));
#46750=CARTESIAN_POINT('Ctrl Pts',(2.27064463408739,-5.13225334989921,6.38427706624255));
#46751=CARTESIAN_POINT('Ctrl Pts',(5.5412661545576,-0.888943702500394,6.54266666666667));
#46752=CARTESIAN_POINT('Ctrl Pts',(3.76204871247451,4.16447367464723,6.70105626709077));
#46753=CARTESIAN_POINT('Ctrl Pts',(-1.44558014992134,5.42274372730397,6.85944586751489));
#46754=CARTESIAN_POINT('Ctrl Pts',(-5.33583013879699,1.73918608313389,7.017835467939));
#46755=CARTESIAN_POINT('Ctrl Pts',(-4.36345808770768,-3.52931792541838,
7.17622506836312));
#46756=CARTESIAN_POINT('Ctrl Pts',(0.585398768149902,-5.58150157073431,
7.33461466878722));
#46757=CARTESIAN_POINT('Ctrl Pts',(5.00077294593711,-2.54717911522619,7.49300426921134));
#46758=CARTESIAN_POINT('Ctrl Pts',(4.85886772928377,2.80842587425515,7.65139386963545));
#46759=CARTESIAN_POINT('Ctrl Pts',(0.289003470625252,5.60467023970434,7.80978347005956));
#46760=CARTESIAN_POINT('Ctrl Pts',(-4.54423398570509,3.29329454877997,7.96817307048368));
#46761=CARTESIAN_POINT('Ctrl Pts',(-5.23624284988438,-2.01930986203101,
8.12656267090778));
#46762=CARTESIAN_POINT('Ctrl Pts',(-1.15638506423861,-5.49168690705022,
8.2849522713319));
#46763=CARTESIAN_POINT('Ctrl Pts',(3.97730377557951,-3.9594073014306,8.44334187175601));
#46764=CARTESIAN_POINT('Ctrl Pts',(5.48641602737129,1.1811395668863,8.60173147218012));
#46765=CARTESIAN_POINT('Ctrl Pts',(1.99567506023593,5.24529623146426,8.76012107260423));
#46766=CARTESIAN_POINT('Ctrl Pts',(-3.31375452330647,4.52933576378778,8.91851067302835));
#46767=CARTESIAN_POINT('Ctrl Pts',(-5.60330990528806,-0.314276322941499,
9.07690027345245));
#46768=CARTESIAN_POINT('Ctrl Pts',(-2.78648492405391,-4.87148368260443,
9.23528987387657));
#46769=CARTESIAN_POINT('Ctrl Pts',(2.56970556419197,-4.98923489276881,9.39367947430067));
#46770=CARTESIAN_POINT('Ctrl Pts',(5.58408482763794,-0.560221509409272,
9.5520690747248));
#46771=CARTESIAN_POINT('Ctrl Pts',(3.50960382949614,4.37933013848544,9.7104586751489));
#46772=CARTESIAN_POINT('Ctrl Pts',(-1.76323178056758,5.32793254366621,9.86884827557301));
#46773=CARTESIAN_POINT('Ctrl Pts',(-5.42920782150573,1.4211101057842,10.0272378759971));
#46774=CARTESIAN_POINT('Ctrl Pts',(-4.14746533961321,-3.78079128735878,
10.1856274764213));
#46775=CARTESIAN_POINT('Ctrl Pts',(0.913924515938199,-5.53720087056882,
10.3440170768453));
#46776=CARTESIAN_POINT('Ctrl Pts',(5.14244125175658,-2.24747624550143,10.5024066772695));
#46777=CARTESIAN_POINT('Ctrl Pts',(4.68457414109547,3.09040719298293,10.6607962776936));
#46778=CARTESIAN_POINT('Ctrl Pts',(-0.0424156503481004,5.61195620211585,
10.8191858781177));
#46779=CARTESIAN_POINT('Ctrl Pts',(-4.73075142341831,3.01924534804421,10.9775754785418));
#46780=CARTESIAN_POINT('Ctrl Pts',(-5.10788246569177,-2.32494907869821,
11.1359650789659));
#46781=CARTESIAN_POINT('Ctrl Pts',(-0.83012360158913,-5.55038253708208,
11.29435467939));
#46782=CARTESIAN_POINT('Ctrl Pts',(4.20413935203321,-3.71766913677734,11.4527442798141));
#46783=CARTESIAN_POINT('Ctrl Pts',(5.4071070543997,1.50301191083837,11.6111338802383));
#46784=CARTESIAN_POINT('Ctrl Pts',(1.68249699449844,5.35397565976581,11.7695234806624));
#46785=CARTESIAN_POINT('Ctrl Pts',(-3.57539781300678,4.32578108329668,11.9279130810865));
#46786=CARTESIAN_POINT('Ctrl Pts',(-5.57497896454372,-0.644562678686908,
12.0863026815106));
#46787=CARTESIAN_POINT('Ctrl Pts',(-2.49399816411355,-5.02750680350203,
12.2446922819347));
#46788=CARTESIAN_POINT('Ctrl Pts',(2.85980057185626,-4.82880856848474,12.4030818823588));
#46789=CARTESIAN_POINT('Ctrl Pts',(5.60742015127818,-0.229544655569092,
12.5614714827829));
#46790=CARTESIAN_POINT('Ctrl Pts',(3.24491363866216,4.57890674500859,12.719861083207));
#46791=CARTESIAN_POINT('Ctrl Pts',(-2.07473134476337,5.2145317478099,12.8782506836311));
#46792=CARTESIAN_POINT('Ctrl Pts',(-5.50364253389182,1.09807575376104,13.0366402840552));
#46793=CARTESIAN_POINT('Ctrl Pts',(-3.91700173031292,-4.01907314521474,
13.1950298844794));
#46794=CARTESIAN_POINT('Ctrl Pts',(1.23926150294374,-5.47358040309844,13.3534194849035));
#46795=CARTESIAN_POINT('Ctrl Pts',(5.26616714033573,-1.93993173898181,13.5118090853276));
#46796=CARTESIAN_POINT('Ctrl Pts',(4.49393567316656,3.36160581676376,13.6701986857517));
#46797=CARTESIAN_POINT('Ctrl Pts',(-0.37368677949048,5.59966156947901,13.8285882861758));
#46798=CARTESIAN_POINT('Ctrl Pts',(-4.90076286490465,2.73466174212266,13.9869778865999));
#46799=CARTESIAN_POINT('Ctrl Pts',(-4.96170024281806,-2.6224763492295,14.1453674870241));
#46800=CARTESIAN_POINT('Ctrl Pts',(-0.500965766713239,-5.58971240785062,
14.3037570874481));
#46801=CARTESIAN_POINT('Ctrl Pts',(4.41630632680696,-3.46295970661421,14.4621466878723));
#46802=CARTESIAN_POINT('Ctrl Pts',(5.30893222256936,1.81964011770419,14.6205362882964));
#46803=CARTESIAN_POINT('Ctrl Pts',(1.36344855288682,5.44397460921243,14.7789258887205));
#46804=CARTESIAN_POINT('Ctrl Pts',(-3.8245662340255,4.10713338267972,14.9373154891446));
#46805=CARTESIAN_POINT('Ctrl Pts',(-5.52719644547832,-0.972600100049373,
15.0957050895687));
#46806=CARTESIAN_POINT('Ctrl Pts',(-2.19280963135567,-5.16598852343466,
15.2540946899928));
#46807=CARTESIAN_POINT('Ctrl Pts',(3.1399174908515,-4.65153411790834,15.4124842904169));
#46808=CARTESIAN_POINT('Ctrl Pts',(5.61119070642755,0.101933098625243,15.570873890841));
#46809=CARTESIAN_POINT('Ctrl Pts',(2.96890166689401,4.76250715547379,15.7292634912652));
#46810=CARTESIAN_POINT('Ctrl Pts',(-2.37899199430077,5.08293700270077,15.8876530916893));
#46811=CARTESIAN_POINT('Ctrl Pts',(-5.55887456610132,0.77121012556931,16.0460426921134));
#46812=CARTESIAN_POINT('Ctrl Pts',(-3.6728713685327,-4.24333212091212,16.2044322925375));
#46813=CARTESIAN_POINT('Ctrl Pts',(1.56027460344289,-5.39086213084865,16.3628218929616));
#46814=CARTESIAN_POINT('Ctrl Pts',(5.37151891603578,-1.6256186728991,16.5212114933857));
#46815=CARTESIAN_POINT('Ctrl Pts',(4.28761748980119,3.62107556422837,16.6796010938098));
#46816=CARTESIAN_POINT('Ctrl Pts',(-0.703654103366955,5.56782913593124,
16.837990694234));
#46817=CARTESIAN_POINT('Ctrl Pts',(-5.05367508773934,2.44053686424434,16.996380294658));
#46818=CARTESIAN_POINT('Ctrl Pts',(-4.79820629612424,-2.91085395156691,
17.1547698950822));
#46819=CARTESIAN_POINT('Ctrl Pts',(-0.170059880676311,-5.60953857520067,
17.3131594955063));
#46820=CARTESIAN_POINT('Ctrl Pts',(4.61306416589918,-3.1961690882258,17.4715490959304));
#46821=CARTESIAN_POINT('Ctrl Pts',(5.19223457942065,2.12992207191625,17.6299386963545));
#46822=CARTESIAN_POINT('Ctrl Pts',(1.03964195313792,5.51497404300314,17.7883282967786));
#46823=CARTESIAN_POINT('Ctrl Pts',(-4.06038856288912,3.87416514472648,17.9467178972027));
#46824=CARTESIAN_POINT('Ctrl Pts',(-5.46013260889923,-1.2972623935191,18.1051074976268));
#46825=CARTESIAN_POINT('Ctrl Pts',(-1.88396342402579,-5.28641057370242,
18.263497098051));
#46826=CARTESIAN_POINT('Ctrl Pts',(3.40906601855249,-4.45809715790996,18.421886698475));
#46827=CARTESIAN_POINT('Ctrl Pts',(5.59540809582856,0.433183460669457,18.5802762988992));
#46828=CARTESIAN_POINT('Ctrl Pts',(2.68248361160703,4.92924556464132,18.7386658993233));
#46829=CARTESIAN_POINT('Ctrl Pts',(-2.67486165184133,4.93407626226733,18.8970554997474));
#46830=CARTESIAN_POINT('Ctrl Pts',(-5.59488418789844,0.440757141037727,
19.0554451001715));
#46831=CARTESIAN_POINT('Ctrl Pts',(-3.41559541723082,-4.45106913067933,
19.2138347005956));
#46832=CARTESIAN_POINT('Ctrl Pts',(1.87521226298597,-5.29264014294805,19.3722243010197));
#46833=CARTESIAN_POINT('Ctrl Pts',(5.4593310390734,-1.29910318035845,19.5306139014438));
#46834=CARTESIAN_POINT('Ctrl Pts',(4.29665441087326,2.99477908070078,19.6626052351306));
#46835=CARTESIAN_POINT('Ctrl Pts',(1.51594212951325,4.70625215719564,19.76819830208));
#46836=CARTESIAN_POINT('Ctrl Pts',(-0.098356599343019,4.8159189904991,19.8209948355547));
#46837=CARTESIAN_POINT('Ctrl Pts',(-0.873129088225867,4.67109725817113,
19.8473931022921));
#46838=CARTESIAN_POINT('Ctrl Pts',(-2.1691713542861,4.440502182833,2.77555756156289E-16));
#46839=CARTESIAN_POINT('Ctrl Pts',(-2.90569614448715,4.08071213863434,0.0263982667373523));
#46840=CARTESIAN_POINT('Ctrl Pts',(-4.18506188590834,2.9876674997228,0.079194800212056));
#46841=CARTESIAN_POINT('Ctrl Pts',(-5.44423633550983,-0.165994773226382,
0.184787867161464));
#46842=CARTESIAN_POINT('Ctrl Pts',(-3.75076474552906,-4.4712827971004,0.316779200848224));
#46843=CARTESIAN_POINT('Ctrl Pts',(1.71836951190277,-5.58097530104301,0.475168801272335));
#46844=CARTESIAN_POINT('Ctrl Pts',(5.61232575004223,-1.59613152473566,0.633558401696447));
#46845=CARTESIAN_POINT('Ctrl Pts',(4.39642357920323,3.83894615716052,0.79194800212056));
#46846=CARTESIAN_POINT('Ctrl Pts',(-0.828475367720669,5.77779529104613,
0.95033760254467));
#46847=CARTESIAN_POINT('Ctrl Pts',(-5.29708120982622,2.45007174146416,1.10872720296878));
#46848=CARTESIAN_POINT('Ctrl Pts',(-4.93905272373294,-3.10982123746271,
1.26711680339289));
#46849=CARTESIAN_POINT('Ctrl Pts',(-0.0796382180607007,-5.83601056696721,
1.42550640381701));
#46850=CARTESIAN_POINT('Ctrl Pts',(4.85216704464777,-3.24358692935388,1.58389600424112));
#46851=CARTESIAN_POINT('Ctrl Pts',(5.36221633668567,2.30467772808354,1.74228560466523));
#46852=CARTESIAN_POINT('Ctrl Pts',(0.985546901846022,5.75270124391223,1.90067520508934));
#46853=CARTESIAN_POINT('Ctrl Pts',(-4.28923976604036,3.95817764109155,2.05906480551345));
#46854=CARTESIAN_POINT('Ctrl Pts',(-5.65519172986948,-1.44347996433883,
2.21745440593756));
#46855=CARTESIAN_POINT('Ctrl Pts',(-1.86747541082905,-5.52967924499536,
2.37584400636168));
#46856=CARTESIAN_POINT('Ctrl Pts',(3.62209547684312,-4.57659542575977,2.53423360678579));
#46857=CARTESIAN_POINT('Ctrl Pts',(5.81079840657738,0.547206640537195,2.6926232072099));
#46858=CARTESIAN_POINT('Ctrl Pts',(2.70403255420632,5.17233203472232,2.85101280763401));
#46859=CARTESIAN_POINT('Ctrl Pts',(-2.86695818216828,5.08383316810077,3.00940240805812));
#46860=CARTESIAN_POINT('Ctrl Pts',(-5.82524720767244,0.362361139892822,
3.16779200848224));
#46861=CARTESIAN_POINT('Ctrl Pts',(-3.47490092916519,-4.68933616588121,
3.32618160890635));
#46862=CARTESIAN_POINT('Ctrl Pts',(2.04217461014913,-5.46757101534546,3.48457120933046));
#46863=CARTESIAN_POINT('Ctrl Pts',(5.698185836302,-1.26312642509933,3.64296080975457));
#46864=CARTESIAN_POINT('Ctrl Pts',(4.16135481900965,4.09242424193511,3.80135041017868));
#46865=CARTESIAN_POINT('Ctrl Pts',(-1.16778125175528,5.71848730306133,3.95974001060279));
#46866=CARTESIAN_POINT('Ctrl Pts',(-5.43270075753092,2.13320711609306,4.11812961102691));
#46867=CARTESIAN_POINT('Ctrl Pts',(-4.74671857244836,-3.39609671546603,
4.27651921145102));
#46868=CARTESIAN_POINT('Ctrl Pts',(0.265019444252462,-5.8304866692097,4.43490881187513));
#46869=CARTESIAN_POINT('Ctrl Pts',(5.03524126709262,-2.95146666801078,4.59329841229924));
#46870=CARTESIAN_POINT('Ctrl Pts',(5.21677219698313,2.61726917849946,4.75168801272335));
#46871=CARTESIAN_POINT('Ctrl Pts',(0.644180375313696,5.80084836485576,4.91007761314747));
#46872=CARTESIAN_POINT('Ctrl Pts',(-4.51546268484472,3.69802742693416,5.06846721357158));
#46873=CARTESIAN_POINT('Ctrl Pts',(-5.56009687081743,-1.77486137356051,
5.22685681399569));
#46874=CARTESIAN_POINT('Ctrl Pts',(-1.53773138009144,-5.63029238236797,
5.3852464144198));
#46875=CARTESIAN_POINT('Ctrl Pts',(3.88599178244287,-4.35475349189019,5.54363601484391));
#46876=CARTESIAN_POINT('Ctrl Pts',(5.7683523459164,0.889337574631424,5.70202561526803));
#46877=CARTESIAN_POINT('Ctrl Pts',(2.39392689448955,5.32296196981904,5.86041521569214));
#46878=CARTESIAN_POINT('Ctrl Pts',(-3.16212004345771,4.90569128044887,6.01880481611624));
#46879=CARTESIAN_POINT('Ctrl Pts',(-5.8364795557618,0.0177905445684291,
6.17719441654037));
#46880=CARTESIAN_POINT('Ctrl Pts',(-3.19196770495921,-4.88632298142486,
6.33558401696446));
#46881=CARTESIAN_POINT('Ctrl Pts',(2.36143219311022,-5.33745708232365,6.49397361738859));
#46882=CARTESIAN_POINT('Ctrl Pts',(5.7628235134309,-0.924486485218232,6.65236321781269));
#46883=CARTESIAN_POINT('Ctrl Pts',(3.9124673268201,4.33098251264868,6.81075281823681));
#46884=CARTESIAN_POINT('Ctrl Pts',(-1.50337901955202,5.63956218441419,6.96914241866092));
#46885=CARTESIAN_POINT('Ctrl Pts',(-5.54917351555865,1.80872424723227,7.12753201908502));
#46886=CARTESIAN_POINT('Ctrl Pts',(-4.53792295232564,-3.6704312263084,7.28592161950915));
#46887=CARTESIAN_POINT('Ctrl Pts',(0.60880486367776,-5.80466766889078,7.44431121993324));
#46888=CARTESIAN_POINT('Ctrl Pts',(5.20071967567786,-2.64902339803196,7.60270082035738));
#46889=CARTESIAN_POINT('Ctrl Pts',(5.0531406393351,2.92071562932846,7.76109042078146));
#46890=CARTESIAN_POINT('Ctrl Pts',(0.300558744071995,5.82876269457468,7.9194800212056));
#46891=CARTESIAN_POINT('Ctrl Pts',(-4.72592684287763,3.42497088806201,8.07786962162969));
#46892=CARTESIAN_POINT('Ctrl Pts',(-5.44560441164323,-2.10004826139671,
8.23625922205382));
#46893=CARTESIAN_POINT('Ctrl Pts',(-1.20262099904615,-5.7112619306907,8.39464882247792));
#46894=CARTESIAN_POINT('Ctrl Pts',(4.13632896862666,-4.11771693679927,8.55303842290205));
#46895=CARTESIAN_POINT('Ctrl Pts',(5.70578030455996,1.22836526505724,8.71142802332614));
#46896=CARTESIAN_POINT('Ctrl Pts',(2.07546846542215,5.45501977607246,8.86981762375027));
#46897=CARTESIAN_POINT('Ctrl Pts',(-3.44624891712552,4.71043294289546,9.02820722417436));
#46898=CARTESIAN_POINT('Ctrl Pts',(-5.827347969683,-0.32684208501195,9.18659682459849));
#46899=CARTESIAN_POINT('Ctrl Pts',(-2.89789741049547,-5.06626101839879,
9.3449864250226));
#46900=CARTESIAN_POINT('Ctrl Pts',(2.6724505257232,-5.18872029462616,9.50337602544671));
#46901=CARTESIAN_POINT('Ctrl Pts',(5.80735421258137,-0.582620938447121,
9.66176562587082));
#46902=CARTESIAN_POINT('Ctrl Pts',(3.64992889843646,4.55442961792825,9.82015522629493));
#46903=CARTESIAN_POINT('Ctrl Pts',(-1.83373136775356,5.54096014957879,9.97854482671904));
#46904=CARTESIAN_POINT('Ctrl Pts',(-5.64628473356088,1.47793058560304,10.1369344271431));
#46905=CARTESIAN_POINT('Ctrl Pts',(-4.31329413054894,-3.93195928916814,
10.2953240275673));
#46906=CARTESIAN_POINT('Ctrl Pts',(0.950466110641093,-5.7585956865217,10.4537136279914));
#46907=CARTESIAN_POINT('Ctrl Pts',(5.34805232874179,-2.33733745902108,10.6121032284155));
#46908=CARTESIAN_POINT('Ctrl Pts',(4.87187824185477,3.2139714536451,10.7704928288396));
#46909=CARTESIAN_POINT('Ctrl Pts',(-0.0441115622938141,5.83633997282335,
10.9288824292637));
#46910=CARTESIAN_POINT('Ctrl Pts',(-4.91990183807518,3.13996433291973,11.0872720296878));
#46911=CARTESIAN_POINT('Ctrl Pts',(-5.31211177303214,-2.41790790128923,
11.2456616301119));
#46912=CARTESIAN_POINT('Ctrl Pts',(-0.863314570507911,-5.77230439778191,
11.404051230536));
#46913=CARTESIAN_POINT('Ctrl Pts',(4.37223414935776,-3.86631331522594,11.5624408309602));
#46914=CARTESIAN_POINT('Ctrl Pts',(5.6233003078374,1.56310708404107,11.7208304313843));
#46915=CARTESIAN_POINT('Ctrl Pts',(1.74976854941316,5.56804455188607,11.8792200318084));
#46916=CARTESIAN_POINT('Ctrl Pts',(-3.71835353364465,4.4987395020312,12.0376096322325));
#46917=CARTESIAN_POINT('Ctrl Pts',(-5.79788426826075,-0.670334334610817,
12.1959992326566));
#46918=CARTESIAN_POINT('Ctrl Pts',(-2.59371610417703,-5.22852243748043,
12.3543888330807));
#46919=CARTESIAN_POINT('Ctrl Pts',(2.97414444993972,-5.0218796181506,12.5127784335049));
#46920=CARTESIAN_POINT('Ctrl Pts',(5.83162255631666,-0.238722577403733,
12.6711680339289));
#46921=CARTESIAN_POINT('Ctrl Pts',(3.37465555603293,4.76198592883678,12.8295576343531));
#46922=CARTESIAN_POINT('Ctrl Pts',(-2.15768567041678,5.42302523099255,12.9879472347772));
#46923=CARTESIAN_POINT('Ctrl Pts',(-5.72369558133277,1.1419802977877,13.1463368352013));
#46924=CARTESIAN_POINT('Ctrl Pts',(-4.07361585673539,-4.17976840985925,
13.3047264356254));
#46925=CARTESIAN_POINT('Ctrl Pts',(1.28881110007321,-5.69243147140415,13.4631160360495));
#46926=CARTESIAN_POINT('Ctrl Pts',(5.47672516993668,-2.01749634975762,13.6215056364736));
#46927=CARTESIAN_POINT('Ctrl Pts',(4.67361744461052,3.49601345674377,13.7798952368977));
#46928=CARTESIAN_POINT('Ctrl Pts',(-0.388627959646856,5.82355376186139,
13.9382848373218));
#46929=CARTESIAN_POINT('Ctrl Pts',(-5.09671087507549,2.84400217373111,14.096674437746));
#46930=CARTESIAN_POINT('Ctrl Pts',(-5.16008472222368,-2.72733125376517,
14.2550640381701));
#46931=CARTESIAN_POINT('Ctrl Pts',(-0.520995963614669,-5.81320680126216,
14.4134536385942));
#46932=CARTESIAN_POINT('Ctrl Pts',(4.59288423128786,-3.60141979589384,14.5718432390183));
#46933=CARTESIAN_POINT('Ctrl Pts',(5.5212001355088,1.89239508874033,14.7302328394424));
#46934=CARTESIAN_POINT('Ctrl Pts',(1.41796354132297,5.66164194417672,14.8886224398665));
#46935=CARTESIAN_POINT('Ctrl Pts',(-3.97748449674956,4.27134957432729,15.0470120402906));
#46936=CARTESIAN_POINT('Ctrl Pts',(-5.74819125285225,-1.01148773031227,
15.2054016407147));
#46937=CARTESIAN_POINT('Ctrl Pts',(-2.28048510062285,-5.37254109486827,
15.3637912411389));
#46938=CARTESIAN_POINT('Ctrl Pts',(3.26546132992172,-4.8375171739695,15.5221808415629));
#46939=CARTESIAN_POINT('Ctrl Pts',(5.83554387019465,0.106008706524804,15.6805704419871));
#46940=CARTESIAN_POINT('Ctrl Pts',(3.08760775206024,4.95292726480458,15.8389600424112));
#46941=CARTESIAN_POINT('Ctrl Pts',(-2.4741116237025,5.2861689114788,15.9973496428353));
#46942=CARTESIAN_POINT('Ctrl Pts',(-5.78113596499847,0.802045547256652,
16.1557392432594));
#46943=CARTESIAN_POINT('Ctrl Pts',(-3.81972439042269,-4.4129939691809,16.3141288436835));
#46944=CARTESIAN_POINT('Ctrl Pts',(1.62265932033137,-5.60640586082788,16.4725184441076));
#46945=CARTESIAN_POINT('Ctrl Pts',(5.58628924306583,-1.69061605249735,16.6309080445317));
#46946=CARTESIAN_POINT('Ctrl Pts',(4.45905000728063,3.76585762592941,16.7892976449558));
#46947=CARTESIAN_POINT('Ctrl Pts',(-0.731788421472935,5.79044856687125,
16.94768724538));
#46948=CARTESIAN_POINT('Ctrl Pts',(-5.25573701254373,2.53811725233494,17.106076845804));
#46949=CARTESIAN_POINT('Ctrl Pts',(-4.99005377008544,-3.02723910535429,
17.2644664462282));
#46950=CARTESIAN_POINT('Ctrl Pts',(-0.176859412942431,-5.83382568153235,
17.4228560466523));
#46951=CARTESIAN_POINT('Ctrl Pts',(4.79750907152224,-3.32396204419444,17.5812456470764));
#46952=CARTESIAN_POINT('Ctrl Pts',(5.39983655124094,2.21508309751895,17.7396352475005));
#46953=CARTESIAN_POINT('Ctrl Pts',(1.08121012887367,5.73548016004241,17.8980248479246));
#46954=CARTESIAN_POINT('Ctrl Pts',(-4.22273574869486,4.02906652888012,18.0564144483487));
#46955=CARTESIAN_POINT('Ctrl Pts',(-5.67844599183081,-1.34913104982561,
18.2148040487729));
#46956=CARTESIAN_POINT('Ctrl Pts',(-1.95929024443088,-5.4977779998395,18.373193649197));
#46957=CARTESIAN_POINT('Ctrl Pts',(3.54537126761076,-4.63634599208567,18.5315832496211));
#46958=CARTESIAN_POINT('Ctrl Pts',(5.81913022087222,0.450503506445362,18.6899728500452));
#46959=CARTESIAN_POINT('Ctrl Pts',(2.78973779641457,5.12633240329489,18.8483624504693));
#46960=CARTESIAN_POINT('Ctrl Pts',(-2.78181108657403,5.13135624750109,19.0067520508934));
#46961=CARTESIAN_POINT('Ctrl Pts',(-5.81858536544488,0.458380006525366,
19.1651416513175));
#46962=CARTESIAN_POINT('Ctrl Pts',(-3.55216173231372,-4.62903696208274,
19.3235312517416));
#46963=CARTESIAN_POINT('Ctrl Pts',(1.95018918427537,-5.50425664698007,19.4819208521657));
#46964=CARTESIAN_POINT('Ctrl Pts',(5.67761237270639,-1.3510454371489,19.6403104525899));
#46965=CARTESIAN_POINT('Ctrl Pts',(4.46844825305886,3.11451982677256,19.7723017862766));
#46966=CARTESIAN_POINT('Ctrl Pts',(1.57655429378253,4.89442301364916,19.877894853226));
#46967=CARTESIAN_POINT('Ctrl Pts',(-0.102289207481715,5.00847467404178,
19.9306913867007));
#46968=CARTESIAN_POINT('Ctrl Pts',(-0.908039552611985,4.857862510497,19.9570896534381));
#46969=CARTESIAN_POINT('Ctrl Pts',(-4.94192999916445,-0.00446510791632448,
18.1776795453431));
#46970=CARTESIAN_POINT('Ctrl Pts',(-4.94542698461402,-0.388624254474772,
18.1900543798197));
#46971=CARTESIAN_POINT('Ctrl Pts',(-4.90438878928145,-0.772044124408378,
18.2024292142963));
#46972=CARTESIAN_POINT('Ctrl Pts',(-4.81596832674149,-1.14420594504366,
18.2148040487729));
#46973=CARTESIAN_POINT('Ctrl Pts',(-4.43872740936416,-2.73201336649694,
18.2676005822476));
#46974=CARTESIAN_POINT('Ctrl Pts',(-3.19900882689749,-4.11489568316824,
18.3203971157223));
#46975=CARTESIAN_POINT('Ctrl Pts',(-1.66170595032388,-4.66276484021157,
18.373193649197));
#46976=CARTESIAN_POINT('Ctrl Pts',(-0.124403073750308,-5.21063399725488,
18.4259901826717));
#46977=CARTESIAN_POINT('Ctrl Pts',(1.71048409693019,-4.92348999467027,18.4787867161464));
#46978=CARTESIAN_POINT('Ctrl Pts',(3.00688750781402,-3.93210974362283,18.5315832496211));
#46979=CARTESIAN_POINT('Ctrl Pts',(4.3032909186979,-2.94072949257537,18.5843797830958));
#46980=CARTESIAN_POINT('Ctrl Pts',(5.06121056978506,-1.24511299306501,18.6371763165705));
#46981=CARTESIAN_POINT('Ctrl Pts',(4.93527165791903,0.38200007283176,18.6899728500452));
#46982=CARTESIAN_POINT('Ctrl Pts',(4.80933274605301,2.00911313872853,18.7427693835199));
#46983=CARTESIAN_POINT('Ctrl Pts',(3.79953527123378,3.56772277101172,18.7955659169946));
#46984=CARTESIAN_POINT('Ctrl Pts',(2.36604505332606,4.34786489452101,18.8483624504693));
#46985=CARTESIAN_POINT('Ctrl Pts',(0.932554835418334,5.1280070180303,18.901158983944));
#46986=CARTESIAN_POINT('Ctrl Pts',(-0.92462812557789,5.12968163276569,18.9539555174187));
#46987=CARTESIAN_POINT('Ctrl Pts',(-2.35934865255447,4.3516895666374,19.0067520508934));
#46988=CARTESIAN_POINT('Ctrl Pts',(-2.82356148188028,4.09996535176783,19.0238347005956));
#46989=CARTESIAN_POINT('Ctrl Pts',(-3.24354728379133,3.7666188744385,19.0409173502978));
#46990=CARTESIAN_POINT('Ctrl Pts',(-3.60367707498796,3.37571982724537,19.058));
#46991=CARTESIAN_POINT('Ctrl Pts',(-2.54467524200881,-3.56229978442281,
-6.93889390390723E-18));
#46992=CARTESIAN_POINT('Ctrl Pts',(-2.64087676169121,-3.50326719695733,
3.78010404015323E-18));
#46993=CARTESIAN_POINT('Ctrl Pts',(-2.73444512499906,-3.44042480726573,
1.70774935809012E-16));
#46994=CARTESIAN_POINT('Ctrl Pts',(-2.82511133337028,-3.37382080685403,
1.33573707650214E-16));
#46995=CARTESIAN_POINT('Ctrl Pts',(-2.93010592262241,-3.29669108243516,
6.34680042936623E-17));
#46996=CARTESIAN_POINT('Ctrl Pts',(-3.0312098993845,-3.21451805045997,-1.1579302301566E-16));
#46997=CARTESIAN_POINT('Ctrl Pts',(-3.12833116102487,-3.1277186925041,-1.87350135405495E-16));
#46998=CARTESIAN_POINT('Ctrl Pts',(-3.19203631412683,-3.07078402861756,
-2.34286889761188E-16));
#46999=CARTESIAN_POINT('Ctrl Pts',(-3.25402740755314,-3.01185787186213,
2.54730009275007E-16));
#47000=CARTESIAN_POINT('Ctrl Pts',(-3.3142718238098,-2.95104792020956,3.67761376907083E-16));
#47001=CARTESIAN_POINT('Ctrl Pts',(-3.34056115234898,-2.92451180455305,
4.17085761531429E-16));
#47002=CARTESIAN_POINT('Ctrl Pts',(-3.36651779652415,-2.8976168731598,-1.29958168485043E-16));
#47003=CARTESIAN_POINT('Ctrl Pts',(-3.39213869657566,-2.87037166754254,
-1.66533453693773E-16));
#47004=CARTESIAN_POINT('Ctrl Pts',(-3.4107075535189,-2.85062558819017,-1.9304154815313E-16));
#47005=CARTESIAN_POINT('Ctrl Pts',(-3.42910165503002,-2.83069359301782,
5.20445990861309E-16));
#47006=CARTESIAN_POINT('Ctrl Pts',(-3.44730402197008,-2.81059669044114,
5.13478148889135E-16));
#47007=CARTESIAN_POINT('Ctrl Pts',(-3.53659117665104,-2.71201636542733,
4.79299144256909E-16));
#47008=CARTESIAN_POINT('Ctrl Pts',(-3.62135066124632,-2.60938482813861,
1.69265913904123E-16));
#47009=CARTESIAN_POINT('Ctrl Pts',(-3.70148784592851,-2.50313357384095,
1.80411241501588E-16));
#47010=CARTESIAN_POINT('Ctrl Pts',(-3.78346559823418,-2.39444197154017,
1.91812551751929E-16));
#47011=CARTESIAN_POINT('Ctrl Pts',(-3.86060678067413,-2.28196193869908,
-1.60403205534396E-16));
#47012=CARTESIAN_POINT('Ctrl Pts',(-3.93277586934314,-2.16611326123794,
-5.55111512312578E-17));
#47013=CARTESIAN_POINT('Ctrl Pts',(-3.96434984563583,-2.1154294648487,-9.62087747363501E-18));
#47014=CARTESIAN_POINT('Ctrl Pts',(-3.99497165206884,-2.06410040223293,
2.30246512287273E-16));
#47015=CARTESIAN_POINT('Ctrl Pts',(-4.02462756948077,-2.01215919201488,
2.91433543964104E-16));
#47016=CARTESIAN_POINT('Ctrl Pts',(-4.03961656660672,-1.98590653424469,
3.22359319390632E-16));
#47017=CARTESIAN_POINT('Ctrl Pts',(-4.05435879396083,-1.95949747991113,
2.06007824657555E-17));
#47018=CARTESIAN_POINT('Ctrl Pts',(-4.06885232846184,-1.93293620549746,
1.38777878078145E-17));
#47019=CARTESIAN_POINT('Ctrl Pts',(-4.08041475408644,-1.91174656677398,
8.51442211522865E-18));
#47020=CARTESIAN_POINT('Ctrl Pts',(-4.09181979945551,-1.89045816584063,
2.1634594979841E-16));
#47021=CARTESIAN_POINT('Ctrl Pts',(-4.10305617212226,-1.86909315496197,
2.08166817117217E-16));
#47022=CARTESIAN_POINT('Ctrl Pts',(-4.16736596175704,-1.74681353716178,
1.61354708109947E-16));
#47023=CARTESIAN_POINT('Ctrl Pts',(-4.22623125974132,-1.62188769970873,
-1.58091925840003E-16));
#47024=CARTESIAN_POINT('Ctrl Pts',(-4.27954887166761,-1.49476314498018,
-1.66533453693773E-16));
#47025=CARTESIAN_POINT('Ctrl Pts',(-4.33347479304113,-1.36618820519452,
-1.75071292334113E-16));
#47026=CARTESIAN_POINT('Ctrl Pts',(-4.38172617240059,-1.23536340764327,
-1.43714543602008E-16));
#47027=CARTESIAN_POINT('Ctrl Pts',(-4.42415678995003,-1.10271583109255,
-9.71445146547012E-17));
#47028=CARTESIAN_POINT('Ctrl Pts',(-4.46710218965978,-0.968458930662989,
-5.00094828511621E-17));
#47029=CARTESIAN_POINT('Ctrl Pts',(-4.50408524649974,-0.832334009558243,
-1.01069852635313E-16));
#47030=CARTESIAN_POINT('Ctrl Pts',(-4.53490679318661,-0.694758137572736,
-1.38777878078145E-16));
#47031=CARTESIAN_POINT('Ctrl Pts',(-4.55802295320176,-0.591576233583606,
-1.67058897160268E-16));
#47032=CARTESIAN_POINT('Ctrl Pts',(-4.5776723273625,-0.487577560717138,
-2.48733805589575E-17));
#47033=CARTESIAN_POINT('Ctrl Pts',(-4.59375100179198,-0.38293266212137,
-5.55111512312578E-17));
#47034=CARTESIAN_POINT('Ctrl Pts',(-4.60074932415958,-0.337385453754768,
-6.88463920640666E-17));
#47035=CARTESIAN_POINT('Ctrl Pts',(-4.60707095895173,-0.291715781756126,
-3.50051711561292E-16));
#47036=CARTESIAN_POINT('Ctrl Pts',(-4.61270623945594,-0.245937595982269,
-3.60822483003176E-16));
#47037=CARTESIAN_POINT('Ctrl Pts',(-4.61510536794149,-0.226448282287078,
-3.65407962742523E-16));
#47038=CARTESIAN_POINT('Ctrl Pts',(-4.61738026973089,-0.206937176747096,
-2.11235974110856E-16));
#47039=CARTESIAN_POINT('Ctrl Pts',(-4.61952832377542,-0.187423425576886,
-2.22044604925031E-16));
#47040=CARTESIAN_POINT('Ctrl Pts',(-4.63503826526744,-0.0465251368621273,
-3.00087907403534E-16));
#47041=CARTESIAN_POINT('Ctrl Pts',(-4.64396392467283,0.0947008669712182,
-1.99183435512137E-16));
#47042=CARTESIAN_POINT('Ctrl Pts',(-4.64615947496329,0.235825173850752,
-2.22044604925031E-16));
#47043=CARTESIAN_POINT('Ctrl Pts',(-4.64786848339456,0.345675825581053,
-2.39839656782873E-16));
#47044=CARTESIAN_POINT('Ctrl Pts',(-4.64549890174975,0.455465549450203,
-1.5964104232527E-16));
#47045=CARTESIAN_POINT('Ctrl Pts',(-4.63896138884064,0.56499930567962,-1.38777878078145E-16));
#47046=CARTESIAN_POINT('Ctrl Pts',(-4.63077575597687,0.702146738831947,
-1.08813479195783E-16));
#47047=CARTESIAN_POINT('Ctrl Pts',(-4.61605776615402,0.838893185885087,
-2.45094142526848E-16));
#47048=CARTESIAN_POINT('Ctrl Pts',(-4.59507497843275,0.974861012835041,
-2.22044604925031E-16));
#47049=CARTESIAN_POINT('Ctrl Pts',(-4.57379787866946,1.11273597287572,-1.98671766312435E-16));
#47050=CARTESIAN_POINT('Ctrl Pts',(-4.54607882402517,1.24981106593623,-1.79874459778951E-16));
#47051=CARTESIAN_POINT('Ctrl Pts',(-4.51214338117474,1.38568894112939,-8.32667268468867E-17));
#47052=CARTESIAN_POINT('Ctrl Pts',(-4.50044605637916,1.43252515439685,-4.99666743073618E-17));
#47053=CARTESIAN_POINT('Ctrl Pts',(-4.48800969217396,1.47921903836149,8.24656052999656E-18));
#47054=CARTESIAN_POINT('Ctrl Pts',(-4.47484214689978,1.52575396812219,5.55111512312578E-17));
#47055=CARTESIAN_POINT('Ctrl Pts',(-4.46954654891505,1.54446894309507,7.45195742938095E-17));
#47056=CARTESIAN_POINT('Ctrl Pts',(-4.4641321445575,1.56316001192783,2.98076212871544E-17));
#47057=CARTESIAN_POINT('Ctrl Pts',(-4.45860111065483,1.58182037106622,2.77555756156289E-17));
#47058=CARTESIAN_POINT('Ctrl Pts',(-4.41871853179728,1.7163744631118,1.29589074421813E-17));
#47059=CARTESIAN_POINT('Ctrl Pts',(-4.37289155988743,1.84894716867807,-3.65495115057949E-16));
#47060=CARTESIAN_POINT('Ctrl Pts',(-4.32143318995775,1.97915634222774,-3.60822483003176E-16));
#47061=CARTESIAN_POINT('Ctrl Pts',(-4.26919198995651,2.11134637247354,-3.56078766751783E-16));
#47062=CARTESIAN_POINT('Ctrl Pts',(-4.21114654432903,2.24110115829447,1.76811505571791E-16));
#47063=CARTESIAN_POINT('Ctrl Pts',(-4.147570486657,2.36801906886784,1.66533453693773E-16));
#47064=CARTESIAN_POINT('Ctrl Pts',(-4.08343929176894,2.49604520883007,1.56165655308743E-16));
#47065=CARTESIAN_POINT('Ctrl Pts',(-4.01368020422711,2.62118552486071,-5.6466401912637E-17));
#47066=CARTESIAN_POINT('Ctrl Pts',(-3.93852341174026,2.7430141593252,-2.77555756156289E-17));
#47067=CARTESIAN_POINT('Ctrl Pts',(-3.9294168218154,2.75777587784009,-2.4276745388323E-17));
#47068=CARTESIAN_POINT('Ctrl Pts',(-3.9202309270139,2.77248895031151,-1.25624424874937E-18));
#47069=CARTESIAN_POINT('Ctrl Pts',(-3.91096608990011,2.78715259668566,0.));
#47070=CARTESIAN_POINT('Ctrl Pts',(-3.85692740501027,2.87268072373382,-4.76202655277902E-17));
#47071=CARTESIAN_POINT('Ctrl Pts',(-3.80020397437343,2.95652797095731,1.2876992925575E-16));
#47072=CARTESIAN_POINT('Ctrl Pts',(-3.74088150109056,3.03859647479229,1.66533453693773E-16));
#47073=CARTESIAN_POINT('Ctrl Pts',(-3.7149279190293,3.0745014452201,1.83054995635409E-16));
#47074=CARTESIAN_POINT('Ctrl Pts',(-3.68847672600951,3.11006585723381,-1.71465257258441E-16));
#47075=CARTESIAN_POINT('Ctrl Pts',(-3.66153447975748,3.14528103385681,-1.66533453693773E-16));
#47076=CARTESIAN_POINT('Ctrl Pts',(-3.64469680263863,3.16728891575776,-1.6345130103068E-16));
#47077=CARTESIAN_POINT('Ctrl Pts',(-3.62766732852701,3.18916039136048,2.64610714971295E-16));
#47078=CARTESIAN_POINT('Ctrl Pts',(-3.6104475878738,3.21089327815198,2.77555756156289E-16));
#47079=CARTESIAN_POINT('Ctrl Pts',(-3.59895112257703,3.22540286826887,2.86198291473495E-16));
#47080=CARTESIAN_POINT('Ctrl Pts',(-3.58737284218715,3.23984685581822,3.27202329850872E-16));
#47081=CARTESIAN_POINT('Ctrl Pts',(-3.57571845845413,3.25421848714644,3.33066907387547E-16));
#47082=CARTESIAN_POINT('Ctrl Pts',(-3.4847651283665,3.36637780487935,3.78835338283328E-16));
#47083=CARTESIAN_POINT('Ctrl Pts',(-3.38908875605728,3.4742480319481,-5.71170610872501E-17));
#47084=CARTESIAN_POINT('Ctrl Pts',(-3.28901395033307,3.5775964314093,-5.55111512312578E-17));
#47085=CARTESIAN_POINT('Ctrl Pts',(-3.1878935796381,3.68202459780562,-5.38884630954632E-17));
#47086=CARTESIAN_POINT('Ctrl Pts',(-3.08228201196636,3.78183656326097,2.20761671403476E-16));
#47087=CARTESIAN_POINT('Ctrl Pts',(-2.97246730240431,3.87676781486652,2.77555756156289E-16));
#47088=CARTESIAN_POINT('Ctrl Pts',(-2.86296602007246,3.97142811880605,3.34187742290929E-16));
#47089=CARTESIAN_POINT('Ctrl Pts',(-2.74928508452755,4.0612360937228,2.13145292818159E-16));
#47090=CARTESIAN_POINT('Ctrl Pts',(-2.63167026985783,4.14589663192155,2.22044604925031E-16));
#47091=CARTESIAN_POINT('Ctrl Pts',(-2.51583556938655,4.22927582281283,2.3080922488549E-16));
#47092=CARTESIAN_POINT('Ctrl Pts',(-2.39618466430397,4.30766267709754,-5.76377990669945E-17));
#47093=CARTESIAN_POINT('Ctrl Pts',(-2.27292097783335,4.38073587186789,-1.11022302462516E-16));
#47094=CARTESIAN_POINT('Ctrl Pts',(-2.23861641107446,4.40107230963037,-1.25879332241991E-16));
#47095=CARTESIAN_POINT('Ctrl Pts',(-2.2040318620339,4.42099693210222,2.77555756156289E-16));
#47096=CARTESIAN_POINT('Ctrl Pts',(-2.1691713542861,4.440502182833,2.77555756156289E-16));
#47097=CARTESIAN_POINT('Origin',(0.,0.,0.));
#47098=CARTESIAN_POINT('Origin',(-2.30940107675851,-4.,-10.));
#47099=CARTESIAN_POINT('',(-2.30940107675851,-4.,-10.));
#47100=CARTESIAN_POINT('',(2.3094010767585,-4.,-10.));
#47101=CARTESIAN_POINT('',(-1.15470053837925,-4.,-10.));
#47102=CARTESIAN_POINT('',(-2.30940107675851,-4.,-4.));
#47103=CARTESIAN_POINT('',(-2.30940107675851,-4.,-10.));
#47104=CARTESIAN_POINT('',(2.3094010767585,-4.,-4.));
#47105=CARTESIAN_POINT('',(-2.30940107675851,-4.,-4.));
#47106=CARTESIAN_POINT('',(2.3094010767585,-4.,-10.));
#47107=CARTESIAN_POINT('Origin',(-4.61880215351701,5.6564012731995E-16,
-10.));
#47108=CARTESIAN_POINT('',(-4.61880215351701,5.6564012731995E-16,-10.));
#47109=CARTESIAN_POINT('',(-4.04145188432738,-0.999999999999999,-10.));
#47110=CARTESIAN_POINT('',(-4.61880215351701,5.55111512312578E-16,-4.));
#47111=CARTESIAN_POINT('',(-4.61880215351701,5.6564012731995E-16,-10.));
#47112=CARTESIAN_POINT('',(-4.61880215351701,5.6564012731995E-16,-4.));
#47113=CARTESIAN_POINT('Origin',(-2.3094010767585,4.,-10.));
#47114=CARTESIAN_POINT('',(-2.3094010767585,4.,-10.));
#47115=CARTESIAN_POINT('',(-2.88675134594813,3.,-10.));
#47116=CARTESIAN_POINT('',(-2.3094010767585,4.,-4.));
#47117=CARTESIAN_POINT('',(-2.3094010767585,4.,-10.));
#47118=CARTESIAN_POINT('',(-2.3094010767585,4.,-4.));
#47119=CARTESIAN_POINT('Origin',(2.3094010767585,4.,-10.));
#47120=CARTESIAN_POINT('',(2.3094010767585,4.,-10.));
#47121=CARTESIAN_POINT('',(1.15470053837925,4.,-10.));
#47122=CARTESIAN_POINT('',(2.3094010767585,4.,-4.));
#47123=CARTESIAN_POINT('',(2.3094010767585,4.,-10.));
#47124=CARTESIAN_POINT('',(2.3094010767585,4.,-4.));
#47125=CARTESIAN_POINT('Origin',(4.61880215351701,0.,-10.));
#47126=CARTESIAN_POINT('',(4.61880215351701,0.,-10.));
#47127=CARTESIAN_POINT('',(4.04145188432738,1.,-10.));
#47128=CARTESIAN_POINT('',(4.61880215351701,0.,-4.));
#47129=CARTESIAN_POINT('',(4.61880215351701,0.,-10.));
#47130=CARTESIAN_POINT('',(4.61880215351701,0.,-4.));
#47131=CARTESIAN_POINT('Origin',(2.3094010767585,-4.,-10.));
#47132=CARTESIAN_POINT('',(2.88675134594813,-3.,-10.));
#47133=CARTESIAN_POINT('',(2.3094010767585,-4.,-4.));
#47134=CARTESIAN_POINT('Origin',(0.,0.,-4.));
#47135=CARTESIAN_POINT('Origin',(0.,0.,0.));
#47136=CARTESIAN_POINT('',(-8.,-9.79717439317883E-16,0.));
#47137=CARTESIAN_POINT('Origin',(0.,0.,0.));
#47138=CARTESIAN_POINT('Origin',(0.,0.,-10.));
#47139=CARTESIAN_POINT('',(-8.,-9.79717439317883E-16,-10.));
#47140=CARTESIAN_POINT('',(-8.,-9.79717439317883E-16,-10.));
#47141=CARTESIAN_POINT('Origin',(0.,0.,-10.));
#47142=CARTESIAN_POINT('Origin',(0.,0.,-10.));
#47143=CARTESIAN_POINT('Origin',(0.,0.,20.));
#63726=UNCERTAINTY_MEASURE_WITH_UNIT(LENGTH_MEASURE(0.01),#63756,
'DISTANCE_ACCURACY_VALUE',
'Maximum model space distance between geometric entities at asserted c
onnectivities');
#63735=UNCERTAINTY_MEASURE_WITH_UNIT(LENGTH_MEASURE(0.01),#63756,
'DISTANCE_ACCURACY_VALUE',
'Maximum model space distance between geometric entities at asserted c
onnectivities');
#63746=(
GEOMETRIC_REPRESENTATION_CONTEXT(3)
GLOBAL_UNCERTAINTY_ASSIGNED_CONTEXT((#63726))
GLOBAL_UNIT_ASSIGNED_CONTEXT((#63756,#63758,#63759))
REPRESENTATION_CONTEXT('','3D')
);
#63755=(
GEOMETRIC_REPRESENTATION_CONTEXT(3)
GLOBAL_UNCERTAINTY_ASSIGNED_CONTEXT((#63735))
GLOBAL_UNIT_ASSIGNED_CONTEXT((#63756,#63758,#63759))
REPRESENTATION_CONTEXT('','3D')
);
#63756=(
LENGTH_UNIT()
NAMED_UNIT(*)
SI_UNIT(.MILLI.,.METRE.)
);
#63758=(
NAMED_UNIT(*)
PLANE_ANGLE_UNIT()
SI_UNIT($,.RADIAN.)
);
#63759=(
NAMED_UNIT(*)
SI_UNIT($,.STERADIAN.)
SOLID_ANGLE_UNIT()
);
#63770=SHAPE_DEFINITION_REPRESENTATION(#63829,#63868);
#63829=PRODUCT_DEFINITION_SHAPE('',$,#63888);
#63868=SHAPE_REPRESENTATION('',(#15079),#63746);
#63877=PRODUCT_DEFINITION_CONTEXT('part definition',#63936,'design');
#63888=PRODUCT_DEFINITION('Socket head cap screw M10x20',
'Socket head cap screw M10x20',#63907,#63877);
#63907=PRODUCT_DEFINITION_FORMATION('',$,#63948);
#63936=APPLICATION_CONTEXT(
'Core Data for Automotive Mechanical Design Process');
#63937=PRODUCT_CONTEXT('part definition',#63936,'mechanical');
#63948=PRODUCT('Socket head cap screw M10x20',
'Socket head cap screw M10x20',$,(#63937));
#63960=PRESENTATION_STYLE_ASSIGNMENT((#63967));
#63967=SURFACE_STYLE_USAGE(.BOTH.,#63974);
#63974=SURFACE_SIDE_STYLE('',(#63981));
#63981=SURFACE_STYLE_FILL_AREA(#63988);
#63988=FILL_AREA_STYLE('Dark gray',(#63995));
#63995=FILL_AREA_STYLE_COLOUR('Dark gray',#64002);
#64002=COLOUR_RGB('Dark gray',0.250980392156863,0.282352941176471,0.32156862745098);
ENDSEC;
END-ISO-10303-21;
